ISO-10303-21;
HEADER;
FILE_DESCRIPTION (('STEP AP214'),
    '1' );
FILE_NAME ('slotted pan head screw_iso_ISO 1580 - M5 x 25 - 25S.step',
    '2026-10-06T08:51:13',
    ( '' ),
    ( '' ),
    'SwSTEP 2.0',
    'SolidWorks 2021',
    '' );
FILE_SCHEMA (( 'AUTOMOTIVE_DESIGN' ));
ENDSEC;

DATA;
#27=ORIENTED_EDGE ( 'NONE', *, *, #125600, .F. ) ;
#34=ORIENTED_EDGE ( 'NONE', *, *, #95665, .T. ) ;
#44=AXIS2_PLACEMENT_3D ( 'NONE', #3347, #93234, #125883 ) ;
#73=VECTOR ( 'NONE', #82018, 1000.000000000000114 ) ;
#186=DIRECTION ( 'NONE',  ( 0.9961946980917455452, 0.000000000000000000, -0.08715574274765836016 ) ) ;
#213=AXIS2_PLACEMENT_3D ( 'NONE', #103469, #123843, #48393 ) ;
#278=ORIENTED_EDGE ( 'NONE', *, *, #76259, .F. ) ;
#298=DIRECTION ( 'NONE',  ( -1.000000000000000000, -1.224606353822377258E-16, -0.000000000000000000 ) ) ;
#306=VECTOR ( 'NONE', #44663, 1000.000000000000114 ) ;
#380=CARTESIAN_POINT ( 'NONE',  ( 10.37159235450332062, -3.851859888774471706E-31, 2.500000000000001332 ) ) ;
#395=VECTOR ( 'NONE', #66581, 1000.000000000000114 ) ;
#428=SHAPE_REPRESENTATION ( 'slotted pan head screw_iso_ISO 1580 - M5 x 25 - 25S', ( #127880 ), #95551 ) ;
#496=DIRECTION ( 'NONE',  ( -1.000000000000000000, 0.000000000000000000, -0.000000000000000000 ) ) ;
#549=ORIENTED_EDGE ( 'NONE', *, *, #89231, .T. ) ;
#573=ORIENTED_EDGE ( 'NONE', *, *, #143462, .T. ) ;
#577=AXIS2_PLACEMENT_3D ( 'NONE', #85870, #75032, #8969 ) ;
#618=ORIENTED_EDGE ( 'NONE', *, *, #37492, .F. ) ;
#638=VECTOR ( 'NONE', #31363, 999.9999999999998863 ) ;
#665=CIRCLE ( 'NONE', #130268, 2.500000000000000888 ) ;
#682=ORIENTED_EDGE ( 'NONE', *, *, #122898, .T. ) ;
#726=CIRCLE ( 'NONE', #7757, 2.500000000000000888 ) ;
#767=ADVANCED_FACE ( 'NONE', ( #62489 ), #137913, .T. ) ;
#770=DIRECTION ( 'NONE',  ( 0.000000000000000000, 0.000000000000000000, 1.000000000000000000 ) ) ;
#786=VERTEX_POINT ( 'NONE', #82823 ) ;
#802=VECTOR ( 'NONE', #88315, 1000.000000000000000 ) ;
#827=CIRCLE ( 'NONE', #47185, 2.500000000000000888 ) ;
#850=DIRECTION ( 'NONE',  ( 0.000000000000000000, 1.000000000000000000, 0.000000000000000000 ) ) ;
#901=CONICAL_SURFACE ( 'NONE', #118993, 2.500000000000000888, 0.9599310885968822538 ) ;
#943=DIRECTION ( 'NONE',  ( -1.000000000000000000, -1.224606353822377258E-16, -0.000000000000000000 ) ) ;
#964=DIRECTION ( 'NONE',  ( 0.000000000000000000, -1.000000000000000000, 0.000000000000000000 ) ) ;
#1030=ORIENTED_EDGE ( 'NONE', *, *, #40797, .F. ) ;
#1045=ORIENTED_EDGE ( 'NONE', *, *, #27467, .F. ) ;
#1075=ADVANCED_FACE ( 'NONE', ( #137562 ), #126651, .T. ) ;
#1096=CARTESIAN_POINT ( 'NONE',  ( 6.160000000000001030, 9.521314400968980422E-16, 0.000000000000000000 ) ) ;
#1180=DIRECTION ( 'NONE',  ( -1.000000000000000000, -0.000000000000000000, -0.000000000000000000 ) ) ;
#1247=CARTESIAN_POINT ( 'NONE',  ( 14.27159235450332098, -5.777789833161707559E-31, 2.500000000000001332 ) ) ;
#1262=DIRECTION ( 'NONE',  ( -1.000000000000000000, -1.224606353822377258E-16, -0.000000000000000000 ) ) ;
#1284=FACE_OUTER_BOUND ( 'NONE', #26117, .T. ) ;
#1301=AXIS2_PLACEMENT_3D ( 'NONE', #51952, #96133, #42518 ) ;
#1303=CYLINDRICAL_SURFACE ( 'NONE', #112184, 2.500000000000000000 ) ;
#1306=ORIENTED_EDGE ( 'NONE', *, *, #112485, .F. ) ;
#1314=CARTESIAN_POINT ( 'NONE',  ( 16.61159235450331906, 9.902892378096218942E-16, 0.000000000000000000 ) ) ;
#1361=DIRECTION ( 'NONE',  ( -1.000000000000000000, -1.224606353822377258E-16, -0.000000000000000000 ) ) ;
#1369=ORIENTED_EDGE ( 'NONE', *, *, #69640, .T. ) ;
#1386=CARTESIAN_POINT ( 'NONE',  ( 11.62000000000000099, 9.521314400968980422E-16, 0.000000000000000000 ) ) ;
#1387=ORIENTED_EDGE ( 'NONE', *, *, #16307, .T. ) ;
#1426=DIRECTION ( 'NONE',  ( -1.000000000000000000, -1.224606353822377258E-16, -0.000000000000000000 ) ) ;
#1429=EDGE_CURVE ( 'NONE', #132789, #47888, #104377, .T. ) ;
#1435=CARTESIAN_POINT ( 'NONE',  ( 9.591592354503321260, 9.902892378096218942E-16, 0.000000000000000000 ) ) ;
#1500=DIRECTION ( 'NONE',  ( 0.000000000000000000, -1.000000000000000000, 0.000000000000000000 ) ) ;
#1508=EDGE_CURVE ( 'NONE', #97600, #63490, #117360, .T. ) ;
#1521=CARTESIAN_POINT ( 'NONE',  ( 8.031592354503320763, 9.902892378096218942E-16, 0.000000000000000000 ) ) ;
#1534=CARTESIAN_POINT ( 'NONE',  ( 22.22840764549667725, 2.499999999999998224, 3.061616997868380183E-16 ) ) ;
#1537=DIRECTION ( 'NONE',  ( -1.000000000000000000, -1.224606353822377258E-16, -0.000000000000000000 ) ) ;
#1562=AXIS2_PLACEMENT_3D ( 'NONE', #30778, #9700, #19164 ) ;
#1639=CARTESIAN_POINT ( 'NONE',  ( 26.75159235450331963, 9.902892378096218942E-16, 0.000000000000000000 ) ) ;
#1649=AXIS2_PLACEMENT_3D ( 'NONE', #62270, #141227, #120158 ) ;
#1657=ORIENTED_EDGE ( 'NONE', *, *, #84019, .T. ) ;
#1660=VERTEX_POINT ( 'NONE', #44906 ) ;
#1664=EDGE_CURVE ( 'NONE', #55674, #57540, #75352, .T. ) ;
#1673=VERTEX_POINT ( 'NONE', #141295 ) ;
#1701=DIRECTION ( 'NONE',  ( -1.000000000000000000, -1.224606353822377258E-16, -0.000000000000000000 ) ) ;
#1724=ORIENTED_EDGE ( 'NONE', *, *, #60406, .F. ) ;
#1738=DIRECTION ( 'NONE',  ( 0.000000000000000000, 1.000000000000000000, 0.000000000000000000 ) ) ;
#1781=EDGE_LOOP ( 'NONE', ( #23977, #96409, #94986, #23094, #121520 ) ) ;
#1782=DIRECTION ( 'NONE',  ( -1.000000000000000000, -1.224606353822377258E-16, -0.000000000000000000 ) ) ;
#1792=VERTEX_POINT ( 'NONE', #126670 ) ;
#1796=DIRECTION ( 'NONE',  ( 1.000000000000000000, 1.224606353822377258E-16, 0.000000000000000000 ) ) ;
#1828=DIRECTION ( 'NONE',  ( -1.000000000000000000, -1.224606353822377258E-16, -0.000000000000000000 ) ) ;
#1866=ORIENTED_EDGE ( 'NONE', *, *, #71450, .T. ) ;
#1891=AXIS2_PLACEMENT_3D ( 'NONE', #6712, #50996, #37990 ) ;
#1921=DIRECTION ( 'NONE',  ( 0.000000000000000000, -1.000000000000000000, 0.000000000000000000 ) ) ;
#1948=ORIENTED_EDGE ( 'NONE', *, *, #3075, .T. ) ;
#1985=DIRECTION ( 'NONE',  ( -1.000000000000000000, -0.000000000000000000, -0.000000000000000000 ) ) ;
#1998=VERTEX_POINT ( 'NONE', #64296 ) ;
#2006=CARTESIAN_POINT ( 'NONE',  ( 22.85159235450332105, 2.500000000000001332, 0.000000000000000000 ) ) ;
#2023=VECTOR ( 'NONE', #133398, 1000.000000000000000 ) ;
#2041=DIRECTION ( 'NONE',  ( -1.000000000000000000, -1.224606353822377258E-16, -0.000000000000000000 ) ) ;
#2050=ORIENTED_EDGE ( 'NONE', *, *, #77073, .T. ) ;
#2084=LINE ( 'NONE', #58715, #40119 ) ;
#2093=AXIS2_PLACEMENT_3D ( 'NONE', #101620, #135004, #2272 ) ;
#2103=CARTESIAN_POINT ( 'NONE',  ( 16.76840764549667639, 9.139736423841732040E-16, 0.000000000000000000 ) ) ;
#2105=FACE_OUTER_BOUND ( 'NONE', #89123, .T. ) ;
#2108=AXIS2_PLACEMENT_3D ( 'NONE', #116991, #80996, #28582 ) ;
#2109=CARTESIAN_POINT ( 'NONE',  ( 24.87999999999999901, 9.521314400968980422E-16, 0.000000000000000000 ) ) ;
#2133=CARTESIAN_POINT ( 'NONE',  ( 13.49159235450332162, 2.500000000000001332, 0.000000000000000000 ) ) ;
#2162=ORIENTED_EDGE ( 'NONE', *, *, #106738, .F. ) ;
#2170=EDGE_LOOP ( 'NONE', ( #48629, #11800, #111564, #134897, #33238 ) ) ;
#2182=CIRCLE ( 'NONE', #43947, 2.500000000000000888 ) ;
#2239=DIRECTION ( 'NONE',  ( 0.000000000000000000, -1.000000000000000000, 0.000000000000000000 ) ) ;
#2272=DIRECTION ( 'NONE',  ( 0.000000000000000000, -1.000000000000000000, 0.000000000000000000 ) ) ;
#2299=CIRCLE ( 'NONE', #106395, 2.500000000000000888 ) ;
#2309=DIRECTION ( 'NONE',  ( -1.000000000000000000, -1.224606353822377258E-16, -0.000000000000000000 ) ) ;
#2326=EDGE_CURVE ( 'NONE', #90786, #77143, #116725, .T. ) ;
#2351=CARTESIAN_POINT ( 'NONE',  ( 25.34840764549667469, 9.139736423841732040E-16, 0.000000000000000000 ) ) ;
#2353=FACE_OUTER_BOUND ( 'NONE', #96288, .T. ) ;
#2391=AXIS2_PLACEMENT_3D ( 'NONE', #101695, #56819, #113278 ) ;
#2394=DIRECTION ( 'NONE',  ( 0.000000000000000000, 0.000000000000000000, 1.000000000000000000 ) ) ;
#2406=AXIS2_PLACEMENT_3D ( 'NONE', #126695, #45099, #5621 ) ;
#2413=EDGE_LOOP ( 'NONE', ( #115330, #84092, #137165, #81660, #115388 ) ) ;
#2416=EDGE_CURVE ( 'NONE', #77035, #1792, #73239, .T. ) ;
#2498=AXIS2_PLACEMENT_3D ( 'NONE', #85312, #108468, #119361 ) ;
#2518=DIRECTION ( 'NONE',  ( 0.5735764363510453823, -0.8191520442889923537, 1.003171929053525486E-16 ) ) ;
#2554=CARTESIAN_POINT ( 'NONE',  ( 5.691592354503320905, 9.902892378096218942E-16, 0.000000000000000000 ) ) ;
#2625=CIRCLE ( 'NONE', #116051, 2.500000000000000888 ) ;
#2654=CARTESIAN_POINT ( 'NONE',  ( -25.39999999999996305, 0.000000000000000000, 2.500000000000000000 ) ) ;
#2704=DIRECTION ( 'NONE',  ( -1.000000000000000000, -0.000000000000000000, -0.000000000000000000 ) ) ;
#2727=EDGE_CURVE ( 'NONE', #109693, #12547, #75219, .T. ) ;
#2731=ORIENTED_EDGE ( 'NONE', *, *, #32007, .F. ) ;
#2750=ORIENTED_EDGE ( 'NONE', *, *, #14849, .F. ) ;
#2767=SURFACE_STYLE_FILL_AREA ( #121850 ) ;
#2770=ORIENTED_EDGE ( 'NONE', *, *, #28694, .T. ) ;
#2817=VECTOR ( 'NONE', #133730, 1000.000000000000114 ) ;
#2832=AXIS2_PLACEMENT_3D ( 'NONE', #48944, #83731, #105431 ) ;
#2841=ORIENTED_EDGE ( 'NONE', *, *, #48314, .F. ) ;
#2843=ORIENTED_EDGE ( 'NONE', *, *, #19754, .F. ) ;
#2889=EDGE_CURVE ( 'NONE', #3378, #79257, #26439, .T. ) ;
#2919=EDGE_LOOP ( 'NONE', ( #55155, #101299, #91850, #128345, #50723 ) ) ;
#3030=VERTEX_POINT ( 'NONE', #30740 ) ;
#3075=EDGE_CURVE ( 'NONE', #101812, #82012, #134955, .T. ) ;
#3101=FACE_OUTER_BOUND ( 'NONE', #121817, .T. ) ;
#3106=EDGE_CURVE ( 'NONE', #123367, #121372, #119141, .T. ) ;
#3117=ORIENTED_EDGE ( 'NONE', *, *, #101106, .T. ) ;
#3141=ORIENTED_EDGE ( 'NONE', *, *, #77429, .T. ) ;
#3160=CONICAL_SURFACE ( 'NONE', #86601, 2.500000000000000888, 0.9599310885968822538 ) ;
#3190=FACE_OUTER_BOUND ( 'NONE', #26742, .T. ) ;
#3217=EDGE_CURVE ( 'NONE', #3234, #139953, #116694, .T. ) ;
#3234=VERTEX_POINT ( 'NONE', #142352 ) ;
#3242=DIRECTION ( 'NONE',  ( -1.000000000000000000, -0.000000000000000000, -0.000000000000000000 ) ) ;
#3266=ORIENTED_EDGE ( 'NONE', *, *, #70615, .F. ) ;
#3294=DIRECTION ( 'NONE',  ( -1.000000000000000000, -1.224606353822377258E-16, -0.000000000000000000 ) ) ;
#3309=EDGE_LOOP ( 'NONE', ( #37255, #9683, #53883, #38811, #9565 ) ) ;
#3316=ORIENTED_EDGE ( 'NONE', *, *, #62044, .F. ) ;
#3347=CARTESIAN_POINT ( 'NONE',  ( 26.12840764549667583, 9.139736423841732040E-16, 0.000000000000000000 ) ) ;
#3353=CARTESIAN_POINT ( 'NONE',  ( 27.53159235450332076, -2.500000000000000000, 3.061616997868384127E-16 ) ) ;
#3355=CARTESIAN_POINT ( 'NONE',  ( -25.39999999999996305, 0.000000000000000000, 0.000000000000000000 ) ) ;
#3356=CARTESIAN_POINT ( 'NONE',  ( 23.63159235450331863, -7.703719777548943412E-31, 2.500000000000001332 ) ) ;
#3378=VERTEX_POINT ( 'NONE', #63222 ) ;
#3387=VERTEX_POINT ( 'NONE', #138612 ) ;
#3437=CARTESIAN_POINT ( 'NONE',  ( 27.99999999999999645, 9.521314400968980422E-16, 0.000000000000000000 ) ) ;
#3509=DIRECTION ( 'NONE',  ( -0.5735764363510503783, -0.8191520442889886899, 0.000000000000000000 ) ) ;
#3586=CARTESIAN_POINT ( 'NONE',  ( 26.75159235450331963, -2.500000000000000444, 3.061616997868384620E-16 ) ) ;
#3593=ORIENTED_EDGE ( 'NONE', *, *, #141464, .F. ) ;
#3603=CARTESIAN_POINT ( 'NONE',  ( 27.68840764549667455, 3.061616997868380183E-16, -2.500000000000001332 ) ) ;
#3604=VERTEX_POINT ( 'NONE', #93099 ) ;
#3654=DIRECTION ( 'NONE',  ( -1.000000000000000000, -1.224606353822377258E-16, -0.000000000000000000 ) ) ;
#3686=CYLINDRICAL_SURFACE ( 'NONE', #118716, 2.500000000000000000 ) ;
#3690=ORIENTED_EDGE ( 'NONE', *, *, #136284, .T. ) ;
#3728=LINE ( 'NONE', #80639, #54216 ) ;
#3752=ORIENTED_EDGE ( 'NONE', *, *, #8897, .T. ) ;
#3768=CIRCLE ( 'NONE', #29261, 2.055000000000001048 ) ;
#3821=AXIS2_PLACEMENT_3D ( 'NONE', #67543, #24016, #99395 ) ;
#3822=EDGE_CURVE ( 'NONE', #98397, #42229, #121959, .T. ) ;
#3826=ADVANCED_FACE ( 'NONE', ( #130745 ), #22399, .T. ) ;
#3830=ADVANCED_FACE ( 'NONE', ( #64043 ), #13199, .T. ) ;
#3831=DIRECTION ( 'NONE',  ( -1.000000000000000000, -1.224606353822377258E-16, -0.000000000000000000 ) ) ;
#3851=EDGE_CURVE ( 'NONE', #52853, #49616, #40961, .T. ) ;
#3903=EDGE_CURVE ( 'NONE', #75959, #135574, #52640, .T. ) ;
#3913=ORIENTED_EDGE ( 'NONE', *, *, #97483, .T. ) ;
#3925=DIRECTION ( 'NONE',  ( 0.000000000000000000, -1.000000000000000000, 0.000000000000000000 ) ) ;
#3948=CARTESIAN_POINT ( 'NONE',  ( -25.39999999999996305, 0.000000000000000000, 0.000000000000000000 ) ) ;
#3986=CARTESIAN_POINT ( 'NONE',  ( 16.76840764549667639, 0.000000000000000000, 2.500000000000001332 ) ) ;
#3990=AXIS2_PLACEMENT_3D ( 'NONE', #141080, #8396, #64257 ) ;
#4064=DIRECTION ( 'NONE',  ( 0.000000000000000000, 0.000000000000000000, 1.000000000000000000 ) ) ;
#4095=ORIENTED_EDGE ( 'NONE', *, *, #130697, .F. ) ;
#4140=ORIENTED_EDGE ( 'NONE', *, *, #124875, .F. ) ;
#4193=LINE ( 'NONE', #27424, #134414 ) ;
#4204=EDGE_CURVE ( 'NONE', #138815, #49616, #83786, .T. ) ;
#4215=DIRECTION ( 'NONE',  ( -1.000000000000000000, -1.224606353822377258E-16, -0.000000000000000000 ) ) ;
#4216=FACE_OUTER_BOUND ( 'NONE', #132647, .T. ) ;
#4233=CIRCLE ( 'NONE', #22685, 2.500000000000000888 ) ;
#4260=DIRECTION ( 'NONE',  ( -1.000000000000000000, -1.224606353822377258E-16, -0.000000000000000000 ) ) ;
#4265=ORIENTED_EDGE ( 'NONE', *, *, #36449, .F. ) ;
#4266=CARTESIAN_POINT ( 'NONE',  ( 1.199999999999999956, -0.6000000000000001998, 4.543283425070392845 ) ) ;
#4273=EDGE_CURVE ( 'NONE', #103631, #117466, #41674, .T. ) ;
#4304=ORIENTED_EDGE ( 'NONE', *, *, #31247, .T. ) ;
#4372=ORIENTED_EDGE ( 'NONE', *, *, #61857, .F. ) ;
#4378=CARTESIAN_POINT ( 'NONE',  ( 5.068407645496677105, 9.139736423841732040E-16, 0.000000000000000000 ) ) ;
#4396=VERTEX_POINT ( 'NONE', #109784 ) ;
#4422=VERTEX_POINT ( 'NONE', #56166 ) ;
#4424=ADVANCED_FACE ( 'NONE', ( #100351 ), #129038, .T. ) ;
#4459=ORIENTED_EDGE ( 'NONE', *, *, #6741, .F. ) ;
#4462=AXIS2_PLACEMENT_3D ( 'NONE', #101054, #102525, #125700 ) ;
#4527=DIRECTION ( 'NONE',  ( -1.000000000000000000, -1.224606353822377258E-16, -0.000000000000000000 ) ) ;
#4534=DIRECTION ( 'NONE',  ( -1.000000000000000000, -1.224606353822377258E-16, -0.000000000000000000 ) ) ;
#4538=EDGE_LOOP ( 'NONE', ( #59722, #20676, #143343, #125451, #122426, #85300, #53491, #47215 ) ) ;
#4548=DIRECTION ( 'NONE',  ( -1.000000000000000000, -1.224606353822377258E-16, -0.000000000000000000 ) ) ;
#4597=DIRECTION ( 'NONE',  ( -1.000000000000000000, -1.224606353822377258E-16, -0.000000000000000000 ) ) ;
#4644=ORIENTED_EDGE ( 'NONE', *, *, #20901, .T. ) ;
#4649=AXIS2_PLACEMENT_3D ( 'NONE', #1386, #21016, #78281 ) ;
#4688=CARTESIAN_POINT ( 'NONE',  ( 2.999999999999999112, 5.817072295949927426E-16, 4.750000000000000000 ) ) ;
#4703=CARTESIAN_POINT ( 'NONE',  ( 9.591592354503321260, 9.902892378096218942E-16, 0.000000000000000000 ) ) ;
#4744=AXIS2_PLACEMENT_3D ( 'NONE', #15215, #92798, #59494 ) ;
#4822=EDGE_CURVE ( 'NONE', #57169, #138815, #82914, .T. ) ;
#4830=AXIS2_PLACEMENT_3D ( 'NONE', #46369, #83983, #139785 ) ;
#4853=ORIENTED_EDGE ( 'NONE', *, *, #15862, .F. ) ;
#4891=CARTESIAN_POINT ( 'NONE',  ( 25.65999999999999659, -2.055000000000000160, 2.789133085058098087E-16 ) ) ;
#4942=AXIS2_PLACEMENT_3D ( 'NONE', #138775, #93824, #59105 ) ;
#4951=DIRECTION ( 'NONE',  ( 0.5735764363510451602, 0.8191520442889924647, 0.000000000000000000 ) ) ;
#4952=CARTESIAN_POINT ( 'NONE',  ( -25.39999999999996305, 0.000000000000000000, 0.000000000000000000 ) ) ;
#4961=ORIENTED_EDGE ( 'NONE', *, *, #73302, .T. ) ;
#4993=ORIENTED_EDGE ( 'NONE', *, *, #113814, .F. ) ;
#5028=EDGE_LOOP ( 'NONE', ( #122163, #39685, #104539, #11677, #34961 ) ) ;
#5037=CARTESIAN_POINT ( 'NONE',  ( 9.591592354503321260, -2.500000000000000000, 3.061616997868384127E-16 ) ) ;
#5062=DIRECTION ( 'NONE',  ( -1.000000000000000000, -1.224606353822377258E-16, -0.000000000000000000 ) ) ;
#5087=CARTESIAN_POINT ( 'NONE',  ( 10.37159235450332062, 9.902892378096218942E-16, 0.000000000000000000 ) ) ;
#5088=VERTEX_POINT ( 'NONE', #71816 ) ;
#5103=LINE ( 'NONE', #58877, #37724 ) ;
#5148=ORIENTED_EDGE ( 'NONE', *, *, #4822, .T. ) ;
#5159=DIRECTION ( 'NONE',  ( 0.000000000000000000, -1.000000000000000000, 0.000000000000000000 ) ) ;
#5182=CIRCLE ( 'NONE', #109314, 2.500000000000000888 ) ;
#5196=ORIENTED_EDGE ( 'NONE', *, *, #111600, .T. ) ;
#5264=CARTESIAN_POINT ( 'NONE',  ( 15.83159235450332147, 9.902892378096218942E-16, 0.000000000000000000 ) ) ;
#5325=LINE ( 'NONE', #95203, #113110 ) ;
#5350=AXIS2_PLACEMENT_3D ( 'NONE', #109086, #76498, #54739 ) ;
#5351=DIRECTION ( 'NONE',  ( -1.000000000000000000, -1.224606353822377258E-16, -0.000000000000000000 ) ) ;
#5359=AXIS2_PLACEMENT_3D ( 'NONE', #126788, #139128, #36936 ) ;
#5390=ORIENTED_EDGE ( 'NONE', *, *, #50054, .T. ) ;
#5410=LINE ( 'NONE', #26481, #32516 ) ;
#5412=ORIENTED_EDGE ( 'NONE', *, *, #129327, .T. ) ;
#5425=DIRECTION ( 'NONE',  ( -1.000000000000000000, -1.224606353822377258E-16, -0.000000000000000000 ) ) ;
#5472=CARTESIAN_POINT ( 'NONE',  ( 21.44840764549667611, 3.061616997868385113E-16, -2.500000000000001332 ) ) ;
#5500=LINE ( 'NONE', #14955, #7262 ) ;
#5504=VERTEX_POINT ( 'NONE', #3986 ) ;
#5549=DIRECTION ( 'NONE',  ( 0.000000000000000000, -1.000000000000000000, 0.000000000000000000 ) ) ;
#5595=EDGE_CURVE ( 'NONE', #77074, #64995, #91895, .T. ) ;
#5597=DIRECTION ( 'NONE',  ( 0.000000000000000000, 0.000000000000000000, 1.000000000000000000 ) ) ;
#5609=DIRECTION ( 'NONE',  ( -1.000000000000000000, -1.224606353822377258E-16, -0.000000000000000000 ) ) ;
#5621=DIRECTION ( 'NONE',  ( 0.000000000000000000, -1.000000000000000000, 0.000000000000000000 ) ) ;
#5625=DIRECTION ( 'NONE',  ( 1.000000000000000000, 1.224606353822377258E-16, 0.000000000000000000 ) ) ;
#5628=CIRCLE ( 'NONE', #123756, 4.582731094065999322 ) ;
#5655=DIRECTION ( 'NONE',  ( 0.5735764363510451602, 0.8191520442889924647, 0.000000000000000000 ) ) ;
#5695=DIRECTION ( 'NONE',  ( 0.000000000000000000, 0.000000000000000000, 1.000000000000000000 ) ) ;
#5709=LINE ( 'NONE', #6392, #44111 ) ;
#5718=CYLINDRICAL_SURFACE ( 'NONE', #117018, 2.500000000000000000 ) ;
#5733=VERTEX_POINT ( 'NONE', #139947 ) ;
#5742=ORIENTED_EDGE ( 'NONE', *, *, #63734, .T. ) ;
#5796=DIRECTION ( 'NONE',  ( -1.000000000000000000, -1.224606353822377258E-16, -0.000000000000000000 ) ) ;
#5811=CARTESIAN_POINT ( 'NONE',  ( 6.160000000000001030, 9.521314400968980422E-16, 0.000000000000000000 ) ) ;
#5820=ORIENTED_EDGE ( 'NONE', *, *, #43700, .T. ) ;
#5858=CARTESIAN_POINT ( 'NONE',  ( 26.75159235450331963, 3.061616997868380183E-16, -2.500000000000001332 ) ) ;
#5871=ORIENTED_EDGE ( 'NONE', *, *, #129327, .F. ) ;
#5901=CARTESIAN_POINT ( 'NONE',  ( 18.63999999999999702, -2.055000000000000160, 0.000000000000000000 ) ) ;
#5950=CIRCLE ( 'NONE', #45358, 2.500000000000000888 ) ;
#5983=ORIENTED_EDGE ( 'NONE', *, *, #18800, .F. ) ;
#5994=CARTESIAN_POINT ( 'NONE',  ( 4.911592354503321545, -3.851859888774471706E-31, 2.500000000000001332 ) ) ;
#6002=DIRECTION ( 'NONE',  ( 0.000000000000000000, -1.000000000000000000, 0.000000000000000000 ) ) ;
#6010=CARTESIAN_POINT ( 'NONE',  ( 16.76840764549667639, 2.499999999999998224, 3.061616997868380183E-16 ) ) ;
#6039=EDGE_CURVE ( 'NONE', #44190, #78861, #128529, .T. ) ;
#6059=FACE_OUTER_BOUND ( 'NONE', #96904, .T. ) ;
#6061=DIRECTION ( 'NONE',  ( 1.000000000000000000, 1.224606353822377258E-16, 0.000000000000000000 ) ) ;
#6078=CONICAL_SURFACE ( 'NONE', #77958, 2.055000000000001048, 0.9599310885968758145 ) ;
#6126=CYLINDRICAL_SURFACE ( 'NONE', #131908, 2.500000000000000000 ) ;
#6217=LINE ( 'NONE', #96801, #12201 ) ;
#6239=AXIS2_PLACEMENT_3D ( 'NONE', #6814, #40237, #118468 ) ;
#6251=ORIENTED_EDGE ( 'NONE', *, *, #69555, .F. ) ;
#6269=VERTEX_POINT ( 'NONE', #4891 ) ;
#6310=AXIS2_PLACEMENT_3D ( 'NONE', #32310, #142502, #122870 ) ;
#6316=CARTESIAN_POINT ( 'NONE',  ( 20.19999999999999929, 9.521314400968980422E-16, 0.000000000000000000 ) ) ;
#6317=ORIENTED_EDGE ( 'NONE', *, *, #76259, .T. ) ;
#6319=AXIS2_PLACEMENT_3D ( 'NONE', #89117, #36849, #112982 ) ;
#6334=CARTESIAN_POINT ( 'NONE',  ( 23.32000000000000028, -2.055000000000000160, 0.000000000000000000 ) ) ;
#6341=DIRECTION ( 'NONE',  ( -1.000000000000000000, -1.224606353822377258E-16, -0.000000000000000000 ) ) ;
#6392=CARTESIAN_POINT ( 'NONE',  ( 8.031592354503320763, 2.500000000000001776, 0.000000000000000000 ) ) ;
#6417=DIRECTION ( 'NONE',  ( 0.000000000000000000, -1.000000000000000000, 0.000000000000000000 ) ) ;
#6431=DIRECTION ( 'NONE',  ( -1.000000000000000000, -1.224606353822377258E-16, -0.000000000000000000 ) ) ;
#6459=CARTESIAN_POINT ( 'NONE',  ( 18.17159235450331778, -3.851859888774471706E-31, 2.500000000000001332 ) ) ;
#6485=ORIENTED_EDGE ( 'NONE', *, *, #86231, .F. ) ;
#6555=ORIENTED_EDGE ( 'NONE', *, *, #123057, .F. ) ;
#6562=ORIENTED_EDGE ( 'NONE', *, *, #27556, .F. ) ;
#6633=ADVANCED_FACE ( 'NONE', ( #105158 ), #19843, .T. ) ;
#6644=AXIS2_PLACEMENT_3D ( 'NONE', #136167, #90540, #123174 ) ;
#6666=DIRECTION ( 'NONE',  ( 0.000000000000000000, -1.000000000000000000, 0.000000000000000000 ) ) ;
#6670=ORIENTED_EDGE ( 'NONE', *, *, #32522, .T. ) ;
#6684=ORIENTED_EDGE ( 'NONE', *, *, #97463, .F. ) ;
#6709=EDGE_CURVE ( 'NONE', #81442, #7890, #5950, .T. ) ;
#6712=CARTESIAN_POINT ( 'NONE',  ( 14.74000000000000021, 9.521314400968980422E-16, 0.000000000000000000 ) ) ;
#6732=AXIS2_PLACEMENT_3D ( 'NONE', #80531, #79848, #124023 ) ;
#6741=EDGE_CURVE ( 'NONE', #123367, #31644, #17463, .T. ) ;
#6814=CARTESIAN_POINT ( 'NONE',  ( 17.07999999999999829, 9.521314400968980422E-16, 0.000000000000000000 ) ) ;
#6862=VECTOR ( 'NONE', #30608, 1000.000000000000000 ) ;
#6899=CARTESIAN_POINT ( 'NONE',  ( -25.39999999999996305, 0.000000000000000000, 2.500000000000000000 ) ) ;
#6936=CIRCLE ( 'NONE', #88013, 4.607329295533711289 ) ;
#6982=DIRECTION ( 'NONE',  ( -0.5735764363510507113, 0.8191520442889885789, 1.003171929053520926E-16 ) ) ;
#6989=SHAPE_REPRESENTATION_RELATIONSHIP ( 'NONE' , 'NONE' ,  #428, #53301 ) ;
#7030=CARTESIAN_POINT ( 'NONE',  ( 19.10840764549667270, 9.139736423841732040E-16, 0.000000000000000000 ) ) ;
#7061=ORIENTED_EDGE ( 'NONE', *, *, #44700, .F. ) ;
#7062=CARTESIAN_POINT ( 'NONE',  ( 15.83159235450332147, -2.500000000000000444, 3.061616997868384620E-16 ) ) ;
#7097=VECTOR ( 'NONE', #98256, 1000.000000000000000 ) ;
#7142=CONICAL_SURFACE ( 'NONE', #2498, 2.055000000000001048, 0.9599310885968758145 ) ;
#7206=FACE_OUTER_BOUND ( 'NONE', #134097, .T. ) ;
#7218=ORIENTED_EDGE ( 'NONE', *, *, #27467, .T. ) ;
#7222=CARTESIAN_POINT ( 'NONE',  ( 23.63159235450331863, 9.902892378096218942E-16, 0.000000000000000000 ) ) ;
#7229=EDGE_CURVE ( 'NONE', #13435, #99726, #100692, .T. ) ;
#7233=AXIS2_PLACEMENT_3D ( 'NONE', #123636, #122888, #13383 ) ;
#7262=VECTOR ( 'NONE', #92512, 1000.000000000000000 ) ;
#7268=CARTESIAN_POINT ( 'NONE',  ( 22.53999999999999915, -2.055000000000000160, 0.000000000000000000 ) ) ;
#7277=EDGE_CURVE ( 'NONE', #15156, #71528, #107606, .T. ) ;
#7298=EDGE_CURVE ( 'NONE', #64292, #85310, #38198, .T. ) ;
#7312=CARTESIAN_POINT ( 'NONE',  ( 25.34840764549667469, 3.061616997868380183E-16, -2.500000000000001332 ) ) ;
#7319=EDGE_CURVE ( 'NONE', #1998, #35419, #96013, .T. ) ;
#7326=VERTEX_POINT ( 'NONE', #69477 ) ;
#7328=ORIENTED_EDGE ( 'NONE', *, *, #32406, .F. ) ;
#7367=AXIS2_PLACEMENT_3D ( 'NONE', #57361, #101536, #46512 ) ;
#7410=ORIENTED_EDGE ( 'NONE', *, *, #21282, .F. ) ;
#7431=DIRECTION ( 'NONE',  ( 0.5735764363510453823, -0.8191520442889923537, 1.003171929053525486E-16 ) ) ;
#7483=DIRECTION ( 'NONE',  ( 0.000000000000000000, -1.000000000000000000, 0.000000000000000000 ) ) ;
#7500=ORIENTED_EDGE ( 'NONE', *, *, #122510, .F. ) ;
#7513=ORIENTED_EDGE ( 'NONE', *, *, #76592, .T. ) ;
#7521=ORIENTED_EDGE ( 'NONE', *, *, #95955, .T. ) ;
#7542=ORIENTED_EDGE ( 'NONE', *, *, #58205, .T. ) ;
#7548=AXIS2_PLACEMENT_3D ( 'NONE', #43243, #32354, #77321 ) ;
#7554=CIRCLE ( 'NONE', #107112, 2.500000000000000888 ) ;
#7613=CARTESIAN_POINT ( 'NONE',  ( 2.999999999999999112, 3.061616997868383141E-16, -2.500000000000000000 ) ) ;
#7709=FACE_OUTER_BOUND ( 'NONE', #68074, .T. ) ;
#7714=ORIENTED_EDGE ( 'NONE', *, *, #38022, .F. ) ;
#7718=DIRECTION ( 'NONE',  ( -1.000000000000000000, -1.224606353822377258E-16, -0.000000000000000000 ) ) ;
#7720=ORIENTED_EDGE ( 'NONE', *, *, #126600, .F. ) ;
#7729=CARTESIAN_POINT ( 'NONE',  ( -3.589048004105921397E-14, -0.6000000000000001998, 3.226849613583692822 ) ) ;
#7745=AXIS2_PLACEMENT_3D ( 'NONE', #132305, #75763, #98908 ) ;
#7757=AXIS2_PLACEMENT_3D ( 'NONE', #135921, #79454, #24304 ) ;
#7800=CARTESIAN_POINT ( 'NONE',  ( 10.06000000000000050, 9.521314400968980422E-16, 0.000000000000000000 ) ) ;
#7883=ORIENTED_EDGE ( 'NONE', *, *, #73302, .F. ) ;
#7889=ORIENTED_EDGE ( 'NONE', *, *, #34512, .F. ) ;
#7890=VERTEX_POINT ( 'NONE', #27189 ) ;
#7923=CYLINDRICAL_SURFACE ( 'NONE', #20438, 2.500000000000000000 ) ;
#7973=CARTESIAN_POINT ( 'NONE',  ( 25.65999999999999659, 9.521314400968980422E-16, 0.000000000000000000 ) ) ;
#7997=AXIS2_PLACEMENT_3D ( 'NONE', #89198, #45019, #34111 ) ;
#8011=DIRECTION ( 'NONE',  ( 0.000000000000000000, 1.000000000000000000, 0.000000000000000000 ) ) ;
#8013=ORIENTED_EDGE ( 'NONE', *, *, #32007, .T. ) ;
#8032=DIRECTION ( 'NONE',  ( -1.000000000000000000, -1.224606353822377258E-16, -0.000000000000000000 ) ) ;
#8048=CARTESIAN_POINT ( 'NONE',  ( 13.96000000000000085, 9.521314400968980422E-16, 0.000000000000000000 ) ) ;
#8065=CARTESIAN_POINT ( 'NONE',  ( 12.40000000000000213, 9.521314400968980422E-16, 0.000000000000000000 ) ) ;
#8143=DIRECTION ( 'NONE',  ( -1.000000000000000000, -1.224606353822377258E-16, -0.000000000000000000 ) ) ;
#8207=AXIS2_PLACEMENT_3D ( 'NONE', #34607, #66530, #1921 ) ;
#8236=ORIENTED_EDGE ( 'NONE', *, *, #28139, .F. ) ;
#8251=CARTESIAN_POINT ( 'NONE',  ( 26.90840764549667696, 9.139736423841732040E-16, 0.000000000000000000 ) ) ;
#8274=DIRECTION ( 'NONE',  ( -1.000000000000000000, -1.224606353822377258E-16, -0.000000000000000000 ) ) ;
#8287=DIRECTION ( 'NONE',  ( 0.5735764363510453823, -0.8191520442889923537, 1.003171929053525486E-16 ) ) ;
#8295=ORIENTED_EDGE ( 'NONE', *, *, #46016, .T. ) ;
#8390=CIRCLE ( 'NONE', #135730, 2.500000000000000888 ) ;
#8396=DIRECTION ( 'NONE',  ( -1.000000000000000000, -1.224606353822377258E-16, -0.000000000000000000 ) ) ;
#8425=AXIS2_PLACEMENT_3D ( 'NONE', #119138, #74224, #86539 ) ;
#8479=CIRCLE ( 'NONE', #3821, 2.500000000000000888 ) ;
#8481=CARTESIAN_POINT ( 'NONE',  ( 15.05159235450332034, 9.902892378096218942E-16, 0.000000000000000000 ) ) ;
#8561=DIRECTION ( 'NONE',  ( 1.000000000000000000, 1.224606353822377258E-16, 0.000000000000000000 ) ) ;
#8570=ORIENTED_EDGE ( 'NONE', *, *, #3217, .T. ) ;
#8587=EDGE_CURVE ( 'NONE', #105943, #130911, #135172, .T. ) ;
#8593=DIRECTION ( 'NONE',  ( 0.5735764363510451602, 0.8191520442889924647, 0.000000000000000000 ) ) ;
#8606=LINE ( 'NONE', #63077, #136152 ) ;
#8621=DIRECTION ( 'NONE',  ( 0.5735764363510451602, 0.8191520442889924647, 0.000000000000000000 ) ) ;
#8668=ORIENTED_EDGE ( 'NONE', *, *, #100693, .F. ) ;
#8670=DIRECTION ( 'NONE',  ( 0.5735764363510453823, -0.8191520442889923537, 1.003171929053525486E-16 ) ) ;
#8677=ORIENTED_EDGE ( 'NONE', *, *, #3903, .T. ) ;
#8685=CARTESIAN_POINT ( 'NONE',  ( 27.68840764549667455, 2.499999999999998224, 3.061616997868380183E-16 ) ) ;
#8690=LINE ( 'NONE', #30514, #14150 ) ;
#8698=ORIENTED_EDGE ( 'NONE', *, *, #48886, .F. ) ;
#8707=AXIS2_PLACEMENT_3D ( 'NONE', #115576, #103999, #94568 ) ;
#8713=DIRECTION ( 'NONE',  ( 0.000000000000000000, -1.000000000000000000, 0.000000000000000000 ) ) ;
#8745=ORIENTED_EDGE ( 'NONE', *, *, #127501, .F. ) ;
#8785=LINE ( 'NONE', #23261, #105169 ) ;
#8874=LINE ( 'NONE', #143027, #80592 ) ;
#8882=DIRECTION ( 'NONE',  ( -1.000000000000000000, -1.224606353822377258E-16, -0.000000000000000000 ) ) ;
#8897=EDGE_CURVE ( 'NONE', #24205, #38741, #28775, .T. ) ;
#8902=CONICAL_SURFACE ( 'NONE', #110760, 2.055000000000001048, 0.9599310885968758145 ) ;
#8919=CARTESIAN_POINT ( 'NONE',  ( 12.71159235450332048, 2.500000000000001332, 0.000000000000000000 ) ) ;
#8925=CARTESIAN_POINT ( 'NONE',  ( 0.000000000000000000, 0.000000000000000000, 0.000000000000000000 ) ) ;
#8928=ORIENTED_EDGE ( 'NONE', *, *, #114405, .T. ) ;
#8940=AXIS2_PLACEMENT_3D ( 'NONE', #49775, #126566, #16363 ) ;
#8957=VERTEX_POINT ( 'NONE', #85520 ) ;
#8959=AXIS2_PLACEMENT_3D ( 'NONE', #125705, #72788, #6002 ) ;
#8969=DIRECTION ( 'NONE',  ( 0.000000000000000000, -1.000000000000000000, 0.000000000000000000 ) ) ;
#8974=EDGE_CURVE ( 'NONE', #117002, #55674, #100586, .T. ) ;
#9011=DIRECTION ( 'NONE',  ( -1.000000000000000000, -1.224606353822377258E-16, -0.000000000000000000 ) ) ;
#9015=ORIENTED_EDGE ( 'NONE', *, *, #87301, .F. ) ;
#9035=CARTESIAN_POINT ( 'NONE',  ( 4.600000000000001421, 2.055000000000001492, 0.000000000000000000 ) ) ;
#9038=DIRECTION ( 'NONE',  ( 0.000000000000000000, 9.130123557772669567E-17, -1.000000000000000000 ) ) ;
#9047=DIRECTION ( 'NONE',  ( 1.000000000000000000, 1.224606353822377258E-16, 0.000000000000000000 ) ) ;
#9075=ORIENTED_EDGE ( 'NONE', *, *, #110071, .F. ) ;
#9086=CARTESIAN_POINT ( 'NONE',  ( 13.64840764549667540, -2.500000000000000888, 0.000000000000000000 ) ) ;
#9106=ORIENTED_EDGE ( 'NONE', *, *, #3851, .T. ) ;
#9121=CARTESIAN_POINT ( 'NONE',  ( 0.2271987153435547913, -0.6000000000000000888, 3.878866322980131454 ) ) ;
#9148=VERTEX_POINT ( 'NONE', #91106 ) ;
#9249=CARTESIAN_POINT ( 'NONE',  ( 1.500000000000000000, 0.000000000000000000, 0.000000000000000000 ) ) ;
#9253=CIRCLE ( 'NONE', #90322, 2.500000000000000888 ) ;
#9283=CARTESIAN_POINT ( 'NONE',  ( -3.080955290695428076E-14, 0.5999999999999988676, -3.226721766443181760 ) ) ;
#9286=AXIS2_PLACEMENT_3D ( 'NONE', #5087, #3654, #38476 ) ;
#9292=FACE_OUTER_BOUND ( 'NONE', #120453, .T. ) ;
#9310=LINE ( 'NONE', #41262, #25254 ) ;
#9318=CARTESIAN_POINT ( 'NONE',  ( 20.51159235450331764, 9.902892378096218942E-16, 0.000000000000000000 ) ) ;
#9328=ORIENTED_EDGE ( 'NONE', *, *, #115909, .F. ) ;
#9344=EDGE_CURVE ( 'NONE', #130559, #45081, #17093, .T. ) ;
#9361=CARTESIAN_POINT ( 'NONE',  ( 2.999999999999999112, 0.000000000000000000, 0.000000000000000000 ) ) ;
#9379=ORIENTED_EDGE ( 'NONE', *, *, #140544, .F. ) ;
#9389=FACE_OUTER_BOUND ( 'NONE', #125906, .T. ) ;
#9405=DIRECTION ( 'NONE',  ( -1.000000000000000000, -1.224606353822377258E-16, -0.000000000000000000 ) ) ;
#9450=CARTESIAN_POINT ( 'NONE',  ( 1.031902578047557473, -0.5999999999999992006, -4.508672757499343042 ) ) ;
#9460=AXIS2_PLACEMENT_3D ( 'NONE', #101983, #47649, #58541 ) ;
#9464=DIRECTION ( 'NONE',  ( -0.5735764363510503783, -0.8191520442889886899, 0.000000000000000000 ) ) ;
#9496=AXIS2_PLACEMENT_3D ( 'NONE', #30299, #31034, #74542 ) ;
#9502=CIRCLE ( 'NONE', #81276, 2.500000000000000888 ) ;
#9565=ORIENTED_EDGE ( 'NONE', *, *, #74113, .F. ) ;
#9577=CARTESIAN_POINT ( 'NONE',  ( 18.32840764549667512, 2.499999999999998224, 3.061616997868380183E-16 ) ) ;
#9587=AXIS2_PLACEMENT_3D ( 'NONE', #35705, #92163, #103065 ) ;
#9642=CIRCLE ( 'NONE', #53662, 1.500000000000000000 ) ;
#9657=AXIS2_PLACEMENT_3D ( 'NONE', #32350, #85275, #143244 ) ;
#9662=CARTESIAN_POINT ( 'NONE',  ( 26.90840764549667696, 3.061616997868380183E-16, -2.500000000000001332 ) ) ;
#9683=ORIENTED_EDGE ( 'NONE', *, *, #106663, .T. ) ;
#9700=DIRECTION ( 'NONE',  ( -1.000000000000000000, -1.224606353822377258E-16, -0.000000000000000000 ) ) ;
#9712=CARTESIAN_POINT ( 'NONE',  ( 17.07999999999999829, 2.055000000000001492, 0.000000000000000000 ) ) ;
#9721=FACE_OUTER_BOUND ( 'NONE', #9884, .T. ) ;
#9722=DIRECTION ( 'NONE',  ( 0.000000000000000000, -1.000000000000000000, 0.000000000000000000 ) ) ;
#9747=VECTOR ( 'NONE', #73469, 1000.000000000000000 ) ;
#9750=ORIENTED_EDGE ( 'NONE', *, *, #10040, .F. ) ;
#9805=CIRCLE ( 'NONE', #77006, 2.500000000000000888 ) ;
#9859=CARTESIAN_POINT ( 'NONE',  ( 10.52840764549667618, -1.925929944387235853E-31, 2.500000000000001332 ) ) ;
#9860=VERTEX_POINT ( 'NONE', #19766 ) ;
#9884=EDGE_LOOP ( 'NONE', ( #13825, #86964, #31811, #62397, #141280 ) ) ;
#9899=VECTOR ( 'NONE', #186, 1000.000000000000000 ) ;
#9956=FACE_OUTER_BOUND ( 'NONE', #10775, .T. ) ;
#9966=VERTEX_POINT ( 'NONE', #105098 ) ;
#9985=EDGE_CURVE ( 'NONE', #29352, #102792, #138456, .T. ) ;
#10013=FACE_OUTER_BOUND ( 'NONE', #59639, .T. ) ;
#10018=DIRECTION ( 'NONE',  ( 1.000000000000000000, 1.224606353822377258E-16, 0.000000000000000000 ) ) ;
#10040=EDGE_CURVE ( 'NONE', #24873, #57148, #104642, .T. ) ;
#10080=CIRCLE ( 'NONE', #28640, 2.500000000000000888 ) ;
#10101=LINE ( 'NONE', #54366, #95642 ) ;
#10127=CARTESIAN_POINT ( 'NONE',  ( 17.85999999999999943, 9.521314400968980422E-16, 0.000000000000000000 ) ) ;
#10138=CARTESIAN_POINT ( 'NONE',  ( 14.42840764549667476, 2.500000000000003553, 3.061616997868386099E-16 ) ) ;
#10143=AXIS2_PLACEMENT_3D ( 'NONE', #27066, #4534, #81489 ) ;
#10174=EDGE_LOOP ( 'NONE', ( #106549, #143417, #64177, #79334, #44915 ) ) ;
#10177=ORIENTED_EDGE ( 'NONE', *, *, #123231, .T. ) ;
#10187=DIRECTION ( 'NONE',  ( -1.000000000000000000, -1.224606353822377258E-16, -0.000000000000000000 ) ) ;
#10189=LINE ( 'NONE', #55877, #91675 ) ;
#10201=DIRECTION ( 'NONE',  ( -0.5735764363510503783, -0.8191520442889886899, 0.000000000000000000 ) ) ;
#10210=DIRECTION ( 'NONE',  ( -1.000000000000000000, -1.224606353822377258E-16, -0.000000000000000000 ) ) ;
#10216=EDGE_LOOP ( 'NONE', ( #31767, #97991, #13463, #85973, #35798 ) ) ;
#10222=CONICAL_SURFACE ( 'NONE', #26484, 2.055000000000001048, 0.9599310885968758145 ) ;
#10227=ORIENTED_EDGE ( 'NONE', *, *, #139070, .F. ) ;
#10246=ORIENTED_EDGE ( 'NONE', *, *, #120706, .T. ) ;
#10285=DIRECTION ( 'NONE',  ( -1.000000000000000000, -1.224606353822377258E-16, -0.000000000000000000 ) ) ;
#10306=CARTESIAN_POINT ( 'NONE',  ( 27.53159235450332076, 3.061616997868375253E-16, -2.500000000000001332 ) ) ;
#10316=ADVANCED_FACE ( 'NONE', ( #36375 ), #135688, .T. ) ;
#10319=CARTESIAN_POINT ( 'NONE',  ( 21.44840764549667611, 9.139736423841732040E-16, 0.000000000000000000 ) ) ;
#10330=EDGE_LOOP ( 'NONE', ( #55101, #40055, #129610, #23402, #124751 ) ) ;
#10344=EDGE_CURVE ( 'NONE', #69819, #40894, #54240, .T. ) ;
#10369=ORIENTED_EDGE ( 'NONE', *, *, #99875, .F. ) ;
#10461=DIRECTION ( 'NONE',  ( -1.000000000000000000, -1.224606353822377258E-16, -0.000000000000000000 ) ) ;
#10470=EDGE_CURVE ( 'NONE', #70129, #786, #14579, .T. ) ;
#10471=DIRECTION ( 'NONE',  ( 0.000000000000000000, -1.000000000000000000, 0.000000000000000000 ) ) ;
#10477=CARTESIAN_POINT ( 'NONE',  ( 12.40000000000000213, -2.055000000000000160, 2.789133085058098087E-16 ) ) ;
#10488=LINE ( 'NONE', #88078, #2817 ) ;
#10504=CARTESIAN_POINT ( 'NONE',  ( 1.199999999999999956, -0.5999999999999993117, -4.750000000000000000 ) ) ;
#10522=CARTESIAN_POINT ( 'NONE',  ( -25.39999999999996305, 3.061616997868383141E-16, -2.500000000000000000 ) ) ;
#10535=DIRECTION ( 'NONE',  ( -0.5735764363510507113, 0.8191520442889885789, 1.003171929053520926E-16 ) ) ;
#10543=DIRECTION ( 'NONE',  ( -1.000000000000000000, -1.224606353822377258E-16, -0.000000000000000000 ) ) ;
#10552=ORIENTED_EDGE ( 'NONE', *, *, #37843, .T. ) ;
#10557=DIRECTION ( 'NONE',  ( 1.000000000000000000, 1.224606353822377258E-16, 0.000000000000000000 ) ) ;
#10584=EDGE_LOOP ( 'NONE', ( #110614, #17892, #101559, #141735, #99028 ) ) ;
#10593=CYLINDRICAL_SURFACE ( 'NONE', #73734, 2.500000000000000000 ) ;
#10600=CARTESIAN_POINT ( 'NONE',  ( 25.97159235450331849, 9.902892378096218942E-16, 0.000000000000000000 ) ) ;
#10601=ORIENTED_EDGE ( 'NONE', *, *, #49128, .F. ) ;
#10614=AXIS2_PLACEMENT_3D ( 'NONE', #55342, #110393, #131468 ) ;
#10645=DIRECTION ( 'NONE',  ( 0.5735764363510451602, 0.8191520442889924647, 0.000000000000000000 ) ) ;
#10654=DIRECTION ( 'NONE',  ( -1.000000000000000000, -1.224606353822377258E-16, -0.000000000000000000 ) ) ;
#10696=DIRECTION ( 'NONE',  ( -1.000000000000000000, -0.000000000000000000, -0.000000000000000000 ) ) ;
#10708=CARTESIAN_POINT ( 'NONE',  ( 23.32000000000000028, -2.055000000000000160, 2.789133085058098087E-16 ) ) ;
#10709=CARTESIAN_POINT ( 'NONE',  ( 6.628407645496676714, -2.500000000000000888, 0.000000000000000000 ) ) ;
#10738=DIRECTION ( 'NONE',  ( -1.000000000000000000, -0.000000000000000000, -0.000000000000000000 ) ) ;
#10754=CARTESIAN_POINT ( 'NONE',  ( 21.29159235450332233, 9.902892378096218942E-16, 0.000000000000000000 ) ) ;
#10775=EDGE_LOOP ( 'NONE', ( #6562, #105474 ) ) ;
#10783=PRODUCT_DEFINITION_SHAPE ( 'NONE', 'NONE',  #128095 ) ;
#10800=ADVANCED_FACE ( 'NONE', ( #90588 ), #65545, .T. ) ;
#10801=CONICAL_SURFACE ( 'NONE', #114900, 2.055000000000001048, 0.9599310885968758145 ) ;
#10822=CARTESIAN_POINT ( 'NONE',  ( 9.591592354503321260, 9.902892378096218942E-16, 0.000000000000000000 ) ) ;
#10826=CARTESIAN_POINT ( 'NONE',  ( 13.96000000000000085, -2.055000000000000160, 0.000000000000000000 ) ) ;
#10837=ORIENTED_EDGE ( 'NONE', *, *, #21276, .F. ) ;
#10867=DIRECTION ( 'NONE',  ( 0.000000000000000000, -1.000000000000000000, 0.000000000000000000 ) ) ;
#10928=ADVANCED_FACE ( 'NONE', ( #81144 ), #96332, .T. ) ;
#10940=FILL_AREA_STYLE_COLOUR ( '', #114298 ) ;
#10956=DIRECTION ( 'NONE',  ( 0.000000000000000000, -1.000000000000000000, 0.000000000000000000 ) ) ;
#10979=CIRCLE ( 'NONE', #92038, 2.500000000000000888 ) ;
#10981=DIRECTION ( 'NONE',  ( -1.000000000000000000, -1.224606353822377258E-16, -0.000000000000000000 ) ) ;
#10992=AXIS2_PLACEMENT_3D ( 'NONE', #48171, #126424, #36568 ) ;
#10997=DIRECTION ( 'NONE',  ( 0.000000000000000000, 0.000000000000000000, 1.000000000000000000 ) ) ;
#11006=ORIENTED_EDGE ( 'NONE', *, *, #68435, .F. ) ;
#11008=CARTESIAN_POINT ( 'NONE',  ( -25.39999999999996305, 3.061616997868383141E-16, -2.500000000000000000 ) ) ;
#11041=DIRECTION ( 'NONE',  ( -1.000000000000000000, -0.000000000000000000, -0.000000000000000000 ) ) ;
#11046=DIRECTION ( 'NONE',  ( -1.000000000000000000, 0.000000000000000000, -0.000000000000000000 ) ) ;
#11101=VECTOR ( 'NONE', #13261, 1000.000000000000000 ) ;
#11118=ADVANCED_FACE ( 'NONE', ( #35166 ), #105659, .T. ) ;
#11124=ADVANCED_FACE ( 'NONE', ( #67060 ), #24948, .T. ) ;
#11132=VERTEX_POINT ( 'NONE', #69204 ) ;
#11144=DIRECTION ( 'NONE',  ( -1.000000000000000000, -0.000000000000000000, -0.000000000000000000 ) ) ;
#11178=ORIENTED_EDGE ( 'NONE', *, *, #60358, .T. ) ;
#11341=AXIS2_PLACEMENT_3D ( 'NONE', #60624, #21173, #97267 ) ;
#11346=ORIENTED_EDGE ( 'NONE', *, *, #140544, .T. ) ;
#11371=ORIENTED_EDGE ( 'NONE', *, *, #46718, .T. ) ;
#11373=ORIENTED_EDGE ( 'NONE', *, *, #18742, .T. ) ;
#11385=DIRECTION ( 'NONE',  ( 0.000000000000000000, -1.000000000000000000, 0.000000000000000000 ) ) ;
#11478=CARTESIAN_POINT ( 'NONE',  ( 26.75159235450331963, 9.902892378096218942E-16, 0.000000000000000000 ) ) ;
#11486=DIRECTION ( 'NONE',  ( -1.000000000000000000, -1.224606353822377258E-16, -0.000000000000000000 ) ) ;
#11529=AXIS2_PLACEMENT_3D ( 'NONE', #135030, #135713, #134287 ) ;
#11575=ORIENTED_EDGE ( 'NONE', *, *, #31558, .F. ) ;
#11591=CIRCLE ( 'NONE', #92629, 2.500000000000000888 ) ;
#11593=DIRECTION ( 'NONE',  ( 1.000000000000000000, 1.224606353822377258E-16, 0.000000000000000000 ) ) ;
#11604=CARTESIAN_POINT ( 'NONE',  ( 26.43999999999999773, -2.055000000000000160, 0.000000000000000000 ) ) ;
#11646=DIRECTION ( 'NONE',  ( -1.000000000000000000, -0.000000000000000000, -0.000000000000000000 ) ) ;
#11677=ORIENTED_EDGE ( 'NONE', *, *, #79285, .F. ) ;
#11739=ADVANCED_FACE ( 'NONE', ( #59598 ), #104492, .T. ) ;
#11781=AXIS2_PLACEMENT_3D ( 'NONE', #22285, #10696, #122321 ) ;
#11800=ORIENTED_EDGE ( 'NONE', *, *, #69575, .F. ) ;
#11847=DIRECTION ( 'NONE',  ( 0.000000000000000000, -1.000000000000000000, 0.000000000000000000 ) ) ;
#11888=DIRECTION ( 'NONE',  ( 0.000000000000000000, -9.130123557772670799E-17, 1.000000000000000000 ) ) ;
#11938=DIRECTION ( 'NONE',  ( -1.000000000000000000, -0.000000000000000000, -0.000000000000000000 ) ) ;
#11944=CARTESIAN_POINT ( 'NONE',  ( 10.52840764549667618, -2.499999999999998224, 0.000000000000000000 ) ) ;
#11989=VERTEX_POINT ( 'NONE', #100064 ) ;
#11993=CYLINDRICAL_SURFACE ( 'NONE', #29466, 2.500000000000000000 ) ;
#12035=DIRECTION ( 'NONE',  ( 0.000000000000000000, -1.000000000000000000, 0.000000000000000000 ) ) ;
#12043=ORIENTED_EDGE ( 'NONE', *, *, #110056, .T. ) ;
#12052=ADVANCED_FACE ( 'NONE', ( #55859 ), #82727, .T. ) ;
#12114=ORIENTED_EDGE ( 'NONE', *, *, #53889, .T. ) ;
#12200=ORIENTED_EDGE ( 'NONE', *, *, #112289, .T. ) ;
#12201=VECTOR ( 'NONE', #138935, 1000.000000000000000 ) ;
#12212=CARTESIAN_POINT ( 'NONE',  ( 8.188407645496676324, 9.139736423841732040E-16, 0.000000000000000000 ) ) ;
#12238=DIRECTION ( 'NONE',  ( -1.000000000000000000, -0.000000000000000000, -0.000000000000000000 ) ) ;
#12283=EDGE_CURVE ( 'NONE', #93111, #71989, #52594, .T. ) ;
#12315=ORIENTED_EDGE ( 'NONE', *, *, #106180, .T. ) ;
#12317=DIRECTION ( 'NONE',  ( 0.000000000000000000, -1.000000000000000000, 0.000000000000000000 ) ) ;
#12335=DIRECTION ( 'NONE',  ( -1.000000000000000000, -1.224606353822377258E-16, -0.000000000000000000 ) ) ;
#12391=ADVANCED_FACE ( 'NONE', ( #79613 ), #22279, .T. ) ;
#12397=CARTESIAN_POINT ( 'NONE',  ( 4.911592354503321545, 9.902892378096218942E-16, 0.000000000000000000 ) ) ;
#12448=FACE_OUTER_BOUND ( 'NONE', #91426, .T. ) ;
#12451=ORIENTED_EDGE ( 'NONE', *, *, #81111, .T. ) ;
#12486=FACE_OUTER_BOUND ( 'NONE', #71804, .T. ) ;
#12492=ORIENTED_EDGE ( 'NONE', *, *, #38227, .T. ) ;
#12496=DIRECTION ( 'NONE',  ( -1.000000000000000000, -1.224606353822377258E-16, -0.000000000000000000 ) ) ;
#12513=DIRECTION ( 'NONE',  ( 0.000000000000000000, 1.000000000000000000, 0.000000000000000000 ) ) ;
#12547=VERTEX_POINT ( 'NONE', #17158 ) ;
#12564=CARTESIAN_POINT ( 'NONE',  ( 12.40000000000000213, 9.521314400968980422E-16, 0.000000000000000000 ) ) ;
#12574=VERTEX_POINT ( 'NONE', #124484 ) ;
#12587=DIRECTION ( 'NONE',  ( 0.000000000000000000, 1.000000000000000000, 0.000000000000000000 ) ) ;
#12607=DIRECTION ( 'NONE',  ( 0.000000000000000000, -1.000000000000000000, 0.000000000000000000 ) ) ;
#12616=CYLINDRICAL_SURFACE ( 'NONE', #82705, 2.500000000000000000 ) ;
#12665=CYLINDRICAL_SURFACE ( 'NONE', #77498, 2.500000000000000000 ) ;
#12679=AXIS2_PLACEMENT_3D ( 'NONE', #82384, #60661, #104826 ) ;
#12685=LINE ( 'NONE', #125030, #96195 ) ;
#12692=CARTESIAN_POINT ( 'NONE',  ( -25.39999999999996305, 3.061616997868383141E-16, -2.500000000000000000 ) ) ;
#12693=DIRECTION ( 'NONE',  ( 0.000000000000000000, 1.000000000000000000, 0.000000000000000000 ) ) ;
#12718=ORIENTED_EDGE ( 'NONE', *, *, #91564, .T. ) ;
#12753=ORIENTED_EDGE ( 'NONE', *, *, #3106, .T. ) ;
#12764=ORIENTED_EDGE ( 'NONE', *, *, #33628, .F. ) ;
#12785=EDGE_CURVE ( 'NONE', #40894, #64109, #81384, .T. ) ;
#12796=AXIS2_PLACEMENT_3D ( 'NONE', #63925, #87097, #40748 ) ;
#12819=ORIENTED_EDGE ( 'NONE', *, *, #66799, .T. ) ;
#12836=DIRECTION ( 'NONE',  ( -1.000000000000000000, -1.224606353822377258E-16, -0.000000000000000000 ) ) ;
#12849=ORIENTED_EDGE ( 'NONE', *, *, #98349, .F. ) ;
#12890=ORIENTED_EDGE ( 'NONE', *, *, #22191, .T. ) ;
#12901=EDGE_LOOP ( 'NONE', ( #92474, #12819, #46608, #129177, #95457, #52290 ) ) ;
#12906=EDGE_LOOP ( 'NONE', ( #139796, #39332, #78702, #45739, #74020, #104729 ) ) ;
#12907=EDGE_CURVE ( 'NONE', #110525, #119001, #26963, .T. ) ;
#12909=DIRECTION ( 'NONE',  ( 0.000000000000000000, -1.000000000000000000, 0.000000000000000000 ) ) ;
#12931=DIRECTION ( 'NONE',  ( 0.000000000000000000, -1.000000000000000000, 0.000000000000000000 ) ) ;
#12945=EDGE_LOOP ( 'NONE', ( #33299, #64789, #106945, #134076, #99145, #7889 ) ) ;
#12947=CARTESIAN_POINT ( 'NONE',  ( 23.32000000000000028, 2.055000000000001492, 0.000000000000000000 ) ) ;
#12998=CARTESIAN_POINT ( 'NONE',  ( 23.00840764549667483, 9.139736423841732040E-16, 0.000000000000000000 ) ) ;
#13027=FACE_OUTER_BOUND ( 'NONE', #59108, .T. ) ;
#13036=CARTESIAN_POINT ( 'NONE',  ( 11.93159235450332112, 9.902892378096218942E-16, 0.000000000000000000 ) ) ;
#13039=EDGE_LOOP ( 'NONE', ( #113514, #23393, #107616, #139517, #29659 ) ) ;
#13050=CYLINDRICAL_SURFACE ( 'NONE', #99807, 2.500000000000000000 ) ;
#13076=DIRECTION ( 'NONE',  ( -1.000000000000000000, -0.000000000000000000, -0.000000000000000000 ) ) ;
#13096=CIRCLE ( 'NONE', #43254, 2.500000000000000888 ) ;
#13151=DIRECTION ( 'NONE',  ( 0.000000000000000000, 1.000000000000000000, 0.000000000000000000 ) ) ;
#13185=CARTESIAN_POINT ( 'NONE',  ( 22.22840764549667725, 9.139736423841732040E-16, 0.000000000000000000 ) ) ;
#13199=CONICAL_SURFACE ( 'NONE', #91865, 2.500000000000000888, 0.9599310885968822538 ) ;
#13208=CARTESIAN_POINT ( 'NONE',  ( 6.940000000000001279, 9.521314400968980422E-16, 0.000000000000000000 ) ) ;
#13214=CARTESIAN_POINT ( 'NONE',  ( 10.52840764549667618, 3.061616997868382155E-16, -2.500000000000001332 ) ) ;
#13261=DIRECTION ( 'NONE',  ( -1.000000000000000000, -0.000000000000000000, -0.000000000000000000 ) ) ;
#13271=CARTESIAN_POINT ( 'NONE',  ( 2.999999999999999112, 0.000000000000000000, 0.000000000000000000 ) ) ;
#13289=CIRCLE ( 'NONE', #112856, 2.500000000000000888 ) ;
#13313=FACE_OUTER_BOUND ( 'NONE', #143259, .T. ) ;
#13330=AXIS2_PLACEMENT_3D ( 'NONE', #132290, #122803, #23485 ) ;
#13383=DIRECTION ( 'NONE',  ( 0.000000000000000000, -1.000000000000000000, 0.000000000000000000 ) ) ;
#13398=CARTESIAN_POINT ( 'NONE',  ( 8.811592354503320124, 9.902892378096218942E-16, 0.000000000000000000 ) ) ;
#13418=ORIENTED_EDGE ( 'NONE', *, *, #95955, .F. ) ;
#13431=ORIENTED_EDGE ( 'NONE', *, *, #41735, .F. ) ;
#13435=VERTEX_POINT ( 'NONE', #123101 ) ;
#13450=CARTESIAN_POINT ( 'NONE',  ( 21.29159235450332233, 3.061616997868380183E-16, -2.500000000000001332 ) ) ;
#13456=ADVANCED_FACE ( 'NONE', ( #34659 ), #78894, .T. ) ;
#13457=VERTEX_POINT ( 'NONE', #23780 ) ;
#13463=ORIENTED_EDGE ( 'NONE', *, *, #57746, .T. ) ;
#13468=EDGE_LOOP ( 'NONE', ( #137241, #135798, #13861, #113131, #118867 ) ) ;
#13501=ORIENTED_EDGE ( 'NONE', *, *, #95832, .T. ) ;
#13507=CYLINDRICAL_SURFACE ( 'NONE', #72968, 2.500000000000000000 ) ;
#13513=CARTESIAN_POINT ( 'NONE',  ( 8.968407645496675684, 3.061616997868382155E-16, -2.500000000000001332 ) ) ;
#13530=ORIENTED_EDGE ( 'NONE', *, *, #42040, .F. ) ;
#13572=EDGE_LOOP ( 'NONE', ( #549, #53587, #83815, #46997, #119073, #61675 ) ) ;
#13592=CONICAL_SURFACE ( 'NONE', #101562, 2.500000000000000888, 0.9599310885968822538 ) ;
#13599=CARTESIAN_POINT ( 'NONE',  ( 27.22000000000000242, 2.055000000000001492, 2.516649172247811554E-16 ) ) ;
#13603=AXIS2_PLACEMENT_3D ( 'NONE', #30237, #5609, #73747 ) ;
#13613=ORIENTED_EDGE ( 'NONE', *, *, #44700, .T. ) ;
#13626=CIRCLE ( 'NONE', #94561, 2.500000000000000888 ) ;
#13627=( LENGTH_UNIT ( ) NAMED_UNIT ( * ) SI_UNIT ( .MILLI., .METRE. ) );
#13635=EDGE_LOOP ( 'NONE', ( #52720, #114237, #83354, #142087, #36125, #29417 ) ) ;
#13720=EDGE_LOOP ( 'NONE', ( #123956, #34169, #70523, #112338, #38011, #3316 ) ) ;
#13722=ADVANCED_FACE ( 'NONE', ( #111219 ), #45694, .T. ) ;
#13757=EDGE_CURVE ( 'NONE', #61398, #108329, #94284, .T. ) ;
#13762=ORIENTED_EDGE ( 'NONE', *, *, #114405, .F. ) ;
#13792=CARTESIAN_POINT ( 'NONE',  ( 25.97159235450331849, 9.902892378096218942E-16, 0.000000000000000000 ) ) ;
#13818=ORIENTED_EDGE ( 'NONE', *, *, #20026, .F. ) ;
#13825=ORIENTED_EDGE ( 'NONE', *, *, #44319, .T. ) ;
#13861=ORIENTED_EDGE ( 'NONE', *, *, #125979, .T. ) ;
#13862=EDGE_CURVE ( 'NONE', #13457, #109156, #110512, .T. ) ;
#13867=DIRECTION ( 'NONE',  ( -1.000000000000000000, -1.224606353822377258E-16, -0.000000000000000000 ) ) ;
#13899=CARTESIAN_POINT ( 'NONE',  ( 23.63159235450331863, 9.902892378096218942E-16, 0.000000000000000000 ) ) ;
#13928=DIRECTION ( 'NONE',  ( -1.000000000000000000, -0.000000000000000000, -0.000000000000000000 ) ) ;
#14004=DIRECTION ( 'NONE',  ( -0.5735764363510507113, 0.8191520442889885789, 1.003171929053520926E-16 ) ) ;
#14006=ORIENTED_EDGE ( 'NONE', *, *, #13757, .T. ) ;
#14048=CARTESIAN_POINT ( 'NONE',  ( 12.08840764549667668, 9.139736423841732040E-16, 0.000000000000000000 ) ) ;
#14062=DIRECTION ( 'NONE',  ( 1.000000000000000000, 1.224606353822377258E-16, 0.000000000000000000 ) ) ;
#14092=CARTESIAN_POINT ( 'NONE',  ( 22.07159235450331991, 9.902892378096218942E-16, 0.000000000000000000 ) ) ;
#14122=CARTESIAN_POINT ( 'NONE',  ( 9.748407645496676821, 9.139736423841732040E-16, 0.000000000000000000 ) ) ;
#14123=DIRECTION ( 'NONE',  ( -1.000000000000000000, -1.224606353822377258E-16, -0.000000000000000000 ) ) ;
#14150=VECTOR ( 'NONE', #74749, 1000.000000000000000 ) ;
#14206=DIRECTION ( 'NONE',  ( -1.000000000000000000, -0.000000000000000000, -0.000000000000000000 ) ) ;
#14229=EDGE_CURVE ( 'NONE', #64283, #52993, #141408, .T. ) ;
#14257=LINE ( 'NONE', #24420, #23341 ) ;
#14288=DIRECTION ( 'NONE',  ( -1.000000000000000000, -0.000000000000000000, -0.000000000000000000 ) ) ;
#14302=LINE ( 'NONE', #15004, #24277 ) ;
#14306=VECTOR ( 'NONE', #118188, 1000.000000000000000 ) ;
#14346=EDGE_CURVE ( 'NONE', #3387, #41073, #74260, .T. ) ;
#14351=DIRECTION ( 'NONE',  ( -1.000000000000000000, -0.000000000000000000, -0.000000000000000000 ) ) ;
#14363=LINE ( 'NONE', #91914, #136449 ) ;
#14373=DIRECTION ( 'NONE',  ( -1.000000000000000000, -1.224606353822377258E-16, -0.000000000000000000 ) ) ;
#14376=DIRECTION ( 'NONE',  ( -1.000000000000000000, -1.224606353822377258E-16, -0.000000000000000000 ) ) ;
#14393=ORIENTED_EDGE ( 'NONE', *, *, #130521, .F. ) ;
#14402=ADVANCED_FACE ( 'NONE', ( #2353 ), #88126, .T. ) ;
#14415=CYLINDRICAL_SURFACE ( 'NONE', #94525, 2.500000000000000000 ) ;
#14429=ORIENTED_EDGE ( 'NONE', *, *, #61867, .F. ) ;
#14431=AXIS2_PLACEMENT_3D ( 'NONE', #98216, #30832, #87340 ) ;
#14433=AXIS2_PLACEMENT_3D ( 'NONE', #89251, #21844, #45775 ) ;
#14480=EDGE_CURVE ( 'NONE', #61706, #133114, #92968, .T. ) ;
#14489=ORIENTED_EDGE ( 'NONE', *, *, #32406, .T. ) ;
#14520=ADVANCED_FACE ( 'NONE', ( #25560 ), #50195, .T. ) ;
#14552=CONICAL_SURFACE ( 'NONE', #56203, 2.500000000000000888, 0.9599310885968822538 ) ;
#14579=CIRCLE ( 'NONE', #90981, 2.500000000000000888 ) ;
#14666=VERTEX_POINT ( 'NONE', #142718 ) ;
#14678=ORIENTED_EDGE ( 'NONE', *, *, #84019, .F. ) ;
#14712=DIRECTION ( 'NONE',  ( -1.000000000000000000, -1.224606353822377258E-16, -0.000000000000000000 ) ) ;
#14725=ORIENTED_EDGE ( 'NONE', *, *, #47773, .F. ) ;
#14803=CIRCLE ( 'NONE', #123607, 2.500000000000000888 ) ;
#14817=CARTESIAN_POINT ( 'NONE',  ( 23.00840764549667483, -3.851859888774471706E-31, 2.500000000000001332 ) ) ;
#14820=DIRECTION ( 'NONE',  ( 0.000000000000000000, -1.000000000000000000, 0.000000000000000000 ) ) ;
#14848=CIRCLE ( 'NONE', #126013, 2.500000000000000888 ) ;
#14849=EDGE_CURVE ( 'NONE', #88219, #8957, #125260, .T. ) ;
#14888=EDGE_CURVE ( 'NONE', #140709, #14666, #111377, .T. ) ;
#14907=ORIENTED_EDGE ( 'NONE', *, *, #62044, .T. ) ;
#14918=AXIS2_PLACEMENT_3D ( 'NONE', #83390, #61657, #105128 ) ;
#14934=AXIS2_PLACEMENT_3D ( 'NONE', #5264, #15412, #127058 ) ;
#14947=DIRECTION ( 'NONE',  ( -1.000000000000000000, 0.000000000000000000, 0.000000000000000000 ) ) ;
#14949=DIRECTION ( 'NONE',  ( 1.000000000000000000, 1.224606353822377258E-16, 0.000000000000000000 ) ) ;
#14955=CARTESIAN_POINT ( 'NONE',  ( 17.85999999999999943, 2.055000000000001492, 2.516649172247811554E-16 ) ) ;
#14966=EDGE_LOOP ( 'NONE', ( #104057, #131918, #31732, #124404, #16257, #62113 ) ) ;
#15004=CARTESIAN_POINT ( 'NONE',  ( -25.39999999999996305, 3.061616997868383141E-16, -2.500000000000000000 ) ) ;
#15101=DIRECTION ( 'NONE',  ( 0.000000000000000000, 0.000000000000000000, 1.000000000000000000 ) ) ;
#15111=LINE ( 'NONE', #93414, #138859 ) ;
#15114=LINE ( 'NONE', #70971, #53563 ) ;
#15154=ORIENTED_EDGE ( 'NONE', *, *, #140228, .T. ) ;
#15156=VERTEX_POINT ( 'NONE', #25754 ) ;
#15215=CARTESIAN_POINT ( 'NONE',  ( 15.05159235450332034, 9.902892378096218942E-16, 0.000000000000000000 ) ) ;
#15223=CARTESIAN_POINT ( 'NONE',  ( 1.199999999999999956, 0.000000000000000000, 0.000000000000000000 ) ) ;
#15255=ORIENTED_EDGE ( 'NONE', *, *, #12907, .F. ) ;
#15257=CARTESIAN_POINT ( 'NONE',  ( 23.78840764549667597, 9.139736423841732040E-16, 0.000000000000000000 ) ) ;
#15264=ORIENTED_EDGE ( 'NONE', *, *, #40405, .F. ) ;
#15269=DIRECTION ( 'NONE',  ( -1.000000000000000000, -1.224606353822377258E-16, -0.000000000000000000 ) ) ;
#15339=VERTEX_POINT ( 'NONE', #49685 ) ;
#15341=ORIENTED_EDGE ( 'NONE', *, *, #134623, .F. ) ;
#15370=EDGE_CURVE ( 'NONE', #5088, #117466, #92977, .T. ) ;
#15385=EDGE_CURVE ( 'NONE', #49616, #45081, #35158, .T. ) ;
#15403=EDGE_CURVE ( 'NONE', #141686, #64292, #97511, .T. ) ;
#15412=DIRECTION ( 'NONE',  ( -1.000000000000000000, -1.224606353822377258E-16, -0.000000000000000000 ) ) ;
#15438=VERTEX_POINT ( 'NONE', #130812 ) ;
#15449=VECTOR ( 'NONE', #122180, 1000.000000000000000 ) ;
#15462=LINE ( 'NONE', #93067, #141090 ) ;
#15464=DIRECTION ( 'NONE',  ( 1.000000000000000000, 1.224606353822377258E-16, 0.000000000000000000 ) ) ;
#15516=DIRECTION ( 'NONE',  ( 0.5735764363510453823, -0.8191520442889923537, 1.003171929053525486E-16 ) ) ;
#15524=DIRECTION ( 'NONE',  ( 0.000000000000000000, -1.000000000000000000, 0.000000000000000000 ) ) ;
#15548=DIRECTION ( 'NONE',  ( -1.000000000000000000, -0.000000000000000000, -0.000000000000000000 ) ) ;
#15557=EDGE_LOOP ( 'NONE', ( #47965, #62750, #92957, #84494, #60242 ) ) ;
#15579=ORIENTED_EDGE ( 'NONE', *, *, #84953, .F. ) ;
#15590=DIRECTION ( 'NONE',  ( -0.5735764363510503783, -0.8191520442889886899, 0.000000000000000000 ) ) ;
#15628=FACE_OUTER_BOUND ( 'NONE', #30931, .T. ) ;
#15669=ORIENTED_EDGE ( 'NONE', *, *, #9985, .T. ) ;
#15690=DIRECTION ( 'NONE',  ( -1.000000000000000000, -0.000000000000000000, -0.000000000000000000 ) ) ;
#15699=DIRECTION ( 'NONE',  ( 0.000000000000000000, -1.000000000000000000, 0.000000000000000000 ) ) ;
#15718=( LENGTH_UNIT ( ) NAMED_UNIT ( * ) SI_UNIT ( .MILLI., .METRE. ) );
#15727=CARTESIAN_POINT ( 'NONE',  ( 2.999999999999999112, 0.000000000000000000, 0.000000000000000000 ) ) ;
#15787=ORIENTED_EDGE ( 'NONE', *, *, #136655, .T. ) ;
#15862=EDGE_CURVE ( 'NONE', #54899, #113725, #141491, .T. ) ;
#15898=FACE_OUTER_BOUND ( 'NONE', #76357, .T. ) ;
#15926=ORIENTED_EDGE ( 'NONE', *, *, #107582, .T. ) ;
#15957=EDGE_CURVE ( 'NONE', #124568, #40245, #51390, .T. ) ;
#15978=CARTESIAN_POINT ( 'NONE',  ( 19.88840764549667384, 2.500000000000003553, 3.061616997868386099E-16 ) ) ;
#15992=EDGE_CURVE ( 'NONE', #3604, #29061, #106929, .T. ) ;
#16039=CARTESIAN_POINT ( 'NONE',  ( 13.49159235450332162, 9.902892378096218942E-16, 0.000000000000000000 ) ) ;
#16052=LINE ( 'NONE', #122155, #118372 ) ;
#16095=DIRECTION ( 'NONE',  ( 0.000000000000000000, -1.000000000000000000, 0.000000000000000000 ) ) ;
#16118=EDGE_CURVE ( 'NONE', #65821, #13457, #80532, .T. ) ;
#16132=VERTEX_POINT ( 'NONE', #63777 ) ;
#16147=CARTESIAN_POINT ( 'NONE',  ( 19.88840764549667384, 9.139736423841732040E-16, 0.000000000000000000 ) ) ;
#16181=CARTESIAN_POINT ( 'NONE',  ( 5.691592354503320905, 9.902892378096218942E-16, 0.000000000000000000 ) ) ;
#16185=CARTESIAN_POINT ( 'NONE',  ( 4.600000000000001421, 9.521314400968980422E-16, 0.000000000000000000 ) ) ;
#16237=VERTEX_POINT ( 'NONE', #107248 ) ;
#16257=ORIENTED_EDGE ( 'NONE', *, *, #76140, .F. ) ;
#16258=CARTESIAN_POINT ( 'NONE',  ( -25.39999999999996305, 3.061616997868383141E-16, -2.500000000000000000 ) ) ;
#16307=EDGE_CURVE ( 'NONE', #77389, #110325, #116353, .T. ) ;
#16338=CARTESIAN_POINT ( 'NONE',  ( -25.39999999999996305, 3.061616997868383141E-16, -2.500000000000000000 ) ) ;
#16339=CARTESIAN_POINT ( 'NONE',  ( 0.000000000000000000, 0.5999999999999987566, 3.054668707061621191 ) ) ;
#16342=AXIS2_PLACEMENT_3D ( 'NONE', #114651, #37851, #5159 ) ;
#16363=DIRECTION ( 'NONE',  ( 0.000000000000000000, 0.000000000000000000, 1.000000000000000000 ) ) ;
#16379=EDGE_CURVE ( 'NONE', #70361, #54903, #100221, .T. ) ;
#16392=CIRCLE ( 'NONE', #100060, 2.500000000000000888 ) ;
#16396=DIRECTION ( 'NONE',  ( 0.000000000000000000, 1.000000000000000000, 0.000000000000000000 ) ) ;
#16432=CARTESIAN_POINT ( 'NONE',  ( 15.98840764549667703, 9.139736423841732040E-16, 0.000000000000000000 ) ) ;
#16454=SURFACE_SIDE_STYLE ('',( #60011 ) ) ;
#16492=EDGE_LOOP ( 'NONE', ( #4459, #46061, #37091, #134956, #109823, #25489, #19262, #46200 ) ) ;
#16493=ADVANCED_FACE ( 'NONE', ( #9721 ), #63213, .T. ) ;
#16576=VECTOR ( 'NONE', #58523, 999.9999999999998863 ) ;
#16633=CARTESIAN_POINT ( 'NONE',  ( 15.83159235450332147, 9.902892378096218942E-16, 0.000000000000000000 ) ) ;
#16677=ORIENTED_EDGE ( 'NONE', *, *, #92421, .F. ) ;
#16687=AXIS2_PLACEMENT_3D ( 'NONE', #143160, #109822, #89494 ) ;
#16698=ORIENTED_EDGE ( 'NONE', *, *, #38683, .T. ) ;
#16750=VECTOR ( 'NONE', #37757, 999.9999999999998863 ) ;
#16842=ORIENTED_EDGE ( 'NONE', *, *, #97483, .F. ) ;
#16885=EDGE_LOOP ( 'NONE', ( #76114, #5983, #142149, #12451, #121240 ) ) ;
#16935=DIRECTION ( 'NONE',  ( 0.5735764363510453823, -0.8191520442889923537, 1.003171929053525486E-16 ) ) ;
#16943=DIRECTION ( 'NONE',  ( 0.5735764363510453823, -0.8191520442889923537, 1.003171929053525486E-16 ) ) ;
#16996=DIRECTION ( 'NONE',  ( -1.000000000000000000, -1.224606353822377258E-16, -0.000000000000000000 ) ) ;
#17051=CONICAL_SURFACE ( 'NONE', #30938, 2.500000000000000888, 0.9599310885968822538 ) ;
#17053=DIRECTION ( 'NONE',  ( -1.000000000000000000, -1.224606353822377258E-16, -0.000000000000000000 ) ) ;
#17055=DIRECTION ( 'NONE',  ( 0.000000000000000000, 0.000000000000000000, 1.000000000000000000 ) ) ;
#17063=ORIENTED_EDGE ( 'NONE', *, *, #79029, .F. ) ;
#17077=DIRECTION ( 'NONE',  ( 0.000000000000000000, -1.000000000000000000, 0.000000000000000000 ) ) ;
#17093=LINE ( 'NONE', #16338, #111970 ) ;
#17139=ADVANCED_FACE ( 'NONE', ( #101555 ), #56381, .T. ) ;
#17143=ORIENTED_EDGE ( 'NONE', *, *, #67503, .F. ) ;
#17158=CARTESIAN_POINT ( 'NONE',  ( 21.44840764549667611, -2.500000000000000888, 0.000000000000000000 ) ) ;
#17179=CONICAL_SURFACE ( 'NONE', #51959, 2.055000000000001048, 0.9599310885968758145 ) ;
#17203=( NAMED_UNIT ( * ) PLANE_ANGLE_UNIT ( ) SI_UNIT ( $, .RADIAN. ) );
#17249=ORIENTED_EDGE ( 'NONE', *, *, #127836, .F. ) ;
#17269=DIRECTION ( 'NONE',  ( 0.000000000000000000, -1.000000000000000000, 0.000000000000000000 ) ) ;
#17274=DIRECTION ( 'NONE',  ( 0.000000000000000000, -1.000000000000000000, 0.000000000000000000 ) ) ;
#17276=LINE ( 'NONE', #138352, #90228 ) ;
#17285=ORIENTED_EDGE ( 'NONE', *, *, #91486, .T. ) ;
#17379=DIRECTION ( 'NONE',  ( -1.000000000000000000, -1.224606353822377258E-16, -0.000000000000000000 ) ) ;
#17388=EDGE_CURVE ( 'NONE', #34870, #22742, #10101, .T. ) ;
#17399=CARTESIAN_POINT ( 'NONE',  ( 20.66840764549667497, 9.139736423841732040E-16, 0.000000000000000000 ) ) ;
#17414=VERTEX_POINT ( 'NONE', #42766 ) ;
#17418=EDGE_CURVE ( 'NONE', #71117, #49830, #73940, .T. ) ;
#17463=CIRCLE ( 'NONE', #68529, 4.607329295533711289 ) ;
#17467=FACE_OUTER_BOUND ( 'NONE', #74599, .T. ) ;
#17475=EDGE_CURVE ( 'NONE', #107725, #104096, #121110, .T. ) ;
#17486=CARTESIAN_POINT ( 'NONE',  ( 16.61159235450331906, 9.902892378096218942E-16, 0.000000000000000000 ) ) ;
#17490=DIRECTION ( 'NONE',  ( -1.000000000000000000, -1.224606353822377258E-16, -0.000000000000000000 ) ) ;
#17514=ORIENTED_EDGE ( 'NONE', *, *, #95909, .T. ) ;
#17535=AXIS2_PLACEMENT_3D ( 'NONE', #2351, #79992, #111120 ) ;
#17587=DIRECTION ( 'NONE',  ( 0.000000000000000000, 0.000000000000000000, 1.000000000000000000 ) ) ;
#17597=CARTESIAN_POINT ( 'NONE',  ( 15.83159235450332147, -2.500000000000000000, 3.061616997868384127E-16 ) ) ;
#17614=DIRECTION ( 'NONE',  ( -1.000000000000000000, -0.000000000000000000, -0.000000000000000000 ) ) ;
#17634=AXIS2_PLACEMENT_3D ( 'NONE', #26815, #27515, #92062 ) ;
#17651=CONICAL_SURFACE ( 'NONE', #38588, 2.500000000000000888, 0.9599310885968822538 ) ;
#17707=DIRECTION ( 'NONE',  ( -1.000000000000000000, -1.224606353822377258E-16, -0.000000000000000000 ) ) ;
#17710=CARTESIAN_POINT ( 'NONE',  ( 23.00840764549667483, -2.500000000000000888, 0.000000000000000000 ) ) ;
#17762=ORIENTED_EDGE ( 'NONE', *, *, #124705, .F. ) ;
#17781=AXIS2_PLACEMENT_3D ( 'NONE', #46096, #1796, #101868 ) ;
#17784=DIRECTION ( 'NONE',  ( -1.000000000000000000, -1.224606353822377258E-16, -0.000000000000000000 ) ) ;
#17787=EDGE_CURVE ( 'NONE', #103460, #80827, #112025, .T. ) ;
#17791=CARTESIAN_POINT ( 'NONE',  ( 1.199999999999999956, 0.5999999999999987566, -4.750000000000000888 ) ) ;
#17799=DIRECTION ( 'NONE',  ( -1.000000000000000000, -1.224606353822377258E-16, -0.000000000000000000 ) ) ;
#17813=DIRECTION ( 'NONE',  ( -1.000000000000000000, -1.224606353822377258E-16, -0.000000000000000000 ) ) ;
#17840=AXIS2_PLACEMENT_3D ( 'NONE', #1639, #71061, #124175 ) ;
#17847=DIRECTION ( 'NONE',  ( -1.000000000000000000, -1.224606353822377258E-16, -0.000000000000000000 ) ) ;
#17871=DIRECTION ( 'NONE',  ( 0.000000000000000000, 0.000000000000000000, 1.000000000000000000 ) ) ;
#17892=ORIENTED_EDGE ( 'NONE', *, *, #47128, .T. ) ;
#17895=ORIENTED_EDGE ( 'NONE', *, *, #18633, .F. ) ;
#17996=DIRECTION ( 'NONE',  ( 0.5735764363510451602, 0.8191520442889924647, 0.000000000000000000 ) ) ;
#18014=ORIENTED_EDGE ( 'NONE', *, *, #58532, .T. ) ;
#18021=EDGE_CURVE ( 'NONE', #116046, #72349, #21507, .T. ) ;
#18093=ORIENTED_EDGE ( 'NONE', *, *, #49086, .F. ) ;
#18160=VECTOR ( 'NONE', #36219, 1000.000000000000000 ) ;
#18203=DIRECTION ( 'NONE',  ( -0.5735764363510503783, -0.8191520442889886899, 0.000000000000000000 ) ) ;
#18232=AXIS2_PLACEMENT_3D ( 'NONE', #19242, #109091, #64186 ) ;
#18273=AXIS2_PLACEMENT_3D ( 'NONE', #101259, #77408, #22948 ) ;
#18360=CIRCLE ( 'NONE', #4462, 2.500000000000000888 ) ;
#18379=EDGE_CURVE ( 'NONE', #143241, #36066, #8785, .T. ) ;
#18430=CARTESIAN_POINT ( 'NONE',  ( 12.86840764549667604, 9.139736423841732040E-16, 0.000000000000000000 ) ) ;
#18454=EDGE_CURVE ( 'NONE', #121024, #85852, #38130, .T. ) ;
#18545=AXIS2_PLACEMENT_3D ( 'NONE', #49417, #91469, #47982 ) ;
#18571=ORIENTED_EDGE ( 'NONE', *, *, #18800, .T. ) ;
#18594=CARTESIAN_POINT ( 'NONE',  ( 0.8678420939694353464, -0.6000000000000000888, 4.443813723662917603 ) ) ;
#18595=FILL_AREA_STYLE ('',( #129511 ) ) ;
#18601=EDGE_CURVE ( 'NONE', #28286, #12547, #98351, .T. ) ;
#18612=FACE_OUTER_BOUND ( 'NONE', #108687, .T. ) ;
#18616=EDGE_CURVE ( 'NONE', #81350, #110059, #137689, .T. ) ;
#18627=EDGE_LOOP ( 'NONE', ( #94387, #125540, #27209, #47913, #24086 ) ) ;
#18633=EDGE_CURVE ( 'NONE', #80457, #140709, #102911, .T. ) ;
#18636=ADVANCED_FACE ( 'NONE', ( #7206 ), #139214, .T. ) ;
#18637=DIRECTION ( 'NONE',  ( -1.000000000000000000, -1.224606353822377258E-16, -0.000000000000000000 ) ) ;
#18671=LINE ( 'NONE', #107122, #28795 ) ;
#18676=DIRECTION ( 'NONE',  ( 0.000000000000000000, 0.000000000000000000, 1.000000000000000000 ) ) ;
#18742=EDGE_CURVE ( 'NONE', #40894, #69819, #112230, .T. ) ;
#18767=AXIS2_PLACEMENT_3D ( 'NONE', #28947, #60165, #73876 ) ;
#18782=CARTESIAN_POINT ( 'NONE',  ( 27.99999999999999645, 9.521314400968980422E-16, 0.000000000000000000 ) ) ;
#18800=EDGE_CURVE ( 'NONE', #50175, #100764, #121409, .T. ) ;
#18818=CARTESIAN_POINT ( 'NONE',  ( 5.068407645496677105, -2.499999999999998224, 0.000000000000000000 ) ) ;
#18819=DIRECTION ( 'NONE',  ( 0.000000000000000000, -1.000000000000000000, 0.000000000000000000 ) ) ;
#18832=AXIS2_PLACEMENT_3D ( 'NONE', #29051, #141375, #50808 ) ;
#18875=AXIS2_PLACEMENT_3D ( 'NONE', #57118, #14288, #4064 ) ;
#18882=ORIENTED_EDGE ( 'NONE', *, *, #78011, .F. ) ;
#18915=CARTESIAN_POINT ( 'NONE',  ( 15.05159235450332034, 2.500000000000001776, 0.000000000000000000 ) ) ;
#18921=FACE_OUTER_BOUND ( 'NONE', #30314, .T. ) ;
#18947=DIRECTION ( 'NONE',  ( -1.000000000000000000, -0.000000000000000000, -0.000000000000000000 ) ) ;
#18959=DIRECTION ( 'NONE',  ( -1.000000000000000000, -1.224606353822377258E-16, -0.000000000000000000 ) ) ;
#18969=AXIS2_PLACEMENT_3D ( 'NONE', #56591, #100756, #46420 ) ;
#18974=ORIENTED_EDGE ( 'NONE', *, *, #140869, .F. ) ;
#18976=AXIS2_PLACEMENT_3D ( 'NONE', #16181, #14062, #127106 ) ;
#18982=ORIENTED_EDGE ( 'NONE', *, *, #84272, .F. ) ;
#19027=EDGE_CURVE ( 'NONE', #39158, #99753, #827, .T. ) ;
#19096=DIRECTION ( 'NONE',  ( -1.000000000000000000, -1.224606353822377258E-16, -0.000000000000000000 ) ) ;
#19108=DIRECTION ( 'NONE',  ( -1.000000000000000000, -1.224606353822377258E-16, -0.000000000000000000 ) ) ;
#19122=ORIENTED_EDGE ( 'NONE', *, *, #115611, .F. ) ;
#19124=AXIS2_PLACEMENT_3D ( 'NONE', #84232, #40705, #95057 ) ;
#19159=CARTESIAN_POINT ( 'NONE',  ( 1.199999999999999956, 0.5999999999999987566, 4.543283425070392845 ) ) ;
#19164=DIRECTION ( 'NONE',  ( 0.000000000000000000, -1.000000000000000000, 0.000000000000000000 ) ) ;
#19174=EDGE_LOOP ( 'NONE', ( #22701, #68483, #49166, #38239, #116343 ) ) ;
#19191=ORIENTED_EDGE ( 'NONE', *, *, #37322, .T. ) ;
#19229=LINE ( 'NONE', #28699, #74721 ) ;
#19242=CARTESIAN_POINT ( 'NONE',  ( 16.61159235450331906, 9.902892378096218942E-16, 0.000000000000000000 ) ) ;
#19253=LINE ( 'NONE', #6899, #108323 ) ;
#19262=ORIENTED_EDGE ( 'NONE', *, *, #97463, .T. ) ;
#19305=CARTESIAN_POINT ( 'NONE',  ( 24.56840764549667355, 9.139736423841732040E-16, 0.000000000000000000 ) ) ;
#19348=ORIENTED_EDGE ( 'NONE', *, *, #46008, .F. ) ;
#19373=CARTESIAN_POINT ( 'NONE',  ( 12.40000000000000213, 2.055000000000001492, 2.516649172247811554E-16 ) ) ;
#19384=DIRECTION ( 'NONE',  ( -1.000000000000000000, -1.224606353822377258E-16, -0.000000000000000000 ) ) ;
#19409=CARTESIAN_POINT ( 'NONE',  ( 11.15159235450332176, 9.902892378096218942E-16, 0.000000000000000000 ) ) ;
#19417=AXIS2_PLACEMENT_3D ( 'NONE', #108876, #8143, #85014 ) ;
#19449=VECTOR ( 'NONE', #81704, 999.9999999999998863 ) ;
#19450=DIRECTION ( 'NONE',  ( 0.000000000000000000, -1.000000000000000000, 0.000000000000000000 ) ) ;
#19513=ORIENTED_EDGE ( 'NONE', *, *, #77744, .F. ) ;
#19528=AXIS2_PLACEMENT_3D ( 'NONE', #139253, #108694, #51520 ) ;
#19540=AXIS2_PLACEMENT_3D ( 'NONE', #6316, #10461, #117245 ) ;
#19561=FACE_OUTER_BOUND ( 'NONE', #10584, .T. ) ;
#19581=ORIENTED_EDGE ( 'NONE', *, *, #55538, .F. ) ;
#19604=VERTEX_POINT ( 'NONE', #39382 ) ;
#19610=CIRCLE ( 'NONE', #61280, 2.500000000000000888 ) ;
#19622=ORIENTED_EDGE ( 'NONE', *, *, #117102, .F. ) ;
#19665=CARTESIAN_POINT ( 'NONE',  ( 19.10840764549667270, 3.061616997868380183E-16, -2.500000000000001332 ) ) ;
#19717=DIRECTION ( 'NONE',  ( 0.000000000000000000, 1.000000000000000000, 0.000000000000000000 ) ) ;
#19727=ORIENTED_EDGE ( 'NONE', *, *, #61124, .F. ) ;
#19738=EDGE_CURVE ( 'NONE', #44264, #21906, #128262, .T. ) ;
#19754=EDGE_CURVE ( 'NONE', #15438, #99234, #85701, .T. ) ;
#19766=CARTESIAN_POINT ( 'NONE',  ( 11.62000000000000099, -2.055000000000000160, 2.789133085058098087E-16 ) ) ;
#19797=CARTESIAN_POINT ( 'NONE',  ( 19.73159235450332005, 9.902892378096218942E-16, 0.000000000000000000 ) ) ;
#19802=DIRECTION ( 'NONE',  ( 0.000000000000000000, 0.000000000000000000, -1.000000000000000000 ) ) ;
#19812=CARTESIAN_POINT ( 'NONE',  ( 22.85159235450332105, 9.902892378096218942E-16, 0.000000000000000000 ) ) ;
#19817=ORIENTED_EDGE ( 'NONE', *, *, #25779, .F. ) ;
#19843=CONICAL_SURFACE ( 'NONE', #49992, 2.055000000000001048, 0.9599310885968758145 ) ;
#19862=CARTESIAN_POINT ( 'NONE',  ( 14.74000000000000021, 2.055000000000001492, 2.516649172247811554E-16 ) ) ;
#19896=DIRECTION ( 'NONE',  ( -1.000000000000000000, -1.224606353822377258E-16, -0.000000000000000000 ) ) ;
#19903=AXIS2_PLACEMENT_3D ( 'NONE', #69095, #6431, #82632 ) ;
#19934=FACE_OUTER_BOUND ( 'NONE', #122280, .T. ) ;
#20026=EDGE_CURVE ( 'NONE', #91029, #68485, #113452, .T. ) ;
#20043=ADVANCED_FACE ( 'NONE', ( #139781 ), #41147, .T. ) ;
#20057=DIRECTION ( 'NONE',  ( 0.000000000000000000, -1.000000000000000000, 0.000000000000000000 ) ) ;
#20091=EDGE_CURVE ( 'NONE', #16237, #75959, #99070, .T. ) ;
#20092=ORIENTED_EDGE ( 'NONE', *, *, #55127, .F. ) ;
#20168=ORIENTED_EDGE ( 'NONE', *, *, #82617, .F. ) ;
#20208=ORIENTED_EDGE ( 'NONE', *, *, #59351, .T. ) ;
#20213=EDGE_CURVE ( 'NONE', #60103, #61060, #99572, .T. ) ;
#20244=EDGE_CURVE ( 'NONE', #31644, #123367, #6936, .T. ) ;
#20249=EDGE_LOOP ( 'NONE', ( #131931, #50261, #41231, #47102, #79541 ) ) ;
#20293=ORIENTED_EDGE ( 'NONE', *, *, #23596, .T. ) ;
#20312=CARTESIAN_POINT ( 'NONE',  ( 26.43999999999999773, 9.521314400968980422E-16, 0.000000000000000000 ) ) ;
#20328=CARTESIAN_POINT ( 'NONE',  ( 0.000000000000000000, 0.000000000000000000, 0.000000000000000000 ) ) ;
#20340=CARTESIAN_POINT ( 'NONE',  ( 0.1425507193225278857, -0.5999999999999994227, -3.725915899842271894 ) ) ;
#20351=CARTESIAN_POINT ( 'NONE',  ( 11.15159235450332176, 2.500000000000001332, 0.000000000000000000 ) ) ;
#20352=LINE ( 'NONE', #30556, #58476 ) ;
#20362=AXIS2_PLACEMENT_3D ( 'NONE', #79169, #10285, #2239 ) ;
#20432=DIRECTION ( 'NONE',  ( -0.5735764363510503783, -0.8191520442889886899, 0.000000000000000000 ) ) ;
#20438=AXIS2_PLACEMENT_3D ( 'NONE', #127593, #97050, #73922 ) ;
#20496=VERTEX_POINT ( 'NONE', #16339 ) ;
#20517=ORIENTED_EDGE ( 'NONE', *, *, #9344, .F. ) ;
#20522=ORIENTED_EDGE ( 'NONE', *, *, #46730, .F. ) ;
#20537=DIRECTION ( 'NONE',  ( 1.000000000000000000, 1.224606353822377258E-16, 0.000000000000000000 ) ) ;
#20540=CIRCLE ( 'NONE', #6319, 2.500000000000000888 ) ;
#20548=CARTESIAN_POINT ( 'NONE',  ( 12.71159235450332048, 9.902892378096218942E-16, 0.000000000000000000 ) ) ;
#20565=CARTESIAN_POINT ( 'NONE',  ( -8.688897854252501031E-13, 0.5999999999999986455, 3.228722604634024940 ) ) ;
#20605=EDGE_CURVE ( 'NONE', #115095, #79885, #108522, .T. ) ;
#20672=DIRECTION ( 'NONE',  ( 0.000000000000000000, -1.000000000000000000, -9.130123557772669567E-17 ) ) ;
#20676=ORIENTED_EDGE ( 'NONE', *, *, #20244, .F. ) ;
#20731=EDGE_CURVE ( 'NONE', #63490, #29342, #43686, .T. ) ;
#20741=DIRECTION ( 'NONE',  ( 0.000000000000000000, -1.000000000000000000, 0.000000000000000000 ) ) ;
#20757=ORIENTED_EDGE ( 'NONE', *, *, #35026, .F. ) ;
#20764=AXIS2_PLACEMENT_3D ( 'NONE', #9249, #131084, #86157 ) ;
#20796=CARTESIAN_POINT ( 'NONE',  ( 21.76000000000000156, -2.055000000000000160, 0.000000000000000000 ) ) ;
#20799=AXIS2_PLACEMENT_3D ( 'NONE', #78290, #122476, #23150 ) ;
#20847=EDGE_CURVE ( 'NONE', #40538, #113538, #71542, .T. ) ;
#20871=CIRCLE ( 'NONE', #90319, 2.500000000000000888 ) ;
#20901=EDGE_CURVE ( 'NONE', #108597, #80743, #138599, .T. ) ;
#20941=AXIS2_PLACEMENT_3D ( 'NONE', #7800, #86828, #96228 ) ;
#20978=AXIS2_PLACEMENT_3D ( 'NONE', #42470, #29405, #41722 ) ;
#21007=CARTESIAN_POINT ( 'NONE',  ( 24.41159235450331977, 9.902892378096218942E-16, 0.000000000000000000 ) ) ;
#21016=DIRECTION ( 'NONE',  ( -1.000000000000000000, -1.224606353822377258E-16, -0.000000000000000000 ) ) ;
#21034=CIRCLE ( 'NONE', #65051, 2.500000000000000888 ) ;
#21041=AXIS2_PLACEMENT_3D ( 'NONE', #109226, #141126, #130291 ) ;
#21062=DIRECTION ( 'NONE',  ( 0.000000000000000000, -1.000000000000000000, 0.000000000000000000 ) ) ;
#21107=ORIENTED_EDGE ( 'NONE', *, *, #21443, .F. ) ;
#21117=VECTOR ( 'NONE', #100618, 1000.000000000000000 ) ;
#21123=ORIENTED_EDGE ( 'NONE', *, *, #57683, .T. ) ;
#21133=CIRCLE ( 'NONE', #118292, 2.055000000000001048 ) ;
#21146=ADVANCED_FACE ( 'NONE', ( #45138 ), #138701, .T. ) ;
#21154=VERTEX_POINT ( 'NONE', #100202 ) ;
#21156=ORIENTED_EDGE ( 'NONE', *, *, #49086, .T. ) ;
#21167=DIRECTION ( 'NONE',  ( 0.000000000000000000, -1.000000000000000000, 0.000000000000000000 ) ) ;
#21173=DIRECTION ( 'NONE',  ( -1.000000000000000000, -1.224606353822377258E-16, -0.000000000000000000 ) ) ;
#21194=CIRCLE ( 'NONE', #74413, 2.055000000000001048 ) ;
#21208=DIRECTION ( 'NONE',  ( 0.000000000000000000, -1.000000000000000000, 0.000000000000000000 ) ) ;
#21214=CONICAL_SURFACE ( 'NONE', #79109, 2.500000000000000888, 0.9599310885968822538 ) ;
#21223=EDGE_LOOP ( 'NONE', ( #51974, #43810, #127555, #64712, #2731 ) ) ;
#21225=ORIENTED_EDGE ( 'NONE', *, *, #114486, .T. ) ;
#21244=CARTESIAN_POINT ( 'NONE',  ( 5.068407645496677105, 3.061616997868380183E-16, -2.500000000000001332 ) ) ;
#21255=CARTESIAN_POINT ( 'NONE',  ( 17.54840764549667398, -2.500000000000000888, 0.000000000000000000 ) ) ;
#21263=VECTOR ( 'NONE', #74096, 1000.000000000000000 ) ;
#21271=EDGE_CURVE ( 'NONE', #84890, #30995, #33305, .T. ) ;
#21276=EDGE_CURVE ( 'NONE', #124568, #61398, #9310, .T. ) ;
#21282=EDGE_CURVE ( 'NONE', #34476, #65821, #104082, .T. ) ;
#21316=AXIS2_PLACEMENT_3D ( 'NONE', #88744, #132976, #11847 ) ;
#21332=CARTESIAN_POINT ( 'NONE',  ( 17.39159235450332019, 2.500000000000001332, 0.000000000000000000 ) ) ;
#21344=VERTEX_POINT ( 'NONE', #107237 ) ;
#21443=EDGE_CURVE ( 'NONE', #99753, #23695, #67087, .T. ) ;
#21453=VERTEX_POINT ( 'NONE', #113027 ) ;
#21466=DIRECTION ( 'NONE',  ( 0.000000000000000000, 0.000000000000000000, 1.000000000000000000 ) ) ;
#21504=ADVANCED_FACE ( 'NONE', ( #70309 ), #103574, .T. ) ;
#21507=LINE ( 'NONE', #131694, #109831 ) ;
#21535=CARTESIAN_POINT ( 'NONE',  ( 19.73159235450332005, -2.500000000000000444, 3.061616997868384620E-16 ) ) ;
#21597=CARTESIAN_POINT ( 'NONE',  ( 23.63159235450331863, 9.902892378096218942E-16, 0.000000000000000000 ) ) ;
#21619=CARTESIAN_POINT ( 'NONE',  ( 15.20840764549667767, -2.499999999999998224, 0.000000000000000000 ) ) ;
#21621=FACE_OUTER_BOUND ( 'NONE', #53787, .T. ) ;
#21625=LINE ( 'NONE', #110038, #63194 ) ;
#21640=ORIENTED_EDGE ( 'NONE', *, *, #29899, .F. ) ;
#21675=DIRECTION ( 'NONE',  ( -1.000000000000000000, -1.224606353822377258E-16, -0.000000000000000000 ) ) ;
#21688=CIRCLE ( 'NONE', #70373, 2.055000000000001048 ) ;
#21843=CARTESIAN_POINT ( 'NONE',  ( 11.93159235450332112, -2.500000000000000000, 3.061616997868384127E-16 ) ) ;
#21844=DIRECTION ( 'NONE',  ( -1.000000000000000000, -1.224606353822377258E-16, -0.000000000000000000 ) ) ;
#21877=ORIENTED_EDGE ( 'NONE', *, *, #113518, .T. ) ;
#21906=VERTEX_POINT ( 'NONE', #96608 ) ;
#21910=ORIENTED_EDGE ( 'NONE', *, *, #92421, .T. ) ;
#21913=DIRECTION ( 'NONE',  ( 0.000000000000000000, -1.000000000000000000, 0.000000000000000000 ) ) ;
#21914=DIRECTION ( 'NONE',  ( -1.000000000000000000, -0.000000000000000000, -0.000000000000000000 ) ) ;
#21960=DIRECTION ( 'NONE',  ( 0.000000000000000000, -1.000000000000000000, 0.000000000000000000 ) ) ;
#21964=AXIS2_PLACEMENT_3D ( 'NONE', #73236, #39168, #106522 ) ;
#22005=DIRECTION ( 'NONE',  ( 0.000000000000000000, -1.000000000000000000, 0.000000000000000000 ) ) ;
#22083=VECTOR ( 'NONE', #22147, 999.9999999999998863 ) ;
#22110=FACE_OUTER_BOUND ( 'NONE', #96633, .T. ) ;
#22147=DIRECTION ( 'NONE',  ( 0.5735764363510453823, -0.8191520442889923537, 1.003171929053525486E-16 ) ) ;
#22154=ORIENTED_EDGE ( 'NONE', *, *, #68561, .F. ) ;
#22191=EDGE_CURVE ( 'NONE', #111999, #107725, #125565, .T. ) ;
#22221=EDGE_CURVE ( 'NONE', #113128, #62841, #106456, .T. ) ;
#22228=ORIENTED_EDGE ( 'NONE', *, *, #81664, .F. ) ;
#22247=CARTESIAN_POINT ( 'NONE',  ( 21.76000000000000156, 9.521314400968980422E-16, 0.000000000000000000 ) ) ;
#22279=CYLINDRICAL_SURFACE ( 'NONE', #64203, 2.500000000000000000 ) ;
#22285=CARTESIAN_POINT ( 'NONE',  ( -25.39999999999996305, 0.000000000000000000, 0.000000000000000000 ) ) ;
#22371=DIRECTION ( 'NONE',  ( -1.000000000000000000, -1.224606353822377258E-16, -0.000000000000000000 ) ) ;
#22375=FACE_OUTER_BOUND ( 'NONE', #38093, .T. ) ;
#22398=DIRECTION ( 'NONE',  ( -1.000000000000000000, -1.224606353822377258E-16, -0.000000000000000000 ) ) ;
#22399=CONICAL_SURFACE ( 'NONE', #61789, 4.487534009422227577, 0.08726646259971666819 ) ;
#22417=LINE ( 'NONE', #10826, #70499 ) ;
#22468=ORIENTED_EDGE ( 'NONE', *, *, #27887, .F. ) ;
#22570=CARTESIAN_POINT ( 'NONE',  ( 20.51159235450331764, 2.500000000000001332, 0.000000000000000000 ) ) ;
#22578=CARTESIAN_POINT ( 'NONE',  ( 6.628407645496676714, 9.139736423841732040E-16, 0.000000000000000000 ) ) ;
#22581=VECTOR ( 'NONE', #44649, 999.9999999999998863 ) ;
#22609=CARTESIAN_POINT ( 'NONE',  ( 18.32840764549667512, 9.139736423841732040E-16, 0.000000000000000000 ) ) ;
#22632=DIRECTION ( 'NONE',  ( 0.000000000000000000, -1.000000000000000000, 0.000000000000000000 ) ) ;
#22668=EDGE_CURVE ( 'NONE', #106721, #128260, #5709, .T. ) ;
#22685=AXIS2_PLACEMENT_3D ( 'NONE', #27405, #137639, #128873 ) ;
#22701=ORIENTED_EDGE ( 'NONE', *, *, #114547, .F. ) ;
#22742=VERTEX_POINT ( 'NONE', #115892 ) ;
#22771=DIRECTION ( 'NONE',  ( 1.000000000000000000, 1.224606353822377258E-16, 0.000000000000000000 ) ) ;
#22794=EDGE_CURVE ( 'NONE', #100764, #64995, #87582, .T. ) ;
#22829=CONICAL_SURFACE ( 'NONE', #103862, 2.055000000000001048, 0.9599310885968758145 ) ;
#22832=CYLINDRICAL_SURFACE ( 'NONE', #116982, 2.500000000000000000 ) ;
#22836=CARTESIAN_POINT ( 'NONE',  ( 17.39159235450332019, 3.061616997868380183E-16, -2.500000000000001332 ) ) ;
#22852=ORIENTED_EDGE ( 'NONE', *, *, #136880, .T. ) ;
#22863=ADVANCED_FACE ( 'NONE', ( #10013 ), #88311, .T. ) ;
#22882=DIRECTION ( 'NONE',  ( -1.000000000000000000, -1.224606353822377258E-16, -0.000000000000000000 ) ) ;
#22898=AXIS2_PLACEMENT_3D ( 'NONE', #68082, #21675, #89089 ) ;
#22948=DIRECTION ( 'NONE',  ( 0.000000000000000000, -1.000000000000000000, 0.000000000000000000 ) ) ;
#22985=EDGE_CURVE ( 'NONE', #110525, #108329, #135398, .T. ) ;
#23034=CYLINDRICAL_SURFACE ( 'NONE', #118910, 2.500000000000000000 ) ;
#23038=VECTOR ( 'NONE', #87017, 1000.000000000000000 ) ;
#23048=CARTESIAN_POINT ( 'NONE',  ( -25.39999999999996305, 0.000000000000000000, 2.500000000000000000 ) ) ;
#23094=ORIENTED_EDGE ( 'NONE', *, *, #76790, .T. ) ;
#23105=ORIENTED_EDGE ( 'NONE', *, *, #51218, .T. ) ;
#23128=EDGE_CURVE ( 'NONE', #85852, #137066, #138225, .T. ) ;
#23150=DIRECTION ( 'NONE',  ( 0.000000000000000000, 0.000000000000000000, 1.000000000000000000 ) ) ;
#23168=ADVANCED_FACE ( 'NONE', ( #61427 ), #39670, .T. ) ;
#23191=DIRECTION ( 'NONE',  ( -1.000000000000000000, -1.224606353822377258E-16, -0.000000000000000000 ) ) ;
#23196=EDGE_CURVE ( 'NONE', #77143, #90786, #83656, .T. ) ;
#23220=DIRECTION ( 'NONE',  ( -1.000000000000000000, -0.000000000000000000, -0.000000000000000000 ) ) ;
#23222=CIRCLE ( 'NONE', #78839, 2.500000000000000888 ) ;
#23261=CARTESIAN_POINT ( 'NONE',  ( 14.74000000000000021, -2.055000000000000160, 0.000000000000000000 ) ) ;
#23264=VECTOR ( 'NONE', #44844, 999.9999999999998863 ) ;
#23336=AXIS2_PLACEMENT_3D ( 'NONE', #93697, #139377, #40060 ) ;
#23338=EDGE_CURVE ( 'NONE', #82772, #69799, #16052, .T. ) ;
#23341=VECTOR ( 'NONE', #45497, 1000.000000000000114 ) ;
#23373=DIRECTION ( 'NONE',  ( -1.000000000000000000, -0.000000000000000000, -0.000000000000000000 ) ) ;
#23374=CARTESIAN_POINT ( 'NONE',  ( 11.62000000000000099, 2.055000000000001492, 0.000000000000000000 ) ) ;
#23393=ORIENTED_EDGE ( 'NONE', *, *, #26639, .T. ) ;
#23394=ORIENTED_EDGE ( 'NONE', *, *, #76592, .F. ) ;
#23402=ORIENTED_EDGE ( 'NONE', *, *, #42208, .T. ) ;
#23422=EDGE_LOOP ( 'NONE', ( #97008, #112478, #94156, #66685, #90258 ) ) ;
#23424=AXIS2_PLACEMENT_3D ( 'NONE', #38595, #37160, #103808 ) ;
#23458=AXIS2_PLACEMENT_3D ( 'NONE', #127544, #128966, #6417 ) ;
#23485=DIRECTION ( 'NONE',  ( 0.000000000000000000, 1.000000000000000000, 0.000000000000000000 ) ) ;
#23537=CARTESIAN_POINT ( 'NONE',  ( 10.37159235450332062, 2.500000000000001332, 0.000000000000000000 ) ) ;
#23567=ORIENTED_EDGE ( 'NONE', *, *, #109809, .F. ) ;
#23593=LINE ( 'NONE', #56277, #22083 ) ;
#23596=EDGE_CURVE ( 'NONE', #42879, #108448, #120358, .T. ) ;
#23598=FACE_OUTER_BOUND ( 'NONE', #130932, .T. ) ;
#23603=DIRECTION ( 'NONE',  ( 0.000000000000000000, -1.000000000000000000, 0.000000000000000000 ) ) ;
#23667=CIRCLE ( 'NONE', #95379, 2.500000000000000888 ) ;
#23676=EDGE_LOOP ( 'NONE', ( #62354, #1657, #80835, #2162, #119567, #85141 ) ) ;
#23692=ADVANCED_FACE ( 'NONE', ( #88511 ), #21214, .T. ) ;
#23695=VERTEX_POINT ( 'NONE', #121108 ) ;
#23721=VECTOR ( 'NONE', #23373, 1000.000000000000000 ) ;
#23729=DIRECTION ( 'NONE',  ( 0.000000000000000000, -1.000000000000000000, 0.000000000000000000 ) ) ;
#23773=EDGE_CURVE ( 'NONE', #76159, #103631, #104618, .T. ) ;
#23774=VERTEX_POINT ( 'NONE', #137722 ) ;
#23780=CARTESIAN_POINT ( 'NONE',  ( 14.27159235450332098, 3.061616997868378211E-16, -2.500000000000001332 ) ) ;
#23795=EDGE_LOOP ( 'NONE', ( #12849, #103597, #54630, #64230, #7410 ) ) ;
#23835=DIRECTION ( 'NONE',  ( 0.000000000000000000, -1.000000000000000000, 0.000000000000000000 ) ) ;
#23842=AXIS2_PLACEMENT_3D ( 'NONE', #126383, #94464, #138717 ) ;
#23847=DIRECTION ( 'NONE',  ( 0.000000000000000000, -1.000000000000000000, 0.000000000000000000 ) ) ;
#23856=CARTESIAN_POINT ( 'NONE',  ( 8.031592354503320763, -2.500000000000000000, 3.061616997868384127E-16 ) ) ;
#23877=ORIENTED_EDGE ( 'NONE', *, *, #82813, .F. ) ;
#23895=ORIENTED_EDGE ( 'NONE', *, *, #8974, .F. ) ;
#23931=CARTESIAN_POINT ( 'NONE',  ( 12.40000000000000213, 9.521314400968980422E-16, 0.000000000000000000 ) ) ;
#23939=DIRECTION ( 'NONE',  ( 0.000000000000000000, -1.000000000000000000, 0.000000000000000000 ) ) ;
#23946=CARTESIAN_POINT ( 'NONE',  ( 8.811592354503320124, 3.061616997868378211E-16, -2.500000000000001332 ) ) ;
#23959=DIRECTION ( 'NONE',  ( 0.000000000000000000, 1.000000000000000000, 0.000000000000000000 ) ) ;
#23972=AXIS2_PLACEMENT_3D ( 'NONE', #4952, #48509, #92711 ) ;
#23977=ORIENTED_EDGE ( 'NONE', *, *, #121392, .F. ) ;
#23992=FACE_OUTER_BOUND ( 'NONE', #74875, .T. ) ;
#23995=ADVANCED_FACE ( 'NONE', ( #63735 ), #132501, .T. ) ;
#24007=CIRCLE ( 'NONE', #86524, 2.500000000000000888 ) ;
#24016=DIRECTION ( 'NONE',  ( -1.000000000000000000, -1.224606353822377258E-16, -0.000000000000000000 ) ) ;
#24034=EDGE_CURVE ( 'NONE', #90786, #71989, #33957, .T. ) ;
#24053=AXIS2_PLACEMENT_3D ( 'NONE', #15727, #49152, #5597 ) ;
#24054=EDGE_LOOP ( 'NONE', ( #99732, #66513, #110720, #72403, #63448, #106302 ) ) ;
#24064=CARTESIAN_POINT ( 'NONE',  ( 25.19159235450331735, 9.902892378096218942E-16, 0.000000000000000000 ) ) ;
#24065=DIRECTION ( 'NONE',  ( -1.000000000000000000, -1.224606353822377258E-16, -0.000000000000000000 ) ) ;
#24086=ORIENTED_EDGE ( 'NONE', *, *, #117102, .T. ) ;
#24097=DIRECTION ( 'NONE',  ( 1.000000000000000000, 1.224606353822377258E-16, 0.000000000000000000 ) ) ;
#24098=DIRECTION ( 'NONE',  ( -1.000000000000000000, -0.000000000000000000, -0.000000000000000000 ) ) ;
#24130=CIRCLE ( 'NONE', #135291, 2.055000000000001048 ) ;
#24166=EDGE_CURVE ( 'NONE', #113805, #78627, #109274, .T. ) ;
#24184=ORIENTED_EDGE ( 'NONE', *, *, #106030, .T. ) ;
#24205=VERTEX_POINT ( 'NONE', #25188 ) ;
#24277=VECTOR ( 'NONE', #123809, 1000.000000000000000 ) ;
#24304=DIRECTION ( 'NONE',  ( 0.000000000000000000, -1.000000000000000000, 0.000000000000000000 ) ) ;
#24316=FACE_OUTER_BOUND ( 'NONE', #65157, .T. ) ;
#24349=CARTESIAN_POINT ( 'NONE',  ( 9.279999999999999361, 9.521314400968980422E-16, 0.000000000000000000 ) ) ;
#24390=CARTESIAN_POINT ( 'NONE',  ( 16.30000000000000071, 2.055000000000001492, 0.000000000000000000 ) ) ;
#24420=CARTESIAN_POINT ( 'NONE',  ( 6.940000000000001279, -2.055000000000000160, 0.000000000000000000 ) ) ;
#24517=DIRECTION ( 'NONE',  ( -1.000000000000000000, -1.224606353822377258E-16, -0.000000000000000000 ) ) ;
#24530=CARTESIAN_POINT ( 'NONE',  ( 6.160000000000001030, 2.055000000000001492, 0.000000000000000000 ) ) ;
#24547=ORIENTED_EDGE ( 'NONE', *, *, #120485, .F. ) ;
#24564=ORIENTED_EDGE ( 'NONE', *, *, #90718, .F. ) ;
#24567=AXIS2_PLACEMENT_3D ( 'NONE', #72540, #116702, #61639 ) ;
#24603=DIRECTION ( 'NONE',  ( -1.000000000000000000, -1.224606353822377258E-16, -0.000000000000000000 ) ) ;
#24623=EDGE_CURVE ( 'NONE', #79589, #32976, #67722, .T. ) ;
#24671=VERTEX_POINT ( 'NONE', #40225 ) ;
#24681=CARTESIAN_POINT ( 'NONE',  ( 24.56840764549667355, 9.139736423841732040E-16, 0.000000000000000000 ) ) ;
#24708=DIRECTION ( 'NONE',  ( 1.000000000000000000, 1.224606353822377258E-16, 0.000000000000000000 ) ) ;
#24757=ORIENTED_EDGE ( 'NONE', *, *, #56337, .T. ) ;
#24827=DIRECTION ( 'NONE',  ( 0.000000000000000000, -1.000000000000000000, 0.000000000000000000 ) ) ;
#24858=VERTEX_POINT ( 'NONE', #54654 ) ;
#24873=VERTEX_POINT ( 'NONE', #133636 ) ;
#24943=CARTESIAN_POINT ( 'NONE',  ( 7.251592354503322291, 3.061616997868379197E-16, -2.500000000000001332 ) ) ;
#24948=CYLINDRICAL_SURFACE ( 'NONE', #77862, 2.500000000000000000 ) ;
#24957=ADVANCED_FACE ( 'NONE', ( #3101 ), #123380, .T. ) ;
#24997=FACE_OUTER_BOUND ( 'NONE', #72765, .T. ) ;
#25092=DIRECTION ( 'NONE',  ( 0.000000000000000000, -1.000000000000000000, 0.000000000000000000 ) ) ;
#25188=CARTESIAN_POINT ( 'NONE',  ( 23.78840764549667597, -2.499999999999996003, 0.000000000000000000 ) ) ;
#25189=DIRECTION ( 'NONE',  ( 0.000000000000000000, -1.000000000000000000, 0.000000000000000000 ) ) ;
#25204=LINE ( 'NONE', #123126, #40832 ) ;
#25221=CARTESIAN_POINT ( 'NONE',  ( 26.90840764549667696, 9.139736423841732040E-16, 0.000000000000000000 ) ) ;
#25227=AXIS2_PLACEMENT_3D ( 'NONE', #14122, #1782, #135235 ) ;
#25254=VECTOR ( 'NONE', #96330, 1000.000000000000000 ) ;
#25282=CARTESIAN_POINT ( 'NONE',  ( 24.87999999999999901, -2.055000000000000160, 0.000000000000000000 ) ) ;
#25285=DIRECTION ( 'NONE',  ( 0.000000000000000000, -1.000000000000000000, 0.000000000000000000 ) ) ;
#25299=EDGE_LOOP ( 'NONE', ( #28671, #35318, #112579, #54851, #22154 ) ) ;
#25305=CIRCLE ( 'NONE', #87727, 2.500000000000000888 ) ;
#25321=AXIS2_PLACEMENT_3D ( 'NONE', #31539, #298, #10471 ) ;
#25371=ORIENTED_EDGE ( 'NONE', *, *, #138230, .T. ) ;
#25386=ADVANCED_FACE ( 'NONE', ( #138107 ), #72902, .T. ) ;
#25459=DIRECTION ( 'NONE',  ( -1.000000000000000000, -1.224606353822377258E-16, -0.000000000000000000 ) ) ;
#25489=ORIENTED_EDGE ( 'NONE', *, *, #122898, .F. ) ;
#25525=ORIENTED_EDGE ( 'NONE', *, *, #123549, .F. ) ;
#25526=CARTESIAN_POINT ( 'NONE',  ( 18.17159235450331778, 2.500000000000001776, 0.000000000000000000 ) ) ;
#25534=AXIS2_PLACEMENT_3D ( 'NONE', #92382, #50341, #136613 ) ;
#25560=FACE_OUTER_BOUND ( 'NONE', #12945, .T. ) ;
#25566=ORIENTED_EDGE ( 'NONE', *, *, #127947, .F. ) ;
#25611=EDGE_CURVE ( 'NONE', #128927, #98397, #25865, .T. ) ;
#25628=FACE_OUTER_BOUND ( 'NONE', #129159, .T. ) ;
#25637=CIRCLE ( 'NONE', #88168, 2.500000000000000888 ) ;
#25687=DIRECTION ( 'NONE',  ( 0.000000000000000000, -1.000000000000000000, 0.000000000000000000 ) ) ;
#25729=ORIENTED_EDGE ( 'NONE', *, *, #39468, .F. ) ;
#25741=VECTOR ( 'NONE', #98676, 1000.000000000000114 ) ;
#25742=EDGE_LOOP ( 'NONE', ( #69325, #32223, #66386, #45708, #116129 ) ) ;
#25753=CYLINDRICAL_SURFACE ( 'NONE', #117262, 2.500000000000000000 ) ;
#25754=CARTESIAN_POINT ( 'NONE',  ( 4.911592354503321545, -2.500000000000000444, 3.061616997868384620E-16 ) ) ;
#25770=CARTESIAN_POINT ( 'NONE',  ( 18.17159235450331778, 9.902892378096218942E-16, 0.000000000000000000 ) ) ;
#25779=EDGE_CURVE ( 'NONE', #14666, #52856, #46829, .T. ) ;
#25801=CARTESIAN_POINT ( 'NONE',  ( -25.39999999999996305, 3.061616997868383141E-16, -2.500000000000000000 ) ) ;
#25815=CIRCLE ( 'NONE', #65279, 2.500000000000000888 ) ;
#25828=CIRCLE ( 'NONE', #58287, 2.500000000000000888 ) ;
#25829=DIRECTION ( 'NONE',  ( 0.000000000000000000, 0.000000000000000000, -1.000000000000000000 ) ) ;
#25834=DIRECTION ( 'NONE',  ( 0.000000000000000000, -1.000000000000000000, 0.000000000000000000 ) ) ;
#25837=FACE_OUTER_BOUND ( 'NONE', #49843, .T. ) ;
#25843=CIRCLE ( 'NONE', #23458, 2.055000000000001048 ) ;
#25865=CIRCLE ( 'NONE', #137342, 2.500000000000000888 ) ;
#25870=ORIENTED_EDGE ( 'NONE', *, *, #64947, .T. ) ;
#26004=VERTEX_POINT ( 'NONE', #42927 ) ;
#26011=DIRECTION ( 'NONE',  ( 0.000000000000000000, -1.000000000000000000, 0.000000000000000000 ) ) ;
#26058=DIRECTION ( 'NONE',  ( 0.000000000000000000, -1.000000000000000000, 0.000000000000000000 ) ) ;
#26064=ORIENTED_EDGE ( 'NONE', *, *, #98349, .T. ) ;
#26102=EDGE_CURVE ( 'NONE', #114079, #51588, #137050, .T. ) ;
#26117=EDGE_LOOP ( 'NONE', ( #101439, #44321, #103175, #96317, #116610 ) ) ;
#26150=EDGE_CURVE ( 'NONE', #6269, #127775, #69684, .T. ) ;
#26156=ADVANCED_FACE ( 'NONE', ( #124742 ), #58837, .T. ) ;
#26187=CARTESIAN_POINT ( 'NONE',  ( -25.39999999999996305, 0.000000000000000000, 2.500000000000000000 ) ) ;
#26197=CARTESIAN_POINT ( 'NONE',  ( 6.471592354503322042, 9.902892378096218942E-16, 0.000000000000000000 ) ) ;
#26243=CARTESIAN_POINT ( 'NONE',  ( 19.10840764549667270, -3.851859888774471706E-31, 2.500000000000001332 ) ) ;
#26248=ORIENTED_EDGE ( 'NONE', *, *, #27395, .F. ) ;
#26285=ORIENTED_EDGE ( 'NONE', *, *, #15370, .F. ) ;
#26439=LINE ( 'NONE', #88318, #21117 ) ;
#26473=CIRCLE ( 'NONE', #100577, 2.500000000000000888 ) ;
#26481=CARTESIAN_POINT ( 'NONE',  ( 7.251592354503322291, -2.500000000000000000, 3.061616997868384127E-16 ) ) ;
#26484=AXIS2_PLACEMENT_3D ( 'NONE', #93757, #4527, #48839 ) ;
#26498=LINE ( 'NONE', #139575, #124226 ) ;
#26547=CIRCLE ( 'NONE', #7997, 2.500000000000000888 ) ;
#26559=CARTESIAN_POINT ( 'NONE',  ( -25.39999999999996305, 0.000000000000000000, 0.000000000000000000 ) ) ;
#26583=CONICAL_SURFACE ( 'NONE', #107598, 2.055000000000001048, 0.9599310885968758145 ) ;
#26586=AXIS2_PLACEMENT_3D ( 'NONE', #114601, #15269, #59555 ) ;
#26590=AXIS2_PLACEMENT_3D ( 'NONE', #102810, #46316, #112948 ) ;
#26596=FACE_OUTER_BOUND ( 'NONE', #36398, .T. ) ;
#26600=ORIENTED_EDGE ( 'NONE', *, *, #101106, .F. ) ;
#26603=CARTESIAN_POINT ( 'NONE',  ( 24.09999999999999787, 9.521314400968980422E-16, 0.000000000000000000 ) ) ;
#26633=ADVANCED_FACE ( 'NONE', ( #71634 ), #29694, .T. ) ;
#26639=EDGE_CURVE ( 'NONE', #82012, #88219, #64144, .T. ) ;
#26677=EDGE_LOOP ( 'NONE', ( #123293, #19191, #34772, #26765, #5871 ) ) ;
#26735=DIRECTION ( 'NONE',  ( -0.5735764363510503783, -0.8191520442889886899, 0.000000000000000000 ) ) ;
#26742=EDGE_LOOP ( 'NONE', ( #86435, #78249, #96890, #60013, #105443 ) ) ;
#26754=DIRECTION ( 'NONE',  ( -1.000000000000000000, -1.224606353822377258E-16, -0.000000000000000000 ) ) ;
#26765=ORIENTED_EDGE ( 'NONE', *, *, #43820, .T. ) ;
#26785=CARTESIAN_POINT ( 'NONE',  ( 12.71159235450332048, 2.500000000000001776, 0.000000000000000000 ) ) ;
#26815=CARTESIAN_POINT ( 'NONE',  ( 22.53999999999999915, 9.521314400968980422E-16, 0.000000000000000000 ) ) ;
#26840=EDGE_LOOP ( 'NONE', ( #66712, #21123, #82028, #46953, #133082, #126199 ) ) ;
#26846=CARTESIAN_POINT ( 'NONE',  ( 7.408407645496676963, 2.500000000000002220, 3.061616997868384620E-16 ) ) ;
#26875=AXIS2_PLACEMENT_3D ( 'NONE', #69252, #14123, #15524 ) ;
#26891=CARTESIAN_POINT ( 'NONE',  ( 5.848407645496676466, 9.139736423841732040E-16, 0.000000000000000000 ) ) ;
#26920=CARTESIAN_POINT ( 'NONE',  ( 22.22840764549667725, -3.851859888774471706E-31, 2.500000000000001332 ) ) ;
#26963=LINE ( 'NONE', #29809, #142728 ) ;
#26989=CIRCLE ( 'NONE', #80315, 2.500000000000000888 ) ;
#27043=AXIS2_PLACEMENT_3D ( 'NONE', #41264, #17379, #85475 ) ;
#27066=CARTESIAN_POINT ( 'NONE',  ( 27.22000000000000242, 9.521314400968980422E-16, 0.000000000000000000 ) ) ;
#27119=FACE_OUTER_BOUND ( 'NONE', #127849, .T. ) ;
#27181=AXIS2_PLACEMENT_3D ( 'NONE', #8048, #95790, #63208 ) ;
#27189=CARTESIAN_POINT ( 'NONE',  ( 25.34840764549667469, -3.851859888774471706E-31, 2.500000000000001332 ) ) ;
#27209=ORIENTED_EDGE ( 'NONE', *, *, #2416, .T. ) ;
#27272=ORIENTED_EDGE ( 'NONE', *, *, #39785, .F. ) ;
#27283=CARTESIAN_POINT ( 'NONE',  ( 26.75159235450331963, 9.902892378096218942E-16, 0.000000000000000000 ) ) ;
#27320=DIRECTION ( 'NONE',  ( -1.000000000000000000, -1.224606353822377258E-16, -0.000000000000000000 ) ) ;
#27321=CARTESIAN_POINT ( 'NONE',  ( 7.720000000000001528, 9.521314400968980422E-16, 0.000000000000000000 ) ) ;
#27330=EDGE_CURVE ( 'NONE', #111999, #135296, #101953, .T. ) ;
#27336=DIRECTION ( 'NONE',  ( -1.000000000000000000, -0.000000000000000000, -0.000000000000000000 ) ) ;
#27357=DIRECTION ( 'NONE',  ( 0.000000000000000000, -1.000000000000000000, 0.000000000000000000 ) ) ;
#27368=ORIENTED_EDGE ( 'NONE', *, *, #33855, .F. ) ;
#27376=ADVANCED_FACE ( 'NONE', ( #126198 ), #113525, .T. ) ;
#27386=ORIENTED_EDGE ( 'NONE', *, *, #123231, .F. ) ;
#27395=EDGE_CURVE ( 'NONE', #45081, #40200, #74227, .T. ) ;
#27402=EDGE_CURVE ( 'NONE', #70361, #98020, #47268, .T. ) ;
#27405=CARTESIAN_POINT ( 'NONE',  ( 18.17159235450331778, 9.902892378096218942E-16, 0.000000000000000000 ) ) ;
#27410=ORIENTED_EDGE ( 'NONE', *, *, #96857, .F. ) ;
#27424=CARTESIAN_POINT ( 'NONE',  ( 15.52000000000000135, 2.055000000000001492, 2.516649172247811554E-16 ) ) ;
#27432=FACE_OUTER_BOUND ( 'NONE', #46552, .T. ) ;
#27443=LINE ( 'NONE', #115871, #37585 ) ;
#27467=EDGE_CURVE ( 'NONE', #132789, #113538, #27575, .T. ) ;
#27503=CONICAL_SURFACE ( 'NONE', #55377, 2.055000000000001048, 0.9599310885968758145 ) ;
#27514=EDGE_CURVE ( 'NONE', #102792, #33609, #99661, .T. ) ;
#27515=DIRECTION ( 'NONE',  ( -1.000000000000000000, -1.224606353822377258E-16, -0.000000000000000000 ) ) ;
#27534=CARTESIAN_POINT ( 'NONE',  ( 27.53159235450332076, 9.902892378096218942E-16, 0.000000000000000000 ) ) ;
#27552=CONICAL_SURFACE ( 'NONE', #129395, 2.055000000000001048, 0.9599310885968758145 ) ;
#27556=EDGE_CURVE ( 'NONE', #61244, #124821, #130497, .T. ) ;
#27558=ORIENTED_EDGE ( 'NONE', *, *, #58243, .T. ) ;
#27563=CIRCLE ( 'NONE', #6732, 2.500000000000000888 ) ;
#27575=LINE ( 'NONE', #103693, #73 ) ;
#27602=AXIS2_PLACEMENT_3D ( 'NONE', #51032, #5351, #14820 ) ;
#27619=VERTEX_POINT ( 'NONE', #140623 ) ;
#27654=DIRECTION ( 'NONE',  ( -0.5735764363510503783, -0.8191520442889886899, 0.000000000000000000 ) ) ;
#27726=VERTEX_POINT ( 'NONE', #98552 ) ;
#27800=CARTESIAN_POINT ( 'NONE',  ( -25.39999999999996305, 0.000000000000000000, 2.500000000000000000 ) ) ;
#27833=CARTESIAN_POINT ( 'NONE',  ( 27.53159235450332076, 9.902892378096218942E-16, 0.000000000000000000 ) ) ;
#27842=VERTEX_POINT ( 'NONE', #113719 ) ;
#27859=DIRECTION ( 'NONE',  ( -1.000000000000000000, -1.224606353822377258E-16, -0.000000000000000000 ) ) ;
#27887=EDGE_CURVE ( 'NONE', #43549, #59763, #72087, .T. ) ;
#27893=AXIS2_PLACEMENT_3D ( 'NONE', #92501, #69365, #25834 ) ;
#27898=DIRECTION ( 'NONE',  ( 0.000000000000000000, 0.000000000000000000, 1.000000000000000000 ) ) ;
#27911=CARTESIAN_POINT ( 'NONE',  ( -25.39999999999996305, 0.000000000000000000, 0.000000000000000000 ) ) ;
#27917=CONICAL_SURFACE ( 'NONE', #90426, 2.500000000000000888, 0.9599310885968822538 ) ;
#27945=ORIENTED_EDGE ( 'NONE', *, *, #113814, .T. ) ;
#27954=FACE_OUTER_BOUND ( 'NONE', #25742, .T. ) ;
#28001=AXIS2_PLACEMENT_3D ( 'NONE', #4378, #48680, #39974 ) ;
#28042=CARTESIAN_POINT ( 'NONE',  ( 26.75159235450331963, -2.500000000000000000, 3.061616997868384127E-16 ) ) ;
#28076=CARTESIAN_POINT ( 'NONE',  ( 20.66840764549667497, 9.139736423841732040E-16, 0.000000000000000000 ) ) ;
#28128=DIRECTION ( 'NONE',  ( 0.000000000000000000, 1.000000000000000000, 0.000000000000000000 ) ) ;
#28139=EDGE_CURVE ( 'NONE', #88966, #5504, #9502, .T. ) ;
#28152=ORIENTED_EDGE ( 'NONE', *, *, #123929, .F. ) ;
#28204=CARTESIAN_POINT ( 'NONE',  ( 11.15159235450332176, 2.500000000000001776, 0.000000000000000000 ) ) ;
#28232=ORIENTED_EDGE ( 'NONE', *, *, #123395, .F. ) ;
#28239=CONICAL_SURFACE ( 'NONE', #139406, 2.055000000000001048, 0.9599310885968758145 ) ;
#28262=ORIENTED_EDGE ( 'NONE', *, *, #106005, .F. ) ;
#28286=VERTEX_POINT ( 'NONE', #5472 ) ;
#28288=AXIS2_PLACEMENT_3D ( 'NONE', #93980, #138215, #38900 ) ;
#28332=DIRECTION ( 'NONE',  ( -1.000000000000000000, -1.224606353822377258E-16, -0.000000000000000000 ) ) ;
#28357=CARTESIAN_POINT ( 'NONE',  ( 21.76000000000000156, 2.055000000000001492, 2.516649172247811554E-16 ) ) ;
#28385=CIRCLE ( 'NONE', #60805, 2.500000000000000888 ) ;
#28434=DIRECTION ( 'NONE',  ( 0.000000000000000000, -1.000000000000000000, 0.000000000000000000 ) ) ;
#28445=VERTEX_POINT ( 'NONE', #10477 ) ;
#28505=CARTESIAN_POINT ( 'NONE',  ( 23.32000000000000028, 2.055000000000001492, 2.516649172247811554E-16 ) ) ;
#28525=ORIENTED_EDGE ( 'NONE', *, *, #130833, .T. ) ;
#28550=CARTESIAN_POINT ( 'NONE',  ( 24.56840764549667355, 3.061616997868385113E-16, -2.500000000000001332 ) ) ;
#28582=DIRECTION ( 'NONE',  ( 0.000000000000000000, -1.000000000000000000, 0.000000000000000000 ) ) ;
#28640=AXIS2_PLACEMENT_3D ( 'NONE', #49871, #72365, #27357 ) ;
#28647=ORIENTED_EDGE ( 'NONE', *, *, #72371, .T. ) ;
#28648=DIRECTION ( 'NONE',  ( -1.000000000000000000, -1.224606353822377258E-16, -0.000000000000000000 ) ) ;
#28657=CIRCLE ( 'NONE', #65738, 2.500000000000000888 ) ;
#28671=ORIENTED_EDGE ( 'NONE', *, *, #109229, .F. ) ;
#28675=VECTOR ( 'NONE', #68118, 999.9999999999998863 ) ;
#28685=DIRECTION ( 'NONE',  ( -1.000000000000000000, -1.224606353822377258E-16, -0.000000000000000000 ) ) ;
#28693=ORIENTED_EDGE ( 'NONE', *, *, #131884, .T. ) ;
#28694=EDGE_CURVE ( 'NONE', #84890, #109323, #109188, .T. ) ;
#28699=CARTESIAN_POINT ( 'NONE',  ( 14.27159235450332098, 2.500000000000001776, 0.000000000000000000 ) ) ;
#28718=FACE_OUTER_BOUND ( 'NONE', #76137, .T. ) ;
#28724=CARTESIAN_POINT ( 'NONE',  ( 22.85159235450332105, 9.902892378096218942E-16, 0.000000000000000000 ) ) ;
#28737=CARTESIAN_POINT ( 'NONE',  ( 18.32840764549667512, 9.139736423841732040E-16, 0.000000000000000000 ) ) ;
#28738=LINE ( 'NONE', #59937, #19449 ) ;
#28739=ORIENTED_EDGE ( 'NONE', *, *, #35984, .T. ) ;
#28761=DIRECTION ( 'NONE',  ( 0.000000000000000000, 0.000000000000000000, 1.000000000000000000 ) ) ;
#28775=CIRCLE ( 'NONE', #105229, 2.500000000000000888 ) ;
#28795=VECTOR ( 'NONE', #5655, 1000.000000000000000 ) ;
#28819=DIRECTION ( 'NONE',  ( 0.000000000000000000, -0.000000000000000000, 1.000000000000000000 ) ) ;
#28823=FACE_OUTER_BOUND ( 'NONE', #45187, .T. ) ;
#28882=CARTESIAN_POINT ( 'NONE',  ( -25.39999999999996305, 0.000000000000000000, 0.000000000000000000 ) ) ;
#28896=UNCERTAINTY_MEASURE_WITH_UNIT (LENGTH_MEASURE( 1.000000000000000082E-05 ), #13627, 'distance_accuracy_value', 'NONE');
#28922=CARTESIAN_POINT ( 'NONE',  ( 15.52000000000000135, 9.521314400968980422E-16, 0.000000000000000000 ) ) ;
#28934=ORIENTED_EDGE ( 'NONE', *, *, #18742, .F. ) ;
#28947=CARTESIAN_POINT ( 'NONE',  ( 13.18000000000000149, 9.521314400968980422E-16, 0.000000000000000000 ) ) ;
#28966=AXIS2_PLACEMENT_3D ( 'NONE', #129839, #8032, #108049 ) ;
#29019=CARTESIAN_POINT ( 'NONE',  ( 13.49159235450332162, 2.500000000000001776, 0.000000000000000000 ) ) ;
#29021=ADVANCED_FACE ( 'NONE', ( #63995 ), #49094, .T. ) ;
#29028=AXIS2_PLACEMENT_3D ( 'NONE', #35588, #143051, #110398 ) ;
#29031=ORIENTED_EDGE ( 'NONE', *, *, #79683, .T. ) ;
#29051=CARTESIAN_POINT ( 'NONE',  ( 15.52000000000000135, 9.521314400968980422E-16, 0.000000000000000000 ) ) ;
#29061=VERTEX_POINT ( 'NONE', #9577 ) ;
#29093=PLANE ( 'NONE',  #136830 ) ;
#29107=EDGE_CURVE ( 'NONE', #100020, #39592, #69916, .T. ) ;
#29113=FACE_OUTER_BOUND ( 'NONE', #50822, .T. ) ;
#29128=VERTEX_POINT ( 'NONE', #132844 ) ;
#29180=CARTESIAN_POINT ( 'NONE',  ( 8.500000000000000000, 9.521314400968980422E-16, 0.000000000000000000 ) ) ;
#29208=DIRECTION ( 'NONE',  ( 0.000000000000000000, -1.000000000000000000, 0.000000000000000000 ) ) ;
#29220=ADVANCED_FACE ( 'NONE', ( #12448 ), #79230, .T. ) ;
#29227=CARTESIAN_POINT ( 'NONE',  ( -25.39999999999996305, 3.061616997868383141E-16, -2.500000000000000000 ) ) ;
#29232=FACE_OUTER_BOUND ( 'NONE', #139304, .T. ) ;
#29249=DIRECTION ( 'NONE',  ( -1.000000000000000000, -0.000000000000000000, -0.000000000000000000 ) ) ;
#29261=AXIS2_PLACEMENT_3D ( 'NONE', #119662, #10210, #142190 ) ;
#29284=EDGE_CURVE ( 'NONE', #95787, #97600, #92822, .T. ) ;
#29300=CARTESIAN_POINT ( 'NONE',  ( 21.29159235450332233, 9.902892378096218942E-16, 0.000000000000000000 ) ) ;
#29342=VERTEX_POINT ( 'NONE', #104451 ) ;
#29352=VERTEX_POINT ( 'NONE', #48667 ) ;
#29405=DIRECTION ( 'NONE',  ( -1.000000000000000000, -1.224606353822377258E-16, -0.000000000000000000 ) ) ;
#29417=ORIENTED_EDGE ( 'NONE', *, *, #78563, .F. ) ;
#29466=AXIS2_PLACEMENT_3D ( 'NONE', #89568, #123659, #21466 ) ;
#29578=DIRECTION ( 'NONE',  ( -1.000000000000000000, -1.224606353822377258E-16, -0.000000000000000000 ) ) ;
#29586=VERTEX_POINT ( 'NONE', #79007 ) ;
#29611=CARTESIAN_POINT ( 'NONE',  ( 20.66840764549667497, 2.499999999999998224, 3.061616997868380183E-16 ) ) ;
#29641=VECTOR ( 'NONE', #121379, 1000.000000000000000 ) ;
#29653=CARTESIAN_POINT ( 'NONE',  ( 7.408407645496676963, 9.139736423841732040E-16, 0.000000000000000000 ) ) ;
#29659=ORIENTED_EDGE ( 'NONE', *, *, #108528, .F. ) ;
#29694=CONICAL_SURFACE ( 'NONE', #119916, 2.055000000000001048, 0.9599310885968758145 ) ;
#29706=CARTESIAN_POINT ( 'NONE',  ( 26.90840764549667696, -3.851859888774471706E-31, 2.500000000000001332 ) ) ;
#29723=ORIENTED_EDGE ( 'NONE', *, *, #2416, .F. ) ;
#29739=AXIS2_PLACEMENT_3D ( 'NONE', #123859, #24517, #135449 ) ;
#29768=VERTEX_POINT ( 'NONE', #84686 ) ;
#29779=LINE ( 'NONE', #18915, #71710 ) ;
#29787=CARTESIAN_POINT ( 'NONE',  ( 28.00000000000000355, 2.500000000000000000, 0.000000000000000000 ) ) ;
#29809=CARTESIAN_POINT ( 'NONE',  ( 6.160000000000001030, -2.055000000000000160, 0.000000000000000000 ) ) ;
#29821=CARTESIAN_POINT ( 'NONE',  ( 4.288407645496676857, 9.139736423841732040E-16, 0.000000000000000000 ) ) ;
#29825=ADVANCED_FACE ( 'NONE', ( #119420 ), #96236, .T. ) ;
#29833=EDGE_CURVE ( 'NONE', #42879, #24873, #72079, .T. ) ;
#29834=DIRECTION ( 'NONE',  ( -1.000000000000000000, -1.224606353822377258E-16, -0.000000000000000000 ) ) ;
#29857=ORIENTED_EDGE ( 'NONE', *, *, #16307, .F. ) ;
#29883=VECTOR ( 'NONE', #47645, 999.9999999999998863 ) ;
#29899=EDGE_CURVE ( 'NONE', #109693, #77035, #46642, .T. ) ;
#29978=ORIENTED_EDGE ( 'NONE', *, *, #95909, .F. ) ;
#30018=ORIENTED_EDGE ( 'NONE', *, *, #49575, .T. ) ;
#30030=ORIENTED_EDGE ( 'NONE', *, *, #79683, .F. ) ;
#30057=CIRCLE ( 'NONE', #129607, 2.500000000000000888 ) ;
#30136=ORIENTED_EDGE ( 'NONE', *, *, #47998, .T. ) ;
#30138=CARTESIAN_POINT ( 'NONE',  ( 7.251592354503322291, -2.500000000000000444, 3.061616997868384620E-16 ) ) ;
#30156=ORIENTED_EDGE ( 'NONE', *, *, #47773, .T. ) ;
#30186=FACE_OUTER_BOUND ( 'NONE', #92557, .T. ) ;
#30201=EDGE_CURVE ( 'NONE', #103076, #128927, #118374, .T. ) ;
#30224=DIRECTION ( 'NONE',  ( 0.000000000000000000, 0.000000000000000000, 1.000000000000000000 ) ) ;
#30231=ORIENTED_EDGE ( 'NONE', *, *, #7298, .T. ) ;
#30237=CARTESIAN_POINT ( 'NONE',  ( 21.76000000000000156, 9.521314400968980422E-16, 0.000000000000000000 ) ) ;
#30243=VERTEX_POINT ( 'NONE', #129247 ) ;
#30299=CARTESIAN_POINT ( 'NONE',  ( 26.43999999999999773, 9.521314400968980422E-16, 0.000000000000000000 ) ) ;
#30314=EDGE_LOOP ( 'NONE', ( #117087, #111486 ) ) ;
#30327=VECTOR ( 'NONE', #91180, 999.9999999999998863 ) ;
#30335=ORIENTED_EDGE ( 'NONE', *, *, #39113, .F. ) ;
#30349=FACE_OUTER_BOUND ( 'NONE', #12906, .T. ) ;
#30350=CONICAL_SURFACE ( 'NONE', #134583, 2.055000000000001048, 0.9599310885968758145 ) ;
#30427=FACE_OUTER_BOUND ( 'NONE', #93039, .T. ) ;
#30480=DIRECTION ( 'NONE',  ( -1.000000000000000000, -1.224606353822377258E-16, -0.000000000000000000 ) ) ;
#30514=CARTESIAN_POINT ( 'NONE',  ( 5.691592354503320905, 2.500000000000001776, 0.000000000000000000 ) ) ;
#30527=ORIENTED_EDGE ( 'NONE', *, *, #103245, .F. ) ;
#30556=CARTESIAN_POINT ( 'NONE',  ( 5.380000000000000782, -2.055000000000000160, 0.000000000000000000 ) ) ;
#30563=ORIENTED_EDGE ( 'NONE', *, *, #79415, .F. ) ;
#30564=AXIS2_PLACEMENT_3D ( 'NONE', #129965, #98050, #29208 ) ;
#30586=CIRCLE ( 'NONE', #16687, 2.500000000000000888 ) ;
#30602=EDGE_CURVE ( 'NONE', #39158, #91753, #82748, .T. ) ;
#30608=DIRECTION ( 'NONE',  ( -1.000000000000000000, -0.000000000000000000, -0.000000000000000000 ) ) ;
#30625=CARTESIAN_POINT ( 'NONE',  ( 7.720000000000001528, 2.055000000000001492, 0.000000000000000000 ) ) ;
#30650=CARTESIAN_POINT ( 'NONE',  ( 24.87999999999999901, 9.521314400968980422E-16, 0.000000000000000000 ) ) ;
#30658=ORIENTED_EDGE ( 'NONE', *, *, #143300, .T. ) ;
#30671=ORIENTED_EDGE ( 'NONE', *, *, #127501, .T. ) ;
#30712=FACE_OUTER_BOUND ( 'NONE', #35950, .T. ) ;
#30727=CARTESIAN_POINT ( 'NONE',  ( 13.64840764549667540, 9.139736423841732040E-16, 0.000000000000000000 ) ) ;
#30740=CARTESIAN_POINT ( 'NONE',  ( 8.188407645496676324, 2.500000000000000888, 3.061616997868383141E-16 ) ) ;
#30741=FACE_OUTER_BOUND ( 'NONE', #128290, .T. ) ;
#30744=ORIENTED_EDGE ( 'NONE', *, *, #55680, .T. ) ;
#30778=CARTESIAN_POINT ( 'NONE',  ( 20.97999999999999687, 9.521314400968980422E-16, 0.000000000000000000 ) ) ;
#30788=ORIENTED_EDGE ( 'NONE', *, *, #39080, .T. ) ;
#30791=DIRECTION ( 'NONE',  ( -1.000000000000000000, -1.224606353822377258E-16, -0.000000000000000000 ) ) ;
#30832=DIRECTION ( 'NONE',  ( -1.000000000000000000, -0.000000000000000000, -0.000000000000000000 ) ) ;
#30833=CONICAL_SURFACE ( 'NONE', #79399, 2.500000000000000888, 0.9599310885968822538 ) ;
#30898=VECTOR ( 'NONE', #8670, 999.9999999999998863 ) ;
#30931=EDGE_LOOP ( 'NONE', ( #38694, #19122, #36948, #58121, #142640 ) ) ;
#30938=AXIS2_PLACEMENT_3D ( 'NONE', #57586, #58331, #88782 ) ;
#30995=VERTEX_POINT ( 'NONE', #126085 ) ;
#31034=DIRECTION ( 'NONE',  ( -1.000000000000000000, -1.224606353822377258E-16, -0.000000000000000000 ) ) ;
#31040=EDGE_CURVE ( 'NONE', #90453, #28286, #139438, .T. ) ;
#31045=EDGE_CURVE ( 'NONE', #115828, #45804, #27443, .T. ) ;
#31087=CARTESIAN_POINT ( 'NONE',  ( 25.97159235450331849, 2.500000000000001776, 0.000000000000000000 ) ) ;
#31170=ORIENTED_EDGE ( 'NONE', *, *, #99427, .T. ) ;
#31234=ORIENTED_EDGE ( 'NONE', *, *, #26639, .F. ) ;
#31247=EDGE_CURVE ( 'NONE', #82012, #52856, #112187, .T. ) ;
#31258=CARTESIAN_POINT ( 'NONE',  ( 0.2262162651715141914, -0.5999999999999993117, -3.877538419241203904 ) ) ;
#31262=ORIENTED_EDGE ( 'NONE', *, *, #115277, .T. ) ;
#31363=DIRECTION ( 'NONE',  ( 0.5735764363510453823, -0.8191520442889923537, 1.003171929053525486E-16 ) ) ;
#31366=CARTESIAN_POINT ( 'NONE',  ( -25.39999999999996305, 0.000000000000000000, 0.000000000000000000 ) ) ;
#31382=DIRECTION ( 'NONE',  ( 0.000000000000000000, 0.000000000000000000, -1.000000000000000000 ) ) ;
#31398=EDGE_CURVE ( 'NONE', #11989, #93367, #134885, .T. ) ;
#31454=AXIS2_PLACEMENT_3D ( 'NONE', #1096, #45380, #89554 ) ;
#31461=DIRECTION ( 'NONE',  ( 1.000000000000000000, 1.224606353822377258E-16, 0.000000000000000000 ) ) ;
#31468=VERTEX_POINT ( 'NONE', #117846 ) ;
#31472=VERTEX_POINT ( 'NONE', #85970 ) ;
#31474=CARTESIAN_POINT ( 'NONE',  ( 1.030267906253082177, 0.5999999999999988676, 4.508336184329993834 ) ) ;
#31513=CIRCLE ( 'NONE', #24567, 2.055000000000001048 ) ;
#31531=ORIENTED_EDGE ( 'NONE', *, *, #132767, .T. ) ;
#31539=CARTESIAN_POINT ( 'NONE',  ( 10.06000000000000050, 9.521314400968980422E-16, 0.000000000000000000 ) ) ;
#31558=EDGE_CURVE ( 'NONE', #77143, #3030, #84561, .T. ) ;
#31562=EDGE_CURVE ( 'NONE', #14666, #47923, #6217, .T. ) ;
#31572=VERTEX_POINT ( 'NONE', #106993 ) ;
#31612=DIRECTION ( 'NONE',  ( 1.000000000000000000, 1.224606353822377258E-16, 0.000000000000000000 ) ) ;
#31644=VERTEX_POINT ( 'NONE', #45359 ) ;
#31676=CARTESIAN_POINT ( 'NONE',  ( 17.07999999999999829, -2.055000000000000160, 2.789133085058098087E-16 ) ) ;
#31685=AXIS2_PLACEMENT_3D ( 'NONE', #9361, #140618, #42056 ) ;
#31732=ORIENTED_EDGE ( 'NONE', *, *, #41971, .T. ) ;
#31750=VECTOR ( 'NONE', #14351, 1000.000000000000000 ) ;
#31752=VECTOR ( 'NONE', #18947, 1000.000000000000000 ) ;
#31758=DIRECTION ( 'NONE',  ( -1.000000000000000000, -1.224606353822377258E-16, -0.000000000000000000 ) ) ;
#31767=ORIENTED_EDGE ( 'NONE', *, *, #84478, .F. ) ;
#31806=CARTESIAN_POINT ( 'NONE',  ( 1.030796516412011643, 0.5999999999999987566, -4.508445023301312027 ) ) ;
#31811=ORIENTED_EDGE ( 'NONE', *, *, #124729, .F. ) ;
#31833=VECTOR ( 'NONE', #12238, 1000.000000000000000 ) ;
#31834=CARTESIAN_POINT ( 'NONE',  ( 9.591592354503321260, 2.500000000000001332, 0.000000000000000000 ) ) ;
#31838=ORIENTED_EDGE ( 'NONE', *, *, #62387, .T. ) ;
#31840=DIRECTION ( 'NONE',  ( -1.000000000000000000, -1.224606353822377258E-16, -0.000000000000000000 ) ) ;
#31883=CIRCLE ( 'NONE', #103577, 2.500000000000000888 ) ;
#31894=DIRECTION ( 'NONE',  ( 0.000000000000000000, -1.000000000000000000, 0.000000000000000000 ) ) ;
#31909=EDGE_CURVE ( 'NONE', #122911, #91753, #100293, .T. ) ;
#31945=CIRCLE ( 'NONE', #117582, 2.500000000000000888 ) ;
#31995=AXIS2_PLACEMENT_3D ( 'NONE', #101975, #14949, #58533 ) ;
#32007=EDGE_CURVE ( 'NONE', #135296, #75313, #79532, .T. ) ;
#32010=ORIENTED_EDGE ( 'NONE', *, *, #62036, .T. ) ;
#32039=CIRCLE ( 'NONE', #29739, 2.055000000000001048 ) ;
#32045=LINE ( 'NONE', #128515, #67590 ) ;
#32047=AXIS2_PLACEMENT_3D ( 'NONE', #110319, #119763, #10997 ) ;
#32052=CIRCLE ( 'NONE', #68916, 2.500000000000000888 ) ;
#32101=DIRECTION ( 'NONE',  ( -1.000000000000000000, -1.224606353822377258E-16, -0.000000000000000000 ) ) ;
#32116=DIRECTION ( 'NONE',  ( 0.5735764363510451602, 0.8191520442889924647, 0.000000000000000000 ) ) ;
#32173=ORIENTED_EDGE ( 'NONE', *, *, #6741, .T. ) ;
#32186=CARTESIAN_POINT ( 'NONE',  ( 15.05159235450332034, 2.500000000000001332, 0.000000000000000000 ) ) ;
#32202=DIRECTION ( 'NONE',  ( -1.000000000000000000, -1.224606353822377258E-16, -0.000000000000000000 ) ) ;
#32209=CARTESIAN_POINT ( 'NONE',  ( -25.39999999999996305, 0.000000000000000000, 0.000000000000000000 ) ) ;
#32223=ORIENTED_EDGE ( 'NONE', *, *, #115909, .T. ) ;
#32266=ADVANCED_FACE ( 'NONE', ( #92028 ), #136250, .T. ) ;
#32267=CARTESIAN_POINT ( 'NONE',  ( 0.000000000000000000, 5.495644160703818878E-16, 4.487534009422227577 ) ) ;
#32310=CARTESIAN_POINT ( 'NONE',  ( 26.12840764549667583, 9.139736423841732040E-16, 0.000000000000000000 ) ) ;
#32327=DIRECTION ( 'NONE',  ( 0.000000000000000000, -1.000000000000000000, 0.000000000000000000 ) ) ;
#32336=DIRECTION ( 'NONE',  ( -1.000000000000000000, -1.224606353822377258E-16, -0.000000000000000000 ) ) ;
#32350=CARTESIAN_POINT ( 'NONE',  ( 1.500000000000000000, 0.000000000000000000, 0.000000000000000000 ) ) ;
#32354=DIRECTION ( 'NONE',  ( 1.000000000000000000, 1.224606353822377258E-16, 0.000000000000000000 ) ) ;
#32366=CARTESIAN_POINT ( 'NONE',  ( 0.000000000000000000, -0.6000000000000000888, 3.054668707061620747 ) ) ;
#32379=AXIS2_PLACEMENT_3D ( 'NONE', #48009, #125562, #92179 ) ;
#32406=EDGE_CURVE ( 'NONE', #119351, #34476, #58738, .T. ) ;
#32477=CARTESIAN_POINT ( 'NONE',  ( 20.97999999999999687, -2.055000000000000160, 0.000000000000000000 ) ) ;
#32499=DIRECTION ( 'NONE',  ( 0.000000000000000000, -1.000000000000000000, 0.000000000000000000 ) ) ;
#32511=DIRECTION ( 'NONE',  ( 0.000000000000000000, -1.000000000000000000, 0.000000000000000000 ) ) ;
#32516=VECTOR ( 'NONE', #93869, 999.9999999999998863 ) ;
#32522=EDGE_CURVE ( 'NONE', #20496, #38971, #102034, .T. ) ;
#32550=CONICAL_SURFACE ( 'NONE', #37196, 2.500000000000000888, 0.9599310885968822538 ) ;
#32596=AXIS2_PLACEMENT_3D ( 'NONE', #71921, #95047, #82774 ) ;
#32626=DIRECTION ( 'NONE',  ( 1.000000000000000000, 1.224606353822377258E-16, 0.000000000000000000 ) ) ;
#32654=LINE ( 'NONE', #130543, #2023 ) ;
#32667=VERTEX_POINT ( 'NONE', #66319 ) ;
#32672=AXIS2_PLACEMENT_3D ( 'NONE', #50269, #114769, #82207 ) ;
#32678=DIRECTION ( 'NONE',  ( -1.000000000000000000, -1.224606353822377258E-16, -0.000000000000000000 ) ) ;
#32681=CARTESIAN_POINT ( 'NONE',  ( 19.10840764549667270, 9.139736423841732040E-16, 0.000000000000000000 ) ) ;
#32736=CARTESIAN_POINT ( 'NONE',  ( 15.98840764549667703, 9.139736423841732040E-16, 0.000000000000000000 ) ) ;
#32740=LINE ( 'NONE', #76975, #25741 ) ;
#32776=ORIENTED_EDGE ( 'NONE', *, *, #81870, .F. ) ;
#32795=DIRECTION ( 'NONE',  ( 1.000000000000000000, 1.224606353822377258E-16, 0.000000000000000000 ) ) ;
#32813=DIRECTION ( 'NONE',  ( 0.000000000000000000, 1.000000000000000000, 0.000000000000000000 ) ) ;
#32820=DIRECTION ( 'NONE',  ( 0.000000000000000000, -1.000000000000000000, 0.000000000000000000 ) ) ;
#32863=FACE_OUTER_BOUND ( 'NONE', #78272, .T. ) ;
#32923=ORIENTED_EDGE ( 'NONE', *, *, #140769, .F. ) ;
#32927=DIRECTION ( 'NONE',  ( 0.000000000000000000, -1.000000000000000000, 0.000000000000000000 ) ) ;
#32958=DIRECTION ( 'NONE',  ( 0.000000000000000000, -1.000000000000000000, 0.000000000000000000 ) ) ;
#32972=EDGE_CURVE ( 'NONE', #69819, #15156, #28738, .T. ) ;
#32976=VERTEX_POINT ( 'NONE', #92522 ) ;
#32984=ORIENTED_EDGE ( 'NONE', *, *, #49765, .F. ) ;
#33013=ORIENTED_EDGE ( 'NONE', *, *, #74692, .T. ) ;
#33066=AXIS2_PLACEMENT_3D ( 'NONE', #27283, #104857, #59951 ) ;
#33103=AXIS2_PLACEMENT_3D ( 'NONE', #64847, #8274, #66279 ) ;
#33112=COLOUR_RGB ( '', 0.09019608, 0.27058824, 0.51372549) ;
#33180=ORIENTED_EDGE ( 'NONE', *, *, #137058, .F. ) ;
#33186=ORIENTED_EDGE ( 'NONE', *, *, #36788, .T. ) ;
#33238=ORIENTED_EDGE ( 'NONE', *, *, #78563, .T. ) ;
#33241=DIRECTION ( 'NONE',  ( -1.000000000000000000, -0.000000000000000000, -0.000000000000000000 ) ) ;
#33277=CARTESIAN_POINT ( 'NONE',  ( 1.199999999999999956, 0.5999999999999987566, -4.543283425070392845 ) ) ;
#33292=DIRECTION ( 'NONE',  ( 0.000000000000000000, 0.000000000000000000, 1.000000000000000000 ) ) ;
#33299=ORIENTED_EDGE ( 'NONE', *, *, #46954, .F. ) ;
#33305=LINE ( 'NONE', #141293, #87777 ) ;
#33347=CARTESIAN_POINT ( 'NONE',  ( 8.031592354503320763, 9.902892378096218942E-16, 0.000000000000000000 ) ) ;
#33350=ORIENTED_EDGE ( 'NONE', *, *, #18601, .T. ) ;
#33354=DIRECTION ( 'NONE',  ( 0.000000000000000000, -1.000000000000000000, 0.000000000000000000 ) ) ;
#33362=ORIENTED_EDGE ( 'NONE', *, *, #141464, .T. ) ;
#33436=ADVANCED_FACE ( 'NONE', ( #117655 ), #131437, .T. ) ;
#33441=CIRCLE ( 'NONE', #116692, 2.500000000000000888 ) ;
#33448=ORIENTED_EDGE ( 'NONE', *, *, #15385, .F. ) ;
#33457=VECTOR ( 'NONE', #11888, 1000.000000000000000 ) ;
#33465=CARTESIAN_POINT ( 'NONE',  ( 0.000000000000000000, 0.000000000000000000, 0.000000000000000000 ) ) ;
#33493=DIRECTION ( 'NONE',  ( 1.000000000000000000, 1.224606353822377258E-16, 0.000000000000000000 ) ) ;
#33547=DIRECTION ( 'NONE',  ( 0.000000000000000000, -1.000000000000000000, 0.000000000000000000 ) ) ;
#33549=EDGE_CURVE ( 'NONE', #55674, #106215, #85061, .T. ) ;
#33561=ADVANCED_FACE ( 'NONE', ( #30712 ), #124145, .T. ) ;
#33609=VERTEX_POINT ( 'NONE', #3603 ) ;
#33617=VECTOR ( 'NONE', #138960, 1000.000000000000000 ) ;
#33628=EDGE_CURVE ( 'NONE', #54899, #5733, #80194, .T. ) ;
#33677=CARTESIAN_POINT ( 'NONE',  ( 18.17159235450331778, 2.500000000000001332, 0.000000000000000000 ) ) ;
#33692=DIRECTION ( 'NONE',  ( 0.000000000000000000, -1.000000000000000000, 0.000000000000000000 ) ) ;
#33769=CARTESIAN_POINT ( 'NONE',  ( 4.600000000000001421, 2.055000000000001492, 2.516649172247811554E-16 ) ) ;
#33773=DIRECTION ( 'NONE',  ( 0.000000000000000000, -1.000000000000000000, 0.000000000000000000 ) ) ;
#33810=ORIENTED_EDGE ( 'NONE', *, *, #1664, .T. ) ;
#33811=AXIS2_PLACEMENT_3D ( 'NONE', #112580, #57509, #46663 ) ;
#33821=DIRECTION ( 'NONE',  ( 0.000000000000000000, -1.000000000000000000, 0.000000000000000000 ) ) ;
#33855=EDGE_CURVE ( 'NONE', #108597, #1998, #118660, .T. ) ;
#33929=CARTESIAN_POINT ( 'NONE',  ( 21.44840764549667611, 2.500000000000003553, 3.061616997868386099E-16 ) ) ;
#33937=ORIENTED_EDGE ( 'NONE', *, *, #64393, .F. ) ;
#33955=FACE_OUTER_BOUND ( 'NONE', #73010, .T. ) ;
#33957=LINE ( 'NONE', #77474, #395 ) ;
#33992=DIRECTION ( 'NONE',  ( 0.000000000000000000, -1.000000000000000000, 0.000000000000000000 ) ) ;
#34002=VECTOR ( 'NONE', #62537, 999.9999999999998863 ) ;
#34049=ORIENTED_EDGE ( 'NONE', *, *, #137897, .T. ) ;
#34111=DIRECTION ( 'NONE',  ( 0.000000000000000000, -1.000000000000000000, 0.000000000000000000 ) ) ;
#34118=ORIENTED_EDGE ( 'NONE', *, *, #7277, .T. ) ;
#34133=VERTEX_POINT ( 'NONE', #133535 ) ;
#34150=CIRCLE ( 'NONE', #73474, 2.500000000000000888 ) ;
#34169=ORIENTED_EDGE ( 'NONE', *, *, #1508, .T. ) ;
#34216=DIRECTION ( 'NONE',  ( -1.000000000000000000, -0.000000000000000000, -0.000000000000000000 ) ) ;
#34229=DIRECTION ( 'NONE',  ( 1.000000000000000000, 1.224606353822377258E-16, 0.000000000000000000 ) ) ;
#34252=ORIENTED_EDGE ( 'NONE', *, *, #137632, .T. ) ;
#34271=DIRECTION ( 'NONE',  ( -1.000000000000000000, -1.224606353822377258E-16, -0.000000000000000000 ) ) ;
#34301=DIRECTION ( 'NONE',  ( -1.000000000000000000, -1.224606353822377258E-16, -0.000000000000000000 ) ) ;
#34321=AXIS2_PLACEMENT_3D ( 'NONE', #80412, #36865, #26011 ) ;
#34361=EDGE_LOOP ( 'NONE', ( #18014, #65218, #117805, #121158, #46525, #93190 ) ) ;
#34363=ORIENTED_EDGE ( 'NONE', *, *, #109809, .T. ) ;
#34382=CONICAL_SURFACE ( 'NONE', #31995, 2.500000000000000888, 0.9599310885968822538 ) ;
#34387=CARTESIAN_POINT ( 'NONE',  ( 18.95159235450331892, 9.902892378096218942E-16, 0.000000000000000000 ) ) ;
#34451=VECTOR ( 'NONE', #81714, 1000.000000000000000 ) ;
#34464=ADVANCED_FACE ( 'NONE', ( #9389 ), #27552, .T. ) ;
#34469=FACE_OUTER_BOUND ( 'NONE', #107121, .T. ) ;
#34476=VERTEX_POINT ( 'NONE', #10138 ) ;
#34512=EDGE_CURVE ( 'NONE', #139953, #87542, #43834, .T. ) ;
#34523=CIRCLE ( 'NONE', #76232, 2.500000000000000888 ) ;
#34596=ORIENTED_EDGE ( 'NONE', *, *, #40328, .F. ) ;
#34607=CARTESIAN_POINT ( 'NONE',  ( 9.748407645496676821, 9.139736423841732040E-16, 0.000000000000000000 ) ) ;
#34657=EDGE_CURVE ( 'NONE', #65821, #36066, #31883, .T. ) ;
#34659=FACE_OUTER_BOUND ( 'NONE', #50424, .T. ) ;
#34664=DIRECTION ( 'NONE',  ( -1.000000000000000000, -1.224606353822377258E-16, -0.000000000000000000 ) ) ;
#34703=ORIENTED_EDGE ( 'NONE', *, *, #111097, .T. ) ;
#34707=CARTESIAN_POINT ( 'NONE',  ( 4.911592354503321545, 9.902892378096218942E-16, 0.000000000000000000 ) ) ;
#34724=EDGE_CURVE ( 'NONE', #113538, #118058, #71236, .T. ) ;
#34741=ADVANCED_FACE ( 'NONE', ( #91981 ), #68961, .T. ) ;
#34772=ORIENTED_EDGE ( 'NONE', *, *, #42040, .T. ) ;
#34774=DIRECTION ( 'NONE',  ( -1.000000000000000000, -0.000000000000000000, -0.000000000000000000 ) ) ;
#34782=DIRECTION ( 'NONE',  ( 1.000000000000000000, 1.224606353822377258E-16, 0.000000000000000000 ) ) ;
#34791=LINE ( 'NONE', #46413, #18160 ) ;
#34812=CARTESIAN_POINT ( 'NONE',  ( 15.52000000000000135, -2.055000000000000160, 2.789133085058098087E-16 ) ) ;
#34824=DIRECTION ( 'NONE',  ( -1.000000000000000000, -1.224606353822377258E-16, -0.000000000000000000 ) ) ;
#34827=CARTESIAN_POINT ( 'NONE',  ( 10.83999999999999986, 2.055000000000001492, 0.000000000000000000 ) ) ;
#34860=CARTESIAN_POINT ( 'NONE',  ( -25.39999999999996305, 0.000000000000000000, 2.500000000000000000 ) ) ;
#34870=VERTEX_POINT ( 'NONE', #40483 ) ;
#34887=DIRECTION ( 'NONE',  ( 0.000000000000000000, -1.000000000000000000, 0.000000000000000000 ) ) ;
#34899=CARTESIAN_POINT ( 'NONE',  ( 11.93159235450332112, 9.902892378096218942E-16, 0.000000000000000000 ) ) ;
#34900=CARTESIAN_POINT ( 'NONE',  ( 6.940000000000001279, 9.521314400968980422E-16, 0.000000000000000000 ) ) ;
#34913=AXIS2_PLACEMENT_3D ( 'NONE', #48642, #135650, #105151 ) ;
#34961=ORIENTED_EDGE ( 'NONE', *, *, #77140, .F. ) ;
#35026=EDGE_CURVE ( 'NONE', #80827, #103460, #105641, .T. ) ;
#35032=ADVANCED_FACE ( 'NONE', ( #19561 ), #6078, .T. ) ;
#35056=AXIS2_PLACEMENT_3D ( 'NONE', #8251, #52498, #22005 ) ;
#35065=CONICAL_SURFACE ( 'NONE', #53567, 2.055000000000001048, 0.9599310885968758145 ) ;
#35155=ADVANCED_FACE ( 'NONE', ( #94088 ), #43192, .T. ) ;
#35158=CIRCLE ( 'NONE', #102206, 2.500000000000000888 ) ;
#35166=FACE_OUTER_BOUND ( 'NONE', #138560, .T. ) ;
#35194=VECTOR ( 'NONE', #64817, 1000.000000000000000 ) ;
#35228=CARTESIAN_POINT ( 'NONE',  ( 24.09999999999999787, 9.521314400968980422E-16, 0.000000000000000000 ) ) ;
#35239=DIRECTION ( 'NONE',  ( 0.5735764363510451602, 0.8191520442889924647, 0.000000000000000000 ) ) ;
#35303=VECTOR ( 'NONE', #138409, 1000.000000000000000 ) ;
#35318=ORIENTED_EDGE ( 'NONE', *, *, #53692, .T. ) ;
#35331=CARTESIAN_POINT ( 'NONE',  ( 19.88840764549667384, 9.139736423841732040E-16, 0.000000000000000000 ) ) ;
#35354=CARTESIAN_POINT ( 'NONE',  ( 2.999999999999999112, 0.000000000000000000, 2.500000000000000000 ) ) ;
#35364=EDGE_LOOP ( 'NONE', ( #92721, #68807, #59020, #66938, #54156 ) ) ;
#35419=VERTEX_POINT ( 'NONE', #135839 ) ;
#35459=DIRECTION ( 'NONE',  ( -1.000000000000000000, -1.224606353822377258E-16, -0.000000000000000000 ) ) ;
#35479=STYLED_ITEM ( 'NONE', ( #85290 ), #53301 ) ;
#35482=ADVANCED_FACE ( 'NONE', ( #114766 ), #12616, .T. ) ;
#35501=EDGE_LOOP ( 'NONE', ( #69491, #82081, #132152, #30671, #33362 ) ) ;
#35537=ADVANCED_FACE ( 'NONE', ( #24316 ), #89624, .T. ) ;
#35572=DIRECTION ( 'NONE',  ( 0.000000000000000000, -1.000000000000000000, 0.000000000000000000 ) ) ;
#35588=CARTESIAN_POINT ( 'NONE',  ( 16.30000000000000071, 9.521314400968980422E-16, 0.000000000000000000 ) ) ;
#35611=DIRECTION ( 'NONE',  ( 0.000000000000000000, -1.000000000000000000, 0.000000000000000000 ) ) ;
#35623=ORIENTED_EDGE ( 'NONE', *, *, #104312, .T. ) ;
#35625=VERTEX_POINT ( 'NONE', #67865 ) ;
#35639=CARTESIAN_POINT ( 'NONE',  ( 6.940000000000001279, 9.521314400968980422E-16, 0.000000000000000000 ) ) ;
#35679=CARTESIAN_POINT ( 'NONE',  ( -25.39999999999996305, 3.061616997868383141E-16, -2.500000000000000000 ) ) ;
#35704=VERTEX_POINT ( 'NONE', #114170 ) ;
#35705=CARTESIAN_POINT ( 'NONE',  ( 15.20840764549667767, 9.139736423841732040E-16, 0.000000000000000000 ) ) ;
#35710=LINE ( 'NONE', #103070, #83096 ) ;
#35718=AXIS2_PLACEMENT_3D ( 'NONE', #22578, #133533, #101595 ) ;
#35731=DIRECTION ( 'NONE',  ( -1.000000000000000000, -1.224606353822377258E-16, -0.000000000000000000 ) ) ;
#35798=ORIENTED_EDGE ( 'NONE', *, *, #29284, .F. ) ;
#35799=VECTOR ( 'NONE', #37683, 1000.000000000000000 ) ;
#35831=CIRCLE ( 'NONE', #26586, 2.055000000000001048 ) ;
#35849=EDGE_LOOP ( 'NONE', ( #93357, #113284, #7500, #108196, #131005 ) ) ;
#35885=CARTESIAN_POINT ( 'NONE',  ( 20.97999999999999687, 9.521314400968980422E-16, 0.000000000000000000 ) ) ;
#35886=DIRECTION ( 'NONE',  ( -0.5735764363510507113, 0.8191520442889885789, 1.003171929053520926E-16 ) ) ;
#35898=DIRECTION ( 'NONE',  ( 0.000000000000000000, -1.000000000000000000, 0.000000000000000000 ) ) ;
#35925=DIRECTION ( 'NONE',  ( -1.000000000000000000, -0.000000000000000000, -0.000000000000000000 ) ) ;
#35950=EDGE_LOOP ( 'NONE', ( #9750, #16698, #20293, #99952, #32776 ) ) ;
#35964=ORIENTED_EDGE ( 'NONE', *, *, #76790, .F. ) ;
#35984=EDGE_CURVE ( 'NONE', #97600, #109094, #41448, .T. ) ;
#35990=CIRCLE ( 'NONE', #49953, 2.055000000000001048 ) ;
#36066=VERTEX_POINT ( 'NONE', #76980 ) ;
#36125=ORIENTED_EDGE ( 'NONE', *, *, #107903, .F. ) ;
#36130=ADVANCED_FACE ( 'NONE', ( #118018 ), #83290, .T. ) ;
#36219=DIRECTION ( 'NONE',  ( -1.000000000000000000, -0.000000000000000000, -0.000000000000000000 ) ) ;
#36264=CARTESIAN_POINT ( 'NONE',  ( 13.18000000000000149, 9.521314400968980422E-16, 0.000000000000000000 ) ) ;
#36267=VERTEX_POINT ( 'NONE', #78866 ) ;
#36272=ORIENTED_EDGE ( 'NONE', *, *, #88963, .T. ) ;
#36276=CARTESIAN_POINT ( 'NONE',  ( 5.691592354503320905, 9.902892378096218942E-16, 0.000000000000000000 ) ) ;
#36308=AXIS2_PLACEMENT_3D ( 'NONE', #8065, #42173, #28434 ) ;
#36347=ORIENTED_EDGE ( 'NONE', *, *, #81767, .F. ) ;
#36372=CARTESIAN_POINT ( 'NONE',  ( 26.75159235450331963, 9.902892378096218942E-16, 0.000000000000000000 ) ) ;
#36375=FACE_OUTER_BOUND ( 'NONE', #70413, .T. ) ;
#36398=EDGE_LOOP ( 'NONE', ( #136381, #116032, #74308, #9106, #54345 ) ) ;
#36449=EDGE_CURVE ( 'NONE', #99997, #128260, #127150, .T. ) ;
#36518=VERTEX_POINT ( 'NONE', #21255 ) ;
#36534=DIRECTION ( 'NONE',  ( 0.000000000000000000, -1.000000000000000000, 0.000000000000000000 ) ) ;
#36537=AXIS2_PLACEMENT_3D ( 'NONE', #108124, #17053, #116360 ) ;
#36568=DIRECTION ( 'NONE',  ( 0.000000000000000000, -1.000000000000000000, 0.000000000000000000 ) ) ;
#36617=ORIENTED_EDGE ( 'NONE', *, *, #136444, .F. ) ;
#36635=ORIENTED_EDGE ( 'NONE', *, *, #21276, .T. ) ;
#36655=ORIENTED_EDGE ( 'NONE', *, *, #127046, .T. ) ;
#36659=VERTEX_POINT ( 'NONE', #131565 ) ;
#36671=VERTEX_POINT ( 'NONE', #86649 ) ;
#36699=ORIENTED_EDGE ( 'NONE', *, *, #16118, .T. ) ;
#36704=DIRECTION ( 'NONE',  ( 0.000000000000000000, 0.000000000000000000, 1.000000000000000000 ) ) ;
#36709=ADVANCED_FACE ( 'NONE', ( #55438 ), #103951, .T. ) ;
#36734=AXIS2_PLACEMENT_3D ( 'NONE', #49957, #26754, #72451 ) ;
#36779=DIRECTION ( 'NONE',  ( 0.000000000000000000, -1.000000000000000000, 0.000000000000000000 ) ) ;
#36788=EDGE_CURVE ( 'NONE', #137207, #87397, #18360, .T. ) ;
#36801=DIRECTION ( 'NONE',  ( -1.000000000000000000, -0.000000000000000000, -0.000000000000000000 ) ) ;
#36822=ORIENTED_EDGE ( 'NONE', *, *, #59381, .T. ) ;
#36825=AXIS2_PLACEMENT_3D ( 'NONE', #143336, #10654, #54921 ) ;
#36846=CARTESIAN_POINT ( 'NONE',  ( 11.30840764549667554, 3.061616997868380183E-16, -2.500000000000001332 ) ) ;
#36849=DIRECTION ( 'NONE',  ( -1.000000000000000000, -1.224606353822377258E-16, -0.000000000000000000 ) ) ;
#36865=DIRECTION ( 'NONE',  ( -1.000000000000000000, -1.224606353822377258E-16, -0.000000000000000000 ) ) ;
#36868=ORIENTED_EDGE ( 'NONE', *, *, #138230, .F. ) ;
#36936=DIRECTION ( 'NONE',  ( 0.000000000000000000, 0.000000000000000000, 1.000000000000000000 ) ) ;
#36948=ORIENTED_EDGE ( 'NONE', *, *, #81725, .T. ) ;
#36957=DIRECTION ( 'NONE',  ( 0.000000000000000000, 0.000000000000000000, 1.000000000000000000 ) ) ;
#37047=DIRECTION ( 'NONE',  ( -1.000000000000000000, -1.224606353822377258E-16, -0.000000000000000000 ) ) ;
#37057=CARTESIAN_POINT ( 'NONE',  ( 15.98840764549667703, 2.500000000000003553, 3.061616997868386099E-16 ) ) ;
#37091=ORIENTED_EDGE ( 'NONE', *, *, #133318, .T. ) ;
#37095=ORIENTED_EDGE ( 'NONE', *, *, #8587, .F. ) ;
#37145=LINE ( 'NONE', #81399, #52337 ) ;
#37149=EDGE_CURVE ( 'NONE', #27619, #86236, #48506, .T. ) ;
#37160=DIRECTION ( 'NONE',  ( -1.000000000000000000, -0.000000000000000000, -0.000000000000000000 ) ) ;
#37185=ADVANCED_FACE ( 'NONE', ( #130703 ), #142287, .T. ) ;
#37196=AXIS2_PLACEMENT_3D ( 'NONE', #136856, #58653, #47750 ) ;
#37251=CARTESIAN_POINT ( 'NONE',  ( 16.30000000000000071, 9.521314400968980422E-16, 0.000000000000000000 ) ) ;
#37253=ORIENTED_EDGE ( 'NONE', *, *, #69640, .F. ) ;
#37255=ORIENTED_EDGE ( 'NONE', *, *, #24623, .F. ) ;
#37280=ORIENTED_EDGE ( 'NONE', *, *, #31247, .F. ) ;
#37322=EDGE_CURVE ( 'NONE', #16237, #24858, #15111, .T. ) ;
#37332=CARTESIAN_POINT ( 'NONE',  ( -25.39999999999996305, 3.061616997868383141E-16, -2.500000000000000000 ) ) ;
#37333=AXIS2_PLACEMENT_3D ( 'NONE', #67848, #112034, #71379 ) ;
#37432=ADVANCED_FACE ( 'NONE', ( #39030 ), #106382, .T. ) ;
#37470=ORIENTED_EDGE ( 'NONE', *, *, #54539, .T. ) ;
#37487=DIRECTION ( 'NONE',  ( 1.000000000000000000, 1.224606353822377258E-16, 0.000000000000000000 ) ) ;
#37492=EDGE_CURVE ( 'NONE', #56823, #3030, #117691, .T. ) ;
#37500=CARTESIAN_POINT ( 'NONE',  ( 21.76000000000000156, -2.055000000000000160, 2.789133085058098087E-16 ) ) ;
#37526=CONICAL_SURFACE ( 'NONE', #56065, 4.487534009422227577, 0.08726646259971666819 ) ;
#37552=VECTOR ( 'NONE', #134176, 1000.000000000000000 ) ;
#37585=VECTOR ( 'NONE', #4951, 1000.000000000000000 ) ;
#37616=CIRCLE ( 'NONE', #58462, 2.500000000000000888 ) ;
#37620=CARTESIAN_POINT ( 'NONE',  ( 22.07159235450331991, 9.902892378096218942E-16, 0.000000000000000000 ) ) ;
#37630=ORIENTED_EDGE ( 'NONE', *, *, #23773, .T. ) ;
#37683=DIRECTION ( 'NONE',  ( -0.5735764363510507113, 0.8191520442889885789, 1.003171929053520926E-16 ) ) ;
#37724=VECTOR ( 'NONE', #136366, 1000.000000000000000 ) ;
#37757=DIRECTION ( 'NONE',  ( 0.5735764363510453823, -0.8191520442889923537, 1.003171929053525486E-16 ) ) ;
#37800=ADVANCED_FACE ( 'NONE', ( #15628 ), #34382, .T. ) ;
#37841=ORIENTED_EDGE ( 'NONE', *, *, #22221, .F. ) ;
#37843=EDGE_CURVE ( 'NONE', #137207, #35625, #19253, .T. ) ;
#37844=CONICAL_SURFACE ( 'NONE', #118832, 2.500000000000000888, 0.9599310885968822538 ) ;
#37851=DIRECTION ( 'NONE',  ( -1.000000000000000000, -1.224606353822377258E-16, -0.000000000000000000 ) ) ;
#37864=AXIS2_PLACEMENT_3D ( 'NONE', #139470, #41525, #42991 ) ;
#37961=DIRECTION ( 'NONE',  ( -1.000000000000000000, -1.224606353822377258E-16, -0.000000000000000000 ) ) ;
#37971=ORIENTED_EDGE ( 'NONE', *, *, #122511, .T. ) ;
#37975=FACE_OUTER_BOUND ( 'NONE', #103779, .T. ) ;
#37990=DIRECTION ( 'NONE',  ( 0.000000000000000000, -1.000000000000000000, 0.000000000000000000 ) ) ;
#38011=ORIENTED_EDGE ( 'NONE', *, *, #105342, .F. ) ;
#38022=EDGE_CURVE ( 'NONE', #78032, #103081, #42468, .T. ) ;
#38028=AXIS2_PLACEMENT_3D ( 'NONE', #33347, #65969, #117597 ) ;
#38030=ORIENTED_EDGE ( 'NONE', *, *, #30201, .T. ) ;
#38045=CARTESIAN_POINT ( 'NONE',  ( 6.471592354503322042, -2.500000000000000444, 3.061616997868384620E-16 ) ) ;
#38081=DIRECTION ( 'NONE',  ( -1.000000000000000000, -1.224606353822377258E-16, -0.000000000000000000 ) ) ;
#38093=EDGE_LOOP ( 'NONE', ( #109123, #107733, #53461, #135462, #1387 ) ) ;
#38096=DIRECTION ( 'NONE',  ( 0.000000000000000000, 0.000000000000000000, 1.000000000000000000 ) ) ;
#38102=CARTESIAN_POINT ( 'NONE',  ( 18.95159235450331892, 9.902892378096218942E-16, 0.000000000000000000 ) ) ;
#38108=EDGE_CURVE ( 'NONE', #105436, #40538, #55189, .T. ) ;
#38117=EDGE_CURVE ( 'NONE', #64517, #61398, #113010, .T. ) ;
#38130=CIRCLE ( 'NONE', #47485, 2.055000000000001048 ) ;
#38159=ORIENTED_EDGE ( 'NONE', *, *, #33549, .F. ) ;
#38164=FACE_OUTER_BOUND ( 'NONE', #35364, .T. ) ;
#38198=CIRCLE ( 'NONE', #119192, 2.500000000000000888 ) ;
#38220=ORIENTED_EDGE ( 'NONE', *, *, #58205, .F. ) ;
#38227=EDGE_CURVE ( 'NONE', #103631, #110059, #5325, .T. ) ;
#38234=ORIENTED_EDGE ( 'NONE', *, *, #7298, .F. ) ;
#38239=ORIENTED_EDGE ( 'NONE', *, *, #63734, .F. ) ;
#38244=DIRECTION ( 'NONE',  ( 1.000000000000000000, 1.224606353822377258E-16, 0.000000000000000000 ) ) ;
#38264=CARTESIAN_POINT ( 'NONE',  ( 8.811592354503320124, 2.500000000000001332, 0.000000000000000000 ) ) ;
#38265=DIRECTION ( 'NONE',  ( 0.5735764363510451602, 0.8191520442889924647, 0.000000000000000000 ) ) ;
#38302=EDGE_LOOP ( 'NONE', ( #97042, #109494, #44942, #11371, #28262, #53819 ) ) ;
#38329=DIRECTION ( 'NONE',  ( -0.5735764363510503783, -0.8191520442889886899, 0.000000000000000000 ) ) ;
#38348=CIRCLE ( 'NONE', #86891, 2.500000000000000888 ) ;
#38375=DIRECTION ( 'NONE',  ( 0.000000000000000000, -1.000000000000000000, 0.000000000000000000 ) ) ;
#38384=CARTESIAN_POINT ( 'NONE',  ( -25.39999999999996305, 0.000000000000000000, 0.000000000000000000 ) ) ;
#38428=EDGE_CURVE ( 'NONE', #76586, #139177, #35710, .T. ) ;
#38473=CONICAL_SURFACE ( 'NONE', #59405, 2.055000000000001048, 0.9599310885968758145 ) ;
#38476=DIRECTION ( 'NONE',  ( 0.000000000000000000, -1.000000000000000000, 0.000000000000000000 ) ) ;
#38588=AXIS2_PLACEMENT_3D ( 'NONE', #29300, #31461, #64807 ) ;
#38595=CARTESIAN_POINT ( 'NONE',  ( -25.39999999999996305, 0.000000000000000000, 0.000000000000000000 ) ) ;
#38600=AXIS2_PLACEMENT_3D ( 'NONE', #116625, #73149, #5695 ) ;
#38683=EDGE_CURVE ( 'NONE', #24873, #42879, #73776, .T. ) ;
#38694=ORIENTED_EDGE ( 'NONE', *, *, #94408, .F. ) ;
#38709=DIRECTION ( 'NONE',  ( -1.000000000000000000, -1.224606353822377258E-16, -0.000000000000000000 ) ) ;
#38741=VERTEX_POINT ( 'NONE', #123246 ) ;
#38791=CIRCLE ( 'NONE', #61889, 2.055000000000001048 ) ;
#38811=ORIENTED_EDGE ( 'NONE', *, *, #118482, .T. ) ;
#38838=ORIENTED_EDGE ( 'NONE', *, *, #15403, .T. ) ;
#38871=CYLINDRICAL_SURFACE ( 'NONE', #69679, 2.500000000000000000 ) ;
#38900=DIRECTION ( 'NONE',  ( 0.000000000000000000, -1.000000000000000000, 0.000000000000000000 ) ) ;
#38967=DIRECTION ( 'NONE',  ( 0.000000000000000000, -1.000000000000000000, 0.000000000000000000 ) ) ;
#38971=VERTEX_POINT ( 'NONE', #94843 ) ;
#38977=EDGE_LOOP ( 'NONE', ( #1030, #70106, #7218, #61350, #124759 ) ) ;
#39008=CARTESIAN_POINT ( 'NONE',  ( 8.031592354503320763, 3.061616997868380183E-16, -2.500000000000001332 ) ) ;
#39014=DIRECTION ( 'NONE',  ( 0.000000000000000000, -1.000000000000000000, 0.000000000000000000 ) ) ;
#39030=FACE_OUTER_BOUND ( 'NONE', #12901, .T. ) ;
#39042=CARTESIAN_POINT ( 'NONE',  ( 10.83999999999999986, 9.521314400968980422E-16, 0.000000000000000000 ) ) ;
#39054=DIRECTION ( 'NONE',  ( 0.000000000000000000, -1.000000000000000000, 0.000000000000000000 ) ) ;
#39079=CIRCLE ( 'NONE', #64632, 2.500000000000000888 ) ;
#39080=EDGE_CURVE ( 'NONE', #55993, #108448, #85120, .T. ) ;
#39113=EDGE_CURVE ( 'NONE', #143241, #50481, #67825, .T. ) ;
#39140=ORIENTED_EDGE ( 'NONE', *, *, #29284, .T. ) ;
#39157=EDGE_CURVE ( 'NONE', #12547, #94195, #103623, .T. ) ;
#39158=VERTEX_POINT ( 'NONE', #14817 ) ;
#39163=EDGE_CURVE ( 'NONE', #4422, #137066, #78202, .T. ) ;
#39168=DIRECTION ( 'NONE',  ( -1.000000000000000000, -1.224606353822377258E-16, -0.000000000000000000 ) ) ;
#39289=LINE ( 'NONE', #42155, #31752 ) ;
#39309=ORIENTED_EDGE ( 'NONE', *, *, #138029, .T. ) ;
#39332=ORIENTED_EDGE ( 'NONE', *, *, #70450, .T. ) ;
#39333=CARTESIAN_POINT ( 'NONE',  ( 27.22000000000000242, 2.055000000000001492, 0.000000000000000000 ) ) ;
#39335=CONICAL_SURFACE ( 'NONE', #127262, 2.500000000000000888, 0.9599310885968822538 ) ;
#39337=CIRCLE ( 'NONE', #120300, 2.055000000000001048 ) ;
#39382=CARTESIAN_POINT ( 'NONE',  ( 25.97159235450331849, 2.500000000000001332, 0.000000000000000000 ) ) ;
#39384=CYLINDRICAL_SURFACE ( 'NONE', #59127, 2.500000000000000000 ) ;
#39390=DIRECTION ( 'NONE',  ( -1.000000000000000000, -1.224606353822377258E-16, -0.000000000000000000 ) ) ;
#39432=VERTEX_POINT ( 'NONE', #23374 ) ;
#39439=AXIS2_PLACEMENT_3D ( 'NONE', #92730, #137699, #81915 ) ;
#39468=EDGE_CURVE ( 'NONE', #62841, #82772, #143074, .T. ) ;
#39486=ORIENTED_EDGE ( 'NONE', *, *, #10470, .T. ) ;
#39503=EDGE_CURVE ( 'NONE', #113128, #115214, #8874, .T. ) ;
#39563=ORIENTED_EDGE ( 'NONE', *, *, #74083, .F. ) ;
#39589=DIRECTION ( 'NONE',  ( 0.000000000000000000, -1.000000000000000000, 0.000000000000000000 ) ) ;
#39592=VERTEX_POINT ( 'NONE', #59617 ) ;
#39611=AXIS2_PLACEMENT_3D ( 'NONE', #31366, #140810, #129964 ) ;
#39629=VECTOR ( 'NONE', #132558, 1000.000000000000000 ) ;
#39670=CONICAL_SURFACE ( 'NONE', #129883, 2.500000000000000888, 0.9599310885968822538 ) ;
#39676=CARTESIAN_POINT ( 'NONE',  ( 14.74000000000000021, -2.055000000000000160, 2.789133085058098087E-16 ) ) ;
#39685=ORIENTED_EDGE ( 'NONE', *, *, #72810, .T. ) ;
#39696=ORIENTED_EDGE ( 'NONE', *, *, #81767, .T. ) ;
#39744=ORIENTED_EDGE ( 'NONE', *, *, #115611, .T. ) ;
#39750=AXIS2_PLACEMENT_3D ( 'NONE', #52085, #118755, #19450 ) ;
#39754=CARTESIAN_POINT ( 'NONE',  ( -25.39999999999996305, 0.000000000000000000, 0.000000000000000000 ) ) ;
#39785=EDGE_CURVE ( 'NONE', #94195, #8957, #10189, .T. ) ;
#39794=CONICAL_SURFACE ( 'NONE', #88320, 2.055000000000001048, 0.9599310885968758145 ) ;
#39800=EDGE_CURVE ( 'NONE', #100733, #61244, #62198, .T. ) ;
#39802=ADVANCED_FACE ( 'NONE', ( #121095 ), #66238, .T. ) ;
#39806=DIRECTION ( 'NONE',  ( 0.000000000000000000, -1.000000000000000000, 0.000000000000000000 ) ) ;
#39816=ORIENTED_EDGE ( 'NONE', *, *, #95832, .F. ) ;
#39832=CARTESIAN_POINT ( 'NONE',  ( 21.76000000000000156, 2.055000000000001492, 0.000000000000000000 ) ) ;
#39839=DIRECTION ( 'NONE',  ( 0.000000000000000000, -1.000000000000000000, 0.000000000000000000 ) ) ;
#39876=AXIS2_PLACEMENT_3D ( 'NONE', #70188, #34664, #91212 ) ;
#39902=CARTESIAN_POINT ( 'NONE',  ( 24.09999999999999787, 9.521314400968980422E-16, 0.000000000000000000 ) ) ;
#39930=CARTESIAN_POINT ( 'NONE',  ( 25.34840764549667469, 2.499999999999998224, 3.061616997868380183E-16 ) ) ;
#39945=VERTEX_POINT ( 'NONE', #34827 ) ;
#39974=DIRECTION ( 'NONE',  ( 0.000000000000000000, -1.000000000000000000, 0.000000000000000000 ) ) ;
#40032=AXIS2_PLACEMENT_3D ( 'NONE', #18430, #140261, #40946 ) ;
#40055=ORIENTED_EDGE ( 'NONE', *, *, #44696, .T. ) ;
#40060=DIRECTION ( 'NONE',  ( 0.000000000000000000, 1.000000000000000000, 0.000000000000000000 ) ) ;
#40068=LINE ( 'NONE', #21843, #80486 ) ;
#40090=AXIS2_PLACEMENT_3D ( 'NONE', #30727, #19108, #63373 ) ;
#40119=VECTOR ( 'NONE', #34774, 1000.000000000000000 ) ;
#40122=DIRECTION ( 'NONE',  ( 1.000000000000000000, 1.224606353822377258E-16, 0.000000000000000000 ) ) ;
#40161=VECTOR ( 'NONE', #14206, 1000.000000000000000 ) ;
#40200=VERTEX_POINT ( 'NONE', #81927 ) ;
#40211=DIRECTION ( 'NONE',  ( -0.5735764363510507113, 0.8191520442889885789, 1.003171929053520926E-16 ) ) ;
#40221=FACE_OUTER_BOUND ( 'NONE', #13039, .T. ) ;
#40225=CARTESIAN_POINT ( 'NONE',  ( 4.911592354503321545, 2.500000000000001332, 0.000000000000000000 ) ) ;
#40229=EDGE_LOOP ( 'NONE', ( #91605, #130690, #60896, #52194, #13530, #36347 ) ) ;
#40237=DIRECTION ( 'NONE',  ( -1.000000000000000000, -1.224606353822377258E-16, -0.000000000000000000 ) ) ;
#40244=CIRCLE ( 'NONE', #121224, 2.500000000000000888 ) ;
#40245=VERTEX_POINT ( 'NONE', #10709 ) ;
#40256=ORIENTED_EDGE ( 'NONE', *, *, #123629, .T. ) ;
#40257=DIRECTION ( 'NONE',  ( 0.000000000000000000, 0.000000000000000000, 1.000000000000000000 ) ) ;
#40328=EDGE_CURVE ( 'NONE', #136372, #110693, #59513, .T. ) ;
#40338=DIRECTION ( 'NONE',  ( 0.000000000000000000, -1.000000000000000000, 0.000000000000000000 ) ) ;
#40391=AXIS2_PLACEMENT_3D ( 'NONE', #140951, #143107, #41645 ) ;
#40393=CARTESIAN_POINT ( 'NONE',  ( 19.73159235450332005, 3.061616997868380183E-16, -2.500000000000001332 ) ) ;
#40405=EDGE_CURVE ( 'NONE', #117002, #103562, #68035, .T. ) ;
#40434=CIRCLE ( 'NONE', #14934, 2.500000000000000888 ) ;
#40482=DIRECTION ( 'NONE',  ( -1.000000000000000000, -0.000000000000000000, -0.000000000000000000 ) ) ;
#40483=CARTESIAN_POINT ( 'NONE',  ( 15.20840764549667767, 3.061616997868380183E-16, -2.500000000000001332 ) ) ;
#40485=CARTESIAN_POINT ( 'NONE',  ( 21.44840764549667611, 0.000000000000000000, 2.500000000000001332 ) ) ;
#40530=EDGE_LOOP ( 'NONE', ( #73890, #30744, #69994, #57560, #71655, #124050 ) ) ;
#40538=VERTEX_POINT ( 'NONE', #13513 ) ;
#40618=DIRECTION ( 'NONE',  ( 0.000000000000000000, -1.000000000000000000, 0.000000000000000000 ) ) ;
#40628=CARTESIAN_POINT ( 'NONE',  ( 27.68840764549667455, 9.139736423841732040E-16, 0.000000000000000000 ) ) ;
#40705=DIRECTION ( 'NONE',  ( -1.000000000000000000, -1.224606353822377258E-16, -0.000000000000000000 ) ) ;
#40747=ADVANCED_FACE ( 'NONE', ( #102706 ), #38871, .T. ) ;
#40748=DIRECTION ( 'NONE',  ( 0.000000000000000000, -1.000000000000000000, 0.000000000000000000 ) ) ;
#40793=CARTESIAN_POINT ( 'NONE',  ( 15.52000000000000135, 2.055000000000001492, 0.000000000000000000 ) ) ;
#40797=EDGE_CURVE ( 'NONE', #15438, #105436, #96085, .T. ) ;
#40832=VECTOR ( 'NONE', #1985, 1000.000000000000000 ) ;
#40842=ORIENTED_EDGE ( 'NONE', *, *, #26102, .T. ) ;
#40894=VERTEX_POINT ( 'NONE', #9035 ) ;
#40946=DIRECTION ( 'NONE',  ( 0.000000000000000000, -1.000000000000000000, 0.000000000000000000 ) ) ;
#40959=CIRCLE ( 'NONE', #119568, 2.500000000000000888 ) ;
#40960=CONICAL_SURFACE ( 'NONE', #142781, 2.055000000000001048, 0.9599310885968758145 ) ;
#40961=CIRCLE ( 'NONE', #68822, 2.500000000000000888 ) ;
#40967=CARTESIAN_POINT ( 'NONE',  ( 10.37159235450332062, 2.500000000000001776, 0.000000000000000000 ) ) ;
#41032=CARTESIAN_POINT ( 'NONE',  ( 24.41159235450331977, 3.061616997868380183E-16, -2.500000000000001332 ) ) ;
#41033=LINE ( 'NONE', #10522, #80830 ) ;
#41050=ORIENTED_EDGE ( 'NONE', *, *, #37149, .F. ) ;
#41069=CARTESIAN_POINT ( 'NONE',  ( 25.19159235450331735, 9.902892378096218942E-16, 0.000000000000000000 ) ) ;
#41073=VERTEX_POINT ( 'NONE', #24943 ) ;
#41117=ORIENTED_EDGE ( 'NONE', *, *, #12785, .F. ) ;
#41147=CYLINDRICAL_SURFACE ( 'NONE', #104222, 2.500000000000000000 ) ;
#41159=CARTESIAN_POINT ( 'NONE',  ( 5.380000000000000782, 9.521314400968980422E-16, 0.000000000000000000 ) ) ;
#41180=VERTEX_POINT ( 'NONE', #83663 ) ;
#41210=CARTESIAN_POINT ( 'NONE',  ( 5.380000000000000782, 2.055000000000001492, 2.516649172247811554E-16 ) ) ;
#41231=ORIENTED_EDGE ( 'NONE', *, *, #103860, .T. ) ;
#41239=CARTESIAN_POINT ( 'NONE',  ( 26.75159235450331963, 2.500000000000001776, 0.000000000000000000 ) ) ;
#41249=CIRCLE ( 'NONE', #122260, 2.500000000000000888 ) ;
#41262=CARTESIAN_POINT ( 'NONE',  ( -25.39999999999996305, 3.061616997868383141E-16, -2.500000000000000000 ) ) ;
#41264=CARTESIAN_POINT ( 'NONE',  ( 12.08840764549667668, 9.139736423841732040E-16, 0.000000000000000000 ) ) ;
#41275=CARTESIAN_POINT ( 'NONE',  ( 24.87999999999999901, 9.521314400968980422E-16, 0.000000000000000000 ) ) ;
#41281=ORIENTED_EDGE ( 'NONE', *, *, #32972, .F. ) ;
#41312=CARTESIAN_POINT ( 'NONE',  ( 19.10840764549667270, 9.139736423841732040E-16, 0.000000000000000000 ) ) ;
#41337=CARTESIAN_POINT ( 'NONE',  ( 4.600000000000001421, -2.055000000000000160, 0.000000000000000000 ) ) ;
#41343=AXIS2_PLACEMENT_3D ( 'NONE', #128883, #96935, #75254 ) ;
#41361=CIRCLE ( 'NONE', #1891, 2.055000000000001048 ) ;
#41362=DIRECTION ( 'NONE',  ( 0.000000000000000000, -1.000000000000000000, 0.000000000000000000 ) ) ;
#41373=ORIENTED_EDGE ( 'NONE', *, *, #69555, .T. ) ;
#41403=DIRECTION ( 'NONE',  ( 0.000000000000000000, 1.000000000000000000, 0.000000000000000000 ) ) ;
#41407=DIRECTION ( 'NONE',  ( 0.000000000000000000, -1.000000000000000000, 0.000000000000000000 ) ) ;
#41435=ORIENTED_EDGE ( 'NONE', *, *, #82813, .T. ) ;
#41448=LINE ( 'NONE', #85661, #6862 ) ;
#41472=ORIENTED_EDGE ( 'NONE', *, *, #119947, .F. ) ;
#41483=EDGE_CURVE ( 'NONE', #124821, #105469, #122216, .T. ) ;
#41511=CARTESIAN_POINT ( 'NONE',  ( 8.811592354503320124, 9.902892378096218942E-16, 0.000000000000000000 ) ) ;
#41522=ORIENTED_EDGE ( 'NONE', *, *, #62387, .F. ) ;
#41525=DIRECTION ( 'NONE',  ( -1.000000000000000000, -0.000000000000000000, -0.000000000000000000 ) ) ;
#41552=CARTESIAN_POINT ( 'NONE',  ( 17.07999999999999829, 9.521314400968980422E-16, 0.000000000000000000 ) ) ;
#41553=CARTESIAN_POINT ( 'NONE',  ( 13.18000000000000149, -2.055000000000000160, 2.789133085058098087E-16 ) ) ;
#41564=ORIENTED_EDGE ( 'NONE', *, *, #7229, .F. ) ;
#41590=FACE_OUTER_BOUND ( 'NONE', #76637, .T. ) ;
#41609=ORIENTED_EDGE ( 'NONE', *, *, #56656, .T. ) ;
#41645=DIRECTION ( 'NONE',  ( 0.000000000000000000, -1.000000000000000000, 0.000000000000000000 ) ) ;
#41652=FACE_OUTER_BOUND ( 'NONE', #116198, .T. ) ;
#41674=LINE ( 'NONE', #74321, #108208 ) ;
#41685=ORIENTED_EDGE ( 'NONE', *, *, #2326, .T. ) ;
#41722=DIRECTION ( 'NONE',  ( 0.000000000000000000, -1.000000000000000000, 0.000000000000000000 ) ) ;
#41735=EDGE_CURVE ( 'NONE', #121024, #65687, #5410, .T. ) ;
#41745=CARTESIAN_POINT ( 'NONE',  ( 14.42840764549667476, 3.061616997868380183E-16, -2.500000000000001332 ) ) ;
#41804=ORIENTED_EDGE ( 'NONE', *, *, #83244, .F. ) ;
#41820=CARTESIAN_POINT ( 'NONE',  ( 16.61159235450331906, -2.500000000000000000, 3.061616997868384127E-16 ) ) ;
#41828=AXIS2_PLACEMENT_3D ( 'NONE', #65426, #109602, #82701 ) ;
#41842=AXIS2_PLACEMENT_3D ( 'NONE', #45173, #35731, #121952 ) ;
#41871=AXIS2_PLACEMENT_3D ( 'NONE', #92518, #56394, #59242 ) ;
#41913=CARTESIAN_POINT ( 'NONE',  ( -25.39999999999996305, 0.000000000000000000, 0.000000000000000000 ) ) ;
#41915=ORIENTED_EDGE ( 'NONE', *, *, #49128, .T. ) ;
#41933=VECTOR ( 'NONE', #62832, 1000.000000000000000 ) ;
#41950=EDGE_CURVE ( 'NONE', #97682, #28445, #113504, .T. ) ;
#41971=EDGE_CURVE ( 'NONE', #103076, #54110, #132964, .T. ) ;
#41990=EDGE_CURVE ( 'NONE', #70009, #24205, #44108, .T. ) ;
#41994=DIRECTION ( 'NONE',  ( -1.000000000000000000, -1.224606353822377258E-16, -0.000000000000000000 ) ) ;
#42040=EDGE_CURVE ( 'NONE', #24858, #29128, #111119, .T. ) ;
#42045=DIRECTION ( 'NONE',  ( 0.5735764363510451602, 0.8191520442889924647, 0.000000000000000000 ) ) ;
#42056=DIRECTION ( 'NONE',  ( 0.000000000000000000, 0.000000000000000000, 1.000000000000000000 ) ) ;
#42062=CIRCLE ( 'NONE', #7233, 2.500000000000000888 ) ;
#42117=FACE_OUTER_BOUND ( 'NONE', #35501, .T. ) ;
#42134=DIRECTION ( 'NONE',  ( 0.000000000000000000, -1.000000000000000000, 0.000000000000000000 ) ) ;
#42155=CARTESIAN_POINT ( 'NONE',  ( -25.39999999999996305, 3.061616997868383141E-16, -2.500000000000000000 ) ) ;
#42156=DIRECTION ( 'NONE',  ( 0.000000000000000000, -1.000000000000000000, 0.000000000000000000 ) ) ;
#42173=DIRECTION ( 'NONE',  ( -1.000000000000000000, -1.224606353822377258E-16, -0.000000000000000000 ) ) ;
#42208=EDGE_CURVE ( 'NONE', #73777, #45804, #65720, .T. ) ;
#42216=CONICAL_SURFACE ( 'NONE', #23336, 2.500000000000000888, 0.9599310885968822538 ) ;
#42217=CARTESIAN_POINT ( 'NONE',  ( 24.41159235450331977, -2.500000000000000000, 3.061616997868384127E-16 ) ) ;
#42219=CARTESIAN_POINT ( 'NONE',  ( 19.10840764549667270, 2.500000000000003553, 3.061616997868386099E-16 ) ) ;
#42229=VERTEX_POINT ( 'NONE', #118293 ) ;
#42262=DIRECTION ( 'NONE',  ( -1.000000000000000000, -1.224606353822377258E-16, -0.000000000000000000 ) ) ;
#42280=CYLINDRICAL_SURFACE ( 'NONE', #37864, 2.500000000000000000 ) ;
#42292=ORIENTED_EDGE ( 'NONE', *, *, #9344, .T. ) ;
#42309=DIRECTION ( 'NONE',  ( 1.000000000000000000, 1.224606353822377258E-16, 0.000000000000000000 ) ) ;
#42316=ORIENTED_EDGE ( 'NONE', *, *, #14229, .T. ) ;
#42322=VERTEX_POINT ( 'NONE', #129902 ) ;
#42351=MANIFOLD_SOLID_BREP ( 'ThdSchPat', #60289 ) ;
#42363=LINE ( 'NONE', #119859, #35194 ) ;
#42422=CARTESIAN_POINT ( 'NONE',  ( 27.22000000000000242, 9.521314400968980422E-16, 0.000000000000000000 ) ) ;
#42447=ORIENTED_EDGE ( 'NONE', *, *, #53692, .F. ) ;
#42449=EDGE_CURVE ( 'NONE', #116046, #106721, #21688, .T. ) ;
#42457=EDGE_LOOP ( 'NONE', ( #80928, #100571, #115681, #91832, #117669, #58654 ) ) ;
#42468=LINE ( 'NONE', #98935, #57488 ) ;
#42470=CARTESIAN_POINT ( 'NONE',  ( 12.40000000000000213, 9.521314400968980422E-16, 0.000000000000000000 ) ) ;
#42517=EDGE_CURVE ( 'NONE', #23695, #112275, #10080, .T. ) ;
#42518=DIRECTION ( 'NONE',  ( 0.000000000000000000, -1.224646799147353207E-16, 1.000000000000000000 ) ) ;
#42536=CIRCLE ( 'NONE', #61086, 2.500000000000000888 ) ;
#42574=DIRECTION ( 'NONE',  ( -1.000000000000000000, -1.224606353822377258E-16, -0.000000000000000000 ) ) ;
#42624=ORIENTED_EDGE ( 'NONE', *, *, #125979, .F. ) ;
#42659=CARTESIAN_POINT ( 'NONE',  ( 10.37159235450332062, 9.902892378096218942E-16, 0.000000000000000000 ) ) ;
#42746=ORIENTED_EDGE ( 'NONE', *, *, #74083, .T. ) ;
#42753=CARTESIAN_POINT ( 'NONE',  ( 5.848407645496676466, 9.139736423841732040E-16, 0.000000000000000000 ) ) ;
#42758=DIRECTION ( 'NONE',  ( 0.000000000000000000, -1.000000000000000000, 0.000000000000000000 ) ) ;
#42766=CARTESIAN_POINT ( 'NONE',  ( 9.748407645496676821, -3.851859888774471706E-31, 2.500000000000001332 ) ) ;
#42879=VERTEX_POINT ( 'NONE', #117061 ) ;
#42916=( NAMED_UNIT ( * ) PLANE_ANGLE_UNIT ( ) SI_UNIT ( $, .RADIAN. ) );
#42927=CARTESIAN_POINT ( 'NONE',  ( 14.74000000000000021, 2.055000000000001492, 0.000000000000000000 ) ) ;
#42978=FACE_OUTER_BOUND ( 'NONE', #16885, .T. ) ;
#42991=DIRECTION ( 'NONE',  ( 0.000000000000000000, 0.000000000000000000, 1.000000000000000000 ) ) ;
#42998=ORIENTED_EDGE ( 'NONE', *, *, #4273, .T. ) ;
#43007=CARTESIAN_POINT ( 'NONE',  ( 26.43999999999999773, 9.521314400968980422E-16, 0.000000000000000000 ) ) ;
#43087=VERTEX_POINT ( 'NONE', #132275 ) ;
#43129=CARTESIAN_POINT ( 'NONE',  ( 27.53159235450332076, -2.500000000000000444, 3.061616997868384620E-16 ) ) ;
#43192=CONICAL_SURFACE ( 'NONE', #142721, 2.055000000000001048, 0.9599310885968758145 ) ;
#43203=ADVANCED_FACE ( 'NONE', ( #67736 ), #93610, .T. ) ;
#43243=CARTESIAN_POINT ( 'NONE',  ( 24.41159235450331977, 9.902892378096218942E-16, 0.000000000000000000 ) ) ;
#43253=CIRCLE ( 'NONE', #36308, 2.055000000000001048 ) ;
#43254=AXIS2_PLACEMENT_3D ( 'NONE', #97209, #29834, #86392 ) ;
#43255=CARTESIAN_POINT ( 'NONE',  ( 0.1422498215950962208, -0.6000000000000000888, 3.724967290803190334 ) ) ;
#43257=EDGE_CURVE ( 'NONE', #30995, #94039, #40434, .T. ) ;
#43274=CARTESIAN_POINT ( 'NONE',  ( 4.288407645496676857, 3.061616997868380183E-16, -2.500000000000001332 ) ) ;
#43305=DIRECTION ( 'NONE',  ( 0.000000000000000000, -1.000000000000000000, 0.000000000000000000 ) ) ;
#43332=EDGE_CURVE ( 'NONE', #71117, #30243, #125661, .T. ) ;
#43357=VECTOR ( 'NONE', #18203, 1000.000000000000114 ) ;
#43374=EDGE_CURVE ( 'NONE', #99726, #88219, #133065, .T. ) ;
#43426=CARTESIAN_POINT ( 'NONE',  ( 17.07999999999999829, 2.055000000000001492, 2.516649172247811554E-16 ) ) ;
#43454=CARTESIAN_POINT ( 'NONE',  ( 17.85999999999999943, -2.055000000000000160, 2.789133085058098087E-16 ) ) ;
#43549=VERTEX_POINT ( 'NONE', #79157 ) ;
#43566=CIRCLE ( 'NONE', #50506, 2.500000000000000888 ) ;
#43647=DIRECTION ( 'NONE',  ( 0.000000000000000000, -1.000000000000000000, 0.000000000000000000 ) ) ;
#43686=CIRCLE ( 'NONE', #117742, 2.500000000000000888 ) ;
#43699=ORIENTED_EDGE ( 'NONE', *, *, #112485, .T. ) ;
#43700=EDGE_CURVE ( 'NONE', #35704, #58993, #61114, .T. ) ;
#43729=ORIENTED_EDGE ( 'NONE', *, *, #60406, .T. ) ;
#43761=VECTOR ( 'NONE', #126918, 1000.000000000000000 ) ;
#43764=ADVANCED_FACE ( 'NONE', ( #129744 ), #901, .T. ) ;
#43810=ORIENTED_EDGE ( 'NONE', *, *, #118549, .T. ) ;
#43820=EDGE_CURVE ( 'NONE', #29128, #110130, #24007, .T. ) ;
#43834=CIRCLE ( 'NONE', #143373, 2.500000000000000888 ) ;
#43894=CARTESIAN_POINT ( 'NONE',  ( 7.251592354503322291, 9.902892378096218942E-16, 0.000000000000000000 ) ) ;
#43947=AXIS2_PLACEMENT_3D ( 'NONE', #121917, #24065, #32820 ) ;
#43948=CIRCLE ( 'NONE', #46252, 2.500000000000000888 ) ;
#44003=EDGE_CURVE ( 'NONE', #116046, #21906, #65962, .T. ) ;
#44041=DIRECTION ( 'NONE',  ( -1.000000000000000000, -1.224606353822377258E-16, -0.000000000000000000 ) ) ;
#44108=CIRCLE ( 'NONE', #125104, 2.500000000000000888 ) ;
#44111=VECTOR ( 'NONE', #17996, 1000.000000000000000 ) ;
#44119=CARTESIAN_POINT ( 'NONE',  ( 0.8691381963085933471, 0.5999999999999987566, -4.444516329276119393 ) ) ;
#44156=VECTOR ( 'NONE', #11144, 1000.000000000000000 ) ;
#44167=AXIS2_PLACEMENT_3D ( 'NONE', #78316, #1426, #67465 ) ;
#44171=DIRECTION ( 'NONE',  ( -1.000000000000000000, -1.224606353822377258E-16, -0.000000000000000000 ) ) ;
#44180=DIRECTION ( 'NONE',  ( 0.000000000000000000, 1.000000000000000000, 0.000000000000000000 ) ) ;
#44190=VERTEX_POINT ( 'NONE', #12947 ) ;
#44226=DIRECTION ( 'NONE',  ( 0.000000000000000000, -1.000000000000000000, 0.000000000000000000 ) ) ;
#44264=VERTEX_POINT ( 'NONE', #39008 ) ;
#44306=AXIS2_PLACEMENT_3D ( 'NONE', #22609, #77760, #98763 ) ;
#44319=EDGE_CURVE ( 'NONE', #143429, #115828, #82097, .T. ) ;
#44321=ORIENTED_EDGE ( 'NONE', *, *, #127947, .T. ) ;
#44355=DIRECTION ( 'NONE',  ( -0.5735764363510503783, -0.8191520442889886899, 0.000000000000000000 ) ) ;
#44364=EDGE_CURVE ( 'NONE', #100733, #105469, #123563, .T. ) ;
#44373=VECTOR ( 'NONE', #72460, 1000.000000000000000 ) ;
#44409=CONICAL_SURFACE ( 'NONE', #74506, 2.500000000000000888, 0.9599310885968822538 ) ;
#44410=VECTOR ( 'NONE', #106130, 1000.000000000000000 ) ;
#44421=ORIENTED_EDGE ( 'NONE', *, *, #121421, .F. ) ;
#44482=ADVANCED_FACE ( 'NONE', ( #25628 ), #17179, .T. ) ;
#44557=ORIENTED_EDGE ( 'NONE', *, *, #119078, .F. ) ;
#44563=ADVANCED_FACE ( 'NONE', ( #115462 ), #10222, .T. ) ;
#44631=ORIENTED_EDGE ( 'NONE', *, *, #42517, .F. ) ;
#44636=CIRCLE ( 'NONE', #74616, 2.500000000000000888 ) ;
#44649=DIRECTION ( 'NONE',  ( 0.5735764363510453823, -0.8191520442889923537, 1.003171929053525486E-16 ) ) ;
#44663=DIRECTION ( 'NONE',  ( -0.5735764363510503783, -0.8191520442889886899, 0.000000000000000000 ) ) ;
#44688=DIRECTION ( 'NONE',  ( 0.000000000000000000, -1.000000000000000000, 0.000000000000000000 ) ) ;
#44692=CARTESIAN_POINT ( 'NONE',  ( 22.85159235450332105, 9.902892378096218942E-16, 0.000000000000000000 ) ) ;
#44696=EDGE_CURVE ( 'NONE', #143429, #123374, #84338, .T. ) ;
#44700=EDGE_CURVE ( 'NONE', #5088, #64283, #51694, .T. ) ;
#44707=( GEOMETRIC_REPRESENTATION_CONTEXT ( 3 ) GLOBAL_UNCERTAINTY_ASSIGNED_CONTEXT ( ( #101081 ) ) GLOBAL_UNIT_ASSIGNED_CONTEXT ( ( #15718, #17203, #62150 ) ) REPRESENTATION_CONTEXT ( 'NONE', 'WORKASPACE' ) );
#44790=DIRECTION ( 'NONE',  ( -0.000000000000000000, 0.000000000000000000, 1.000000000000000000 ) ) ;
#44844=DIRECTION ( 'NONE',  ( 0.5735764363510453823, -0.8191520442889923537, 1.003171929053525486E-16 ) ) ;
#44848=CARTESIAN_POINT ( 'NONE',  ( 14.42840764549667476, 9.139736423841732040E-16, 0.000000000000000000 ) ) ;
#44872=EDGE_CURVE ( 'NONE', #115828, #143429, #35831, .T. ) ;
#44886=ADVANCED_FACE ( 'NONE', ( #121659 ), #1303, .T. ) ;
#44887=LINE ( 'NONE', #67309, #66301 ) ;
#44889=AXIS2_PLACEMENT_3D ( 'NONE', #116306, #61955, #3925 ) ;
#44906=CARTESIAN_POINT ( 'NONE',  ( 19.41999999999999815, -2.055000000000000160, 2.789133085058098087E-16 ) ) ;
#44915=ORIENTED_EDGE ( 'NONE', *, *, #81553, .F. ) ;
#44918=VERTEX_POINT ( 'NONE', #69468 ) ;
#44942=ORIENTED_EDGE ( 'NONE', *, *, #125471, .T. ) ;
#44948=EDGE_CURVE ( 'NONE', #85310, #11989, #91227, .T. ) ;
#45019=DIRECTION ( 'NONE',  ( -1.000000000000000000, -1.224606353822377258E-16, -0.000000000000000000 ) ) ;
#45056=EDGE_CURVE ( 'NONE', #65959, #99234, #126143, .T. ) ;
#45081=VERTEX_POINT ( 'NONE', #95335 ) ;
#45099=DIRECTION ( 'NONE',  ( -1.000000000000000000, -1.224606353822377258E-16, -0.000000000000000000 ) ) ;
#45138=FACE_OUTER_BOUND ( 'NONE', #109800, .T. ) ;
#45173=CARTESIAN_POINT ( 'NONE',  ( 25.19159235450331735, 9.902892378096218942E-16, 0.000000000000000000 ) ) ;
#45187=EDGE_LOOP ( 'NONE', ( #115162, #109233, #34118, #40256, #90721 ) ) ;
#45219=AXIS2_PLACEMENT_3D ( 'NONE', #19305, #104881, #5549 ) ;
#45345=ORIENTED_EDGE ( 'NONE', *, *, #139762, .T. ) ;
#45358=AXIS2_PLACEMENT_3D ( 'NONE', #132253, #77164, #111909 ) ;
#45359=CARTESIAN_POINT ( 'NONE',  ( 1.369266385878517678, 5.729711685171558773E-16, 4.607329295533711289 ) ) ;
#45366=CARTESIAN_POINT ( 'NONE',  ( 8.500000000000000000, 2.055000000000001492, 0.000000000000000000 ) ) ;
#45374=CARTESIAN_POINT ( 'NONE',  ( 25.97159235450331849, 9.902892378096218942E-16, 0.000000000000000000 ) ) ;
#45380=DIRECTION ( 'NONE',  ( -1.000000000000000000, -1.224606353822377258E-16, -0.000000000000000000 ) ) ;
#45385=ORIENTED_EDGE ( 'NONE', *, *, #135183, .T. ) ;
#45417=CIRCLE ( 'NONE', #33811, 2.500000000000000888 ) ;
#45429=AXIS2_PLACEMENT_3D ( 'NONE', #43007, #119116, #97335 ) ;
#45497=DIRECTION ( 'NONE',  ( -0.5735764363510503783, -0.8191520442889886899, 0.000000000000000000 ) ) ;
#45514=CIRCLE ( 'NONE', #96350, 2.500000000000000888 ) ;
#45538=FACE_OUTER_BOUND ( 'NONE', #143378, .T. ) ;
#45544=AXIS2_PLACEMENT_3D ( 'NONE', #44692, #52653, #55533 ) ;
#45570=CARTESIAN_POINT ( 'NONE',  ( 11.62000000000000099, 9.521314400968980422E-16, 0.000000000000000000 ) ) ;
#45576=FACE_OUTER_BOUND ( 'NONE', #114251, .T. ) ;
#45665=DIRECTION ( 'NONE',  ( -1.000000000000000000, -1.224606353822377258E-16, -0.000000000000000000 ) ) ;
#45694=CONICAL_SURFACE ( 'NONE', #64193, 2.500000000000000888, 0.9599310885968822538 ) ;
#45708=ORIENTED_EDGE ( 'NONE', *, *, #20213, .F. ) ;
#45739=ORIENTED_EDGE ( 'NONE', *, *, #3217, .F. ) ;
#45759=AXIS2_PLACEMENT_3D ( 'NONE', #86735, #64258, #108423 ) ;
#45775=DIRECTION ( 'NONE',  ( 0.000000000000000000, -1.000000000000000000, 0.000000000000000000 ) ) ;
#45804=VERTEX_POINT ( 'NONE', #22570 ) ;
#45839=ORIENTED_EDGE ( 'NONE', *, *, #103346, .F. ) ;
#45842=CARTESIAN_POINT ( 'NONE',  ( -8.534745106696862769E-17, 0.000000000000000000, 0.000000000000000000 ) ) ;
#45854=ADVANCED_FACE ( 'NONE', ( #80582 ), #84355, .T. ) ;
#45882=LINE ( 'NONE', #133591, #23721 ) ;
#45895=AXIS2_PLACEMENT_3D ( 'NONE', #58364, #122849, #79396 ) ;
#45944=CIRCLE ( 'NONE', #129206, 4.582731094065999322 ) ;
#45975=CIRCLE ( 'NONE', #89914, 2.500000000000000888 ) ;
#45985=ADVANCED_FACE ( 'NONE', ( #97099 ), #98196, .T. ) ;
#46008=EDGE_CURVE ( 'NONE', #130559, #75959, #75143, .T. ) ;
#46016=EDGE_CURVE ( 'NONE', #76475, #72349, #26473, .T. ) ;
#46061=ORIENTED_EDGE ( 'NONE', *, *, #121354, .T. ) ;
#46087=CIRCLE ( 'NONE', #129346, 2.055000000000001048 ) ;
#46094=DIRECTION ( 'NONE',  ( -1.000000000000000000, -1.224606353822377258E-16, -0.000000000000000000 ) ) ;
#46096=CARTESIAN_POINT ( 'NONE',  ( 13.49159235450332162, 9.902892378096218942E-16, 0.000000000000000000 ) ) ;
#46177=ORIENTED_EDGE ( 'NONE', *, *, #75185, .T. ) ;
#46200=ORIENTED_EDGE ( 'NONE', *, *, #74441, .F. ) ;
#46242=ORIENTED_EDGE ( 'NONE', *, *, #14888, .T. ) ;
#46252=AXIS2_PLACEMENT_3D ( 'NONE', #16633, #100975, #115928 ) ;
#46316=DIRECTION ( 'NONE',  ( -1.000000000000000000, -1.224606353822377258E-16, -0.000000000000000000 ) ) ;
#46338=CARTESIAN_POINT ( 'NONE',  ( 23.00840764549667483, 9.139736423841732040E-16, 0.000000000000000000 ) ) ;
#46348=AXIS2_PLACEMENT_3D ( 'NONE', #61515, #62210, #39014 ) ;
#46360=AXIS2_PLACEMENT_3D ( 'NONE', #26891, #64520, #97868 ) ;
#46369=CARTESIAN_POINT ( 'NONE',  ( 11.93159235450332112, 9.902892378096218942E-16, 0.000000000000000000 ) ) ;
#46413=CARTESIAN_POINT ( 'NONE',  ( -25.39999999999996305, 0.000000000000000000, 2.500000000000000000 ) ) ;
#46420=DIRECTION ( 'NONE',  ( 0.000000000000000000, 0.000000000000000000, 1.000000000000000000 ) ) ;
#46425=ADVANCED_FACE ( 'NONE', ( #19934 ), #63368, .T. ) ;
#46451=DIRECTION ( 'NONE',  ( 0.000000000000000000, -1.000000000000000000, 0.000000000000000000 ) ) ;
#46467=CARTESIAN_POINT ( 'NONE',  ( 8.968407645496675684, 2.500000000000000888, 3.061616997868383141E-16 ) ) ;
#46498=CARTESIAN_POINT ( 'NONE',  ( 9.748407645496676821, 9.139736423841732040E-16, 0.000000000000000000 ) ) ;
#46512=DIRECTION ( 'NONE',  ( 0.000000000000000000, -1.000000000000000000, 0.000000000000000000 ) ) ;
#46525=ORIENTED_EDGE ( 'NONE', *, *, #140228, .F. ) ;
#46552=EDGE_LOOP ( 'NONE', ( #132522, #75659, #9379, #83802, #139733 ) ) ;
#46608=ORIENTED_EDGE ( 'NONE', *, *, #2889, .T. ) ;
#46642=CIRCLE ( 'NONE', #74438, 2.055000000000001048 ) ;
#46663=DIRECTION ( 'NONE',  ( 0.000000000000000000, -1.000000000000000000, 0.000000000000000000 ) ) ;
#46667=DIRECTION ( 'NONE',  ( 1.000000000000000000, 1.224606353822377258E-16, 0.000000000000000000 ) ) ;
#46675=ORIENTED_EDGE ( 'NONE', *, *, #31040, .F. ) ;
#46718=EDGE_CURVE ( 'NONE', #56823, #99997, #50283, .T. ) ;
#46730=EDGE_CURVE ( 'NONE', #143241, #26004, #41361, .T. ) ;
#46788=CARTESIAN_POINT ( 'NONE',  ( 17.39159235450332019, -3.851859888774471706E-31, 2.500000000000001332 ) ) ;
#46829=CIRCLE ( 'NONE', #21316, 2.500000000000000888 ) ;
#46854=ORIENTED_EDGE ( 'NONE', *, *, #18454, .T. ) ;
#46862=DIRECTION ( 'NONE',  ( -1.000000000000000000, -1.224606353822377258E-16, -0.000000000000000000 ) ) ;
#46882=CARTESIAN_POINT ( 'NONE',  ( 6.160000000000001030, 9.521314400968980422E-16, 0.000000000000000000 ) ) ;
#46883=CARTESIAN_POINT ( 'NONE',  ( 8.031592354503320763, 9.902892378096218942E-16, 0.000000000000000000 ) ) ;
#46890=AXIS2_PLACEMENT_3D ( 'NONE', #41552, #19096, #95941 ) ;
#46951=DIRECTION ( 'NONE',  ( -1.000000000000000000, -1.224606353822377258E-16, -0.000000000000000000 ) ) ;
#46953=ORIENTED_EDGE ( 'NONE', *, *, #116184, .T. ) ;
#46954=EDGE_CURVE ( 'NONE', #60103, #139953, #80604, .T. ) ;
#46997=ORIENTED_EDGE ( 'NONE', *, *, #76555, .F. ) ;
#46998=LINE ( 'NONE', #112208, #124989 ) ;
#47015=DIRECTION ( 'NONE',  ( -1.000000000000000000, -0.000000000000000000, -0.000000000000000000 ) ) ;
#47038=CARTESIAN_POINT ( 'NONE',  ( 15.05159235450332034, 9.902892378096218942E-16, 0.000000000000000000 ) ) ;
#47044=CARTESIAN_POINT ( 'NONE',  ( -25.39999999999996305, 0.000000000000000000, 0.000000000000000000 ) ) ;
#47055=DIRECTION ( 'NONE',  ( 0.000000000000000000, -1.000000000000000000, 0.000000000000000000 ) ) ;
#47078=DIRECTION ( 'NONE',  ( 0.000000000000000000, -1.000000000000000000, 0.000000000000000000 ) ) ;
#47079=CARTESIAN_POINT ( 'NONE',  ( 18.17159235450331778, 9.902892378096218942E-16, 0.000000000000000000 ) ) ;
#47102=ORIENTED_EDGE ( 'NONE', *, *, #57683, .F. ) ;
#47128=EDGE_CURVE ( 'NONE', #77035, #90453, #137112, .T. ) ;
#47155=CARTESIAN_POINT ( 'NONE',  ( 24.56840764549667355, -2.500000000000000888, 0.000000000000000000 ) ) ;
#47178=DIRECTION ( 'NONE',  ( 0.000000000000000000, -1.000000000000000000, 0.000000000000000000 ) ) ;
#47185=AXIS2_PLACEMENT_3D ( 'NONE', #62185, #117936, #70930 ) ;
#47215=ORIENTED_EDGE ( 'NONE', *, *, #88012, .T. ) ;
#47227=VECTOR ( 'NONE', #73211, 1000.000000000000000 ) ;
#47268=LINE ( 'NONE', #92840, #136711 ) ;
#47297=FACE_OUTER_BOUND ( 'NONE', #143450, .T. ) ;
#47349=CARTESIAN_POINT ( 'NONE',  ( 1.199999999999999956, 0.5999999999999987566, 4.543283425070392845 ) ) ;
#47485=AXIS2_PLACEMENT_3D ( 'NONE', #34900, #101547, #112446 ) ;
#47514=CIRCLE ( 'NONE', #133164, 2.500000000000000888 ) ;
#47520=CIRCLE ( 'NONE', #103040, 2.500000000000000888 ) ;
#47521=DIRECTION ( 'NONE',  ( 0.000000000000000000, -1.000000000000000000, 0.000000000000000000 ) ) ;
#47570=ORIENTED_EDGE ( 'NONE', *, *, #46008, .T. ) ;
#47589=EDGE_LOOP ( 'NONE', ( #70385, #126737, #73025, #31838, #4853 ) ) ;
#47604=LINE ( 'NONE', #91768, #40161 ) ;
#47645=DIRECTION ( 'NONE',  ( 0.5735764363510453823, -0.8191520442889923537, 1.003171929053525486E-16 ) ) ;
#47649=DIRECTION ( 'NONE',  ( -1.000000000000000000, -1.224606353822377258E-16, -0.000000000000000000 ) ) ;
#47703=VERTEX_POINT ( 'NONE', #137493 ) ;
#47705=AXIS2_PLACEMENT_3D ( 'NONE', #17791, #14947, #36704 ) ;
#47717=DIRECTION ( 'NONE',  ( -1.000000000000000000, -1.224606353822377258E-16, -0.000000000000000000 ) ) ;
#47728=DIRECTION ( 'NONE',  ( -1.000000000000000000, -1.224606353822377258E-16, -0.000000000000000000 ) ) ;
#47730=CIRCLE ( 'NONE', #1301, 1.500000000000000000 ) ;
#47750=DIRECTION ( 'NONE',  ( 0.000000000000000000, 1.000000000000000000, 0.000000000000000000 ) ) ;
#47773=EDGE_CURVE ( 'NONE', #106451, #141686, #122590, .T. ) ;
#47814=CARTESIAN_POINT ( 'NONE',  ( 1.199999999999999956, 0.5999999999999987566, -4.543283425070392845 ) ) ;
#47821=ORIENTED_EDGE ( 'NONE', *, *, #74982, .F. ) ;
#47887=EDGE_LOOP ( 'NONE', ( #142937, #128212, #84520, #118121, #68896, #70012 ) ) ;
#47888=VERTEX_POINT ( 'NONE', #76334 ) ;
#47890=ORIENTED_EDGE ( 'NONE', *, *, #102059, .T. ) ;
#47913=ORIENTED_EDGE ( 'NONE', *, *, #87721, .T. ) ;
#47923=VERTEX_POINT ( 'NONE', #54592 ) ;
#47965=ORIENTED_EDGE ( 'NONE', *, *, #42449, .T. ) ;
#47969=ORIENTED_EDGE ( 'NONE', *, *, #17787, .T. ) ;
#47982=DIRECTION ( 'NONE',  ( 0.000000000000000000, 1.000000000000000000, 0.000000000000000000 ) ) ;
#47991=EDGE_CURVE ( 'NONE', #103562, #128813, #81026, .T. ) ;
#47998=EDGE_CURVE ( 'NONE', #78032, #70129, #85645, .T. ) ;
#48009=CARTESIAN_POINT ( 'NONE',  ( -25.39999999999996305, 0.000000000000000000, 0.000000000000000000 ) ) ;
#48012=DIRECTION ( 'NONE',  ( 0.000000000000000000, -1.000000000000000000, 0.000000000000000000 ) ) ;
#48081=ORIENTED_EDGE ( 'NONE', *, *, #91935, .F. ) ;
#48152=DIRECTION ( 'NONE',  ( 0.000000000000000000, -1.000000000000000000, 0.000000000000000000 ) ) ;
#48171=CARTESIAN_POINT ( 'NONE',  ( 21.44840764549667611, 9.139736423841732040E-16, 0.000000000000000000 ) ) ;
#48180=CARTESIAN_POINT ( 'NONE',  ( 25.65999999999999659, 9.521314400968980422E-16, 0.000000000000000000 ) ) ;
#48185=CYLINDRICAL_SURFACE ( 'NONE', #4942, 2.500000000000000000 ) ;
#48191=CONICAL_SURFACE ( 'NONE', #57526, 2.055000000000001048, 0.9599310885968758145 ) ;
#48197=CARTESIAN_POINT ( 'NONE',  ( 12.71159235450332048, -2.500000000000000444, 3.061616997868384620E-16 ) ) ;
#48231=ORIENTED_EDGE ( 'NONE', *, *, #34724, .F. ) ;
#48243=DIRECTION ( 'NONE',  ( -1.000000000000000000, -0.000000000000000000, -0.000000000000000000 ) ) ;
#48256=ADVANCED_FACE ( 'NONE', ( #139309 ), #84216, .T. ) ;
#48257=ORIENTED_EDGE ( 'NONE', *, *, #43257, .F. ) ;
#48310=CARTESIAN_POINT ( 'NONE',  ( 11.93159235450332112, 2.500000000000001332, 0.000000000000000000 ) ) ;
#48314=EDGE_CURVE ( 'NONE', #26004, #92199, #29779, .T. ) ;
#48340=LINE ( 'NONE', #136764, #34451 ) ;
#48393=DIRECTION ( 'NONE',  ( 0.000000000000000000, -1.000000000000000000, 0.000000000000000000 ) ) ;
#48394=CIRCLE ( 'NONE', #2093, 2.500000000000000888 ) ;
#48403=CARTESIAN_POINT ( 'NONE',  ( -25.39999999999996305, 0.000000000000000000, 2.500000000000000000 ) ) ;
#48477=DIRECTION ( 'NONE',  ( -1.000000000000000000, -1.224606353822377258E-16, -0.000000000000000000 ) ) ;
#48488=VERTEX_POINT ( 'NONE', #102212 ) ;
#48506=CIRCLE ( 'NONE', #122583, 2.500000000000000888 ) ;
#48509=DIRECTION ( 'NONE',  ( -1.000000000000000000, -0.000000000000000000, -0.000000000000000000 ) ) ;
#48529=AXIS2_PLACEMENT_3D ( 'NONE', #96651, #20537, #85101 ) ;
#48557=ORIENTED_EDGE ( 'NONE', *, *, #132967, .F. ) ;
#48590=AXIS2_PLACEMENT_3D ( 'NONE', #1521, #87854, #21167 ) ;
#48608=ORIENTED_EDGE ( 'NONE', *, *, #14480, .T. ) ;
#48629=ORIENTED_EDGE ( 'NONE', *, *, #1429, .F. ) ;
#48642=CARTESIAN_POINT ( 'NONE',  ( 12.71159235450332048, 9.902892378096218942E-16, 0.000000000000000000 ) ) ;
#48646=DIRECTION ( 'NONE',  ( -1.000000000000000000, -1.224606353822377258E-16, -0.000000000000000000 ) ) ;
#48667=CARTESIAN_POINT ( 'NONE',  ( 27.99999999999999645, 2.055000000000001492, 2.789133085058098087E-16 ) ) ;
#48668=ORIENTED_EDGE ( 'NONE', *, *, #15992, .F. ) ;
#48671=CARTESIAN_POINT ( 'NONE',  ( -25.39999999999996305, 0.000000000000000000, 0.000000000000000000 ) ) ;
#48680=DIRECTION ( 'NONE',  ( -1.000000000000000000, -1.224606353822377258E-16, -0.000000000000000000 ) ) ;
#48702=CARTESIAN_POINT ( 'NONE',  ( -25.39999999999996305, 0.000000000000000000, 0.000000000000000000 ) ) ;
#48707=DIRECTION ( 'NONE',  ( 0.000000000000000000, 1.000000000000000000, 0.000000000000000000 ) ) ;
#48710=FACE_OUTER_BOUND ( 'NONE', #98873, .T. ) ;
#48833=CIRCLE ( 'NONE', #9460, 2.055000000000001048 ) ;
#48837=CARTESIAN_POINT ( 'NONE',  ( 9.591592354503321260, 9.902892378096218942E-16, 0.000000000000000000 ) ) ;
#48839=DIRECTION ( 'NONE',  ( 0.000000000000000000, -1.000000000000000000, 0.000000000000000000 ) ) ;
#48851=CONICAL_SURFACE ( 'NONE', #62721, 2.055000000000001048, 0.9599310885968758145 ) ;
#48859=CARTESIAN_POINT ( 'NONE',  ( 26.43999999999999773, 2.055000000000001492, 2.516649172247811554E-16 ) ) ;
#48886=EDGE_CURVE ( 'NONE', #84890, #42322, #4193, .T. ) ;
#48892=CIRCLE ( 'NONE', #129901, 2.500000000000000888 ) ;
#48895=CARTESIAN_POINT ( 'NONE',  ( 6.628407645496676714, 9.139736423841732040E-16, 0.000000000000000000 ) ) ;
#48908=CONICAL_SURFACE ( 'NONE', #127536, 2.055000000000001048, 0.9599310885968758145 ) ;
#48912=AXIS2_PLACEMENT_3D ( 'NONE', #28076, #61459, #138266 ) ;
#48924=CARTESIAN_POINT ( 'NONE',  ( 26.12840764549667583, 9.139736423841732040E-16, 0.000000000000000000 ) ) ;
#48944=CARTESIAN_POINT ( 'NONE',  ( 16.76840764549667639, 9.139736423841732040E-16, 0.000000000000000000 ) ) ;
#49034=FACE_OUTER_BOUND ( 'NONE', #109127, .T. ) ;
#49051=CIRCLE ( 'NONE', #86085, 2.500000000000000888 ) ;
#49076=CARTESIAN_POINT ( 'NONE',  ( 5.691592354503320905, -2.500000000000000444, 3.061616997868384620E-16 ) ) ;
#49086=EDGE_CURVE ( 'NONE', #55674, #117002, #48833, .T. ) ;
#49094=CONICAL_SURFACE ( 'NONE', #125446, 2.500000000000000888, 0.9599310885968822538 ) ;
#49117=CARTESIAN_POINT ( 'NONE',  ( 13.64840764549667540, 9.139736423841732040E-16, 0.000000000000000000 ) ) ;
#49128=EDGE_CURVE ( 'NONE', #121024, #40245, #14257, .T. ) ;
#49150=AXIS2_PLACEMENT_3D ( 'NONE', #33465, #13076, #770 ) ;
#49152=DIRECTION ( 'NONE',  ( -1.000000000000000000, -0.000000000000000000, -0.000000000000000000 ) ) ;
#49166=ORIENTED_EDGE ( 'NONE', *, *, #12907, .T. ) ;
#49225=VECTOR ( 'NONE', #104389, 1000.000000000000000 ) ;
#49361=DIRECTION ( 'NONE',  ( -1.000000000000000000, -1.224606353822377258E-16, -0.000000000000000000 ) ) ;
#49417=CARTESIAN_POINT ( 'NONE',  ( 6.471592354503322042, 9.902892378096218942E-16, 0.000000000000000000 ) ) ;
#49425=ADVANCED_FACE ( 'NONE', ( #87382 ), #119959, .F. ) ;
#49430=DIRECTION ( 'NONE',  ( 1.000000000000000000, 1.224606353822377258E-16, 0.000000000000000000 ) ) ;
#49464=MECHANICAL_DESIGN_GEOMETRIC_PRESENTATION_REPRESENTATION('',(#116575),#132857);
#49471=ORIENTED_EDGE ( 'NONE', *, *, #128334, .F. ) ;
#49477=ORIENTED_EDGE ( 'NONE', *, *, #124799, .F. ) ;
#49513=AXIS2_PLACEMENT_3D ( 'NONE', #44848, #1262, #132560 ) ;
#49575=EDGE_CURVE ( 'NONE', #109693, #118985, #133743, .T. ) ;
#49585=DIRECTION ( 'NONE',  ( 0.000000000000000000, 0.000000000000000000, 1.000000000000000000 ) ) ;
#49616=VERTEX_POINT ( 'NONE', #23537 ) ;
#49658=LINE ( 'NONE', #61953, #66958 ) ;
#49685=CARTESIAN_POINT ( 'NONE',  ( 11.30840764549667554, -2.499999999999998224, 0.000000000000000000 ) ) ;
#49705=DIRECTION ( 'NONE',  ( 0.000000000000000000, -1.000000000000000000, 0.000000000000000000 ) ) ;
#49736=AXIS2_PLACEMENT_3D ( 'NONE', #107946, #22371, #75370 ) ;
#49737=DIRECTION ( 'NONE',  ( 0.000000000000000000, -1.000000000000000000, 0.000000000000000000 ) ) ;
#49763=AXIS2_PLACEMENT_3D ( 'NONE', #100938, #56779, #22632 ) ;
#49765=EDGE_CURVE ( 'NONE', #38741, #72729, #32654, .T. ) ;
#49775=CARTESIAN_POINT ( 'NONE',  ( -25.39999999999996305, 0.000000000000000000, 0.000000000000000000 ) ) ;
#49807=FACE_OUTER_BOUND ( 'NONE', #71010, .T. ) ;
#49830=VERTEX_POINT ( 'NONE', #119613 ) ;
#49843=EDGE_LOOP ( 'NONE', ( #70941, #88094, #75825, #130486, #80248, #19622 ) ) ;
#49859=ORIENTED_EDGE ( 'NONE', *, *, #79441, .F. ) ;
#49871=CARTESIAN_POINT ( 'NONE',  ( 23.00840764549667483, 9.139736423841732040E-16, 0.000000000000000000 ) ) ;
#49925=CARTESIAN_POINT ( 'NONE',  ( 4.288407645496676857, 2.500000000000002220, 3.061616997868384620E-16 ) ) ;
#49934=EDGE_CURVE ( 'NONE', #131273, #88966, #108511, .T. ) ;
#49937=LINE ( 'NONE', #127471, #86459 ) ;
#49941=DIRECTION ( 'NONE',  ( 0.000000000000000000, -1.000000000000000000, 0.000000000000000000 ) ) ;
#49953=AXIS2_PLACEMENT_3D ( 'NONE', #67863, #46094, #44688 ) ;
#49957=CARTESIAN_POINT ( 'NONE',  ( 17.39159235450332019, 9.902892378096218942E-16, 0.000000000000000000 ) ) ;
#49986=VECTOR ( 'NONE', #35925, 1000.000000000000000 ) ;
#49992=AXIS2_PLACEMENT_3D ( 'NONE', #5811, #28332, #77847 ) ;
#50011=ORIENTED_EDGE ( 'NONE', *, *, #98673, .T. ) ;
#50014=EDGE_CURVE ( 'NONE', #5733, #54899, #46087, .T. ) ;
#50038=CARTESIAN_POINT ( 'NONE',  ( 20.51159235450331764, -2.500000000000000444, 3.061616997868384620E-16 ) ) ;
#50054=EDGE_CURVE ( 'NONE', #79257, #103562, #99211, .T. ) ;
#50068=DIRECTION ( 'NONE',  ( 0.000000000000000000, -1.000000000000000000, 0.000000000000000000 ) ) ;
#50075=ORIENTED_EDGE ( 'NONE', *, *, #47998, .F. ) ;
#50096=DIRECTION ( 'NONE',  ( 0.000000000000000000, -1.000000000000000000, 0.000000000000000000 ) ) ;
#50174=FACE_OUTER_BOUND ( 'NONE', #20249, .T. ) ;
#50175=VERTEX_POINT ( 'NONE', #109310 ) ;
#50195=CYLINDRICAL_SURFACE ( 'NONE', #23424, 2.500000000000000000 ) ;
#50227=ORIENTED_EDGE ( 'NONE', *, *, #19027, .F. ) ;
#50242=EDGE_LOOP ( 'NONE', ( #86700, #25566, #37470, #106690, #14907 ) ) ;
#50261=ORIENTED_EDGE ( 'NONE', *, *, #91474, .T. ) ;
#50269=CARTESIAN_POINT ( 'NONE',  ( 6.940000000000001279, 9.521314400968980422E-16, 0.000000000000000000 ) ) ;
#50283=LINE ( 'NONE', #27800, #115318 ) ;
#50341=DIRECTION ( 'NONE',  ( 1.000000000000000000, -0.000000000000000000, -0.000000000000000000 ) ) ;
#50362=ORIENTED_EDGE ( 'NONE', *, *, #44948, .T. ) ;
#50424=EDGE_LOOP ( 'NONE', ( #27410, #8295, #106507, #121820, #70492, #41804 ) ) ;
#50481=VERTEX_POINT ( 'NONE', #81719 ) ;
#50506=AXIS2_PLACEMENT_3D ( 'NONE', #130715, #108901, #33547 ) ;
#50546=ORIENTED_EDGE ( 'NONE', *, *, #30201, .F. ) ;
#50625=CARTESIAN_POINT ( 'NONE',  ( 4.600000000000001421, 9.521314400968980422E-16, 0.000000000000000000 ) ) ;
#50665=AXIS2_PLACEMENT_3D ( 'NONE', #32736, #141482, #98671 ) ;
#50719=DIRECTION ( 'NONE',  ( 0.000000000000000000, -1.000000000000000000, 0.000000000000000000 ) ) ;
#50723=ORIENTED_EDGE ( 'NONE', *, *, #79742, .F. ) ;
#50768=DIRECTION ( 'NONE',  ( 0.000000000000000000, 1.000000000000000000, 0.000000000000000000 ) ) ;
#50773=ORIENTED_EDGE ( 'NONE', *, *, #143462, .F. ) ;
#50774=CARTESIAN_POINT ( 'NONE',  ( 19.41999999999999815, 9.521314400968980422E-16, 0.000000000000000000 ) ) ;
#50780=CIRCLE ( 'NONE', #140998, 2.500000000000000888 ) ;
#50793=AXIS2_PLACEMENT_3D ( 'NONE', #102722, #95931, #115682 ) ;
#50808=DIRECTION ( 'NONE',  ( 0.000000000000000000, -1.000000000000000000, 0.000000000000000000 ) ) ;
#50822=EDGE_LOOP ( 'NONE', ( #58236, #111754, #16842, #36868, #73891 ) ) ;
#50827=CARTESIAN_POINT ( 'NONE',  ( 13.96000000000000085, 2.055000000000001492, 0.000000000000000000 ) ) ;
#50895=DIRECTION ( 'NONE',  ( -1.000000000000000000, -1.224606353822377258E-16, -0.000000000000000000 ) ) ;
#50906=AXIS2_PLACEMENT_3D ( 'NONE', #113950, #111060, #80627 ) ;
#50951=DIRECTION ( 'NONE',  ( -1.000000000000000000, -1.224606353822377258E-16, -0.000000000000000000 ) ) ;
#50962=DIRECTION ( 'NONE',  ( 0.5735764363510451602, 0.8191520442889924647, 0.000000000000000000 ) ) ;
#50964=FACE_OUTER_BOUND ( 'NONE', #78945, .T. ) ;
#50996=DIRECTION ( 'NONE',  ( -1.000000000000000000, -1.224606353822377258E-16, -0.000000000000000000 ) ) ;
#50999=CARTESIAN_POINT ( 'NONE',  ( 10.06000000000000050, 2.055000000000001492, 0.000000000000000000 ) ) ;
#51032=CARTESIAN_POINT ( 'NONE',  ( 20.19999999999999929, 9.521314400968980422E-16, 0.000000000000000000 ) ) ;
#51033=AXIS2_PLACEMENT_3D ( 'NONE', #12564, #122759, #56843 ) ;
#51043=ORIENTED_EDGE ( 'NONE', *, *, #132076, .T. ) ;
#51097=DIRECTION ( 'NONE',  ( 0.000000000000000000, -1.000000000000000000, 0.000000000000000000 ) ) ;
#51124=CONICAL_SURFACE ( 'NONE', #20978, 2.055000000000001048, 0.9599310885968758145 ) ;
#51143=ORIENTED_EDGE ( 'NONE', *, *, #33549, .T. ) ;
#51145=CYLINDRICAL_SURFACE ( 'NONE', #14431, 2.500000000000000000 ) ;
#51163=AXIS2_PLACEMENT_3D ( 'NONE', #68197, #76914, #100775 ) ;
#51218=EDGE_CURVE ( 'NONE', #85852, #121024, #101830, .T. ) ;
#51230=VECTOR ( 'NONE', #111052, 999.9999999999998863 ) ;
#51309=CIRCLE ( 'NONE', #132367, 4.750000000000000000 ) ;
#51367=EDGE_CURVE ( 'NONE', #36267, #130911, #103784, .T. ) ;
#51390=CIRCLE ( 'NONE', #7367, 2.500000000000000888 ) ;
#51428=VECTOR ( 'NONE', #118873, 1000.000000000000000 ) ;
#51485=AXIS2_PLACEMENT_3D ( 'NONE', #59877, #125115, #72221 ) ;
#51494=CIRCLE ( 'NONE', #2832, 2.500000000000000888 ) ;
#51503=EDGE_CURVE ( 'NONE', #143429, #128927, #52980, .T. ) ;
#51520=DIRECTION ( 'NONE',  ( 0.000000000000000000, -1.000000000000000000, 0.000000000000000000 ) ) ;
#51575=ADVANCED_FACE ( 'NONE', ( #84916 ), #55590, .T. ) ;
#51578=DIRECTION ( 'NONE',  ( 0.000000000000000000, -1.000000000000000000, 0.000000000000000000 ) ) ;
#51588=VERTEX_POINT ( 'NONE', #129129 ) ;
#51627=ORIENTED_EDGE ( 'NONE', *, *, #30602, .F. ) ;
#51629=CIRCLE ( 'NONE', #132681, 2.500000000000000888 ) ;
#51694=LINE ( 'NONE', #35679, #123780 ) ;
#51735=EDGE_LOOP ( 'NONE', ( #39816, #98567, #62415, #28693, #139224 ) ) ;
#51758=VERTEX_POINT ( 'NONE', #68713 ) ;
#51868=DIRECTION ( 'NONE',  ( 0.5735764363510453823, -0.8191520442889923537, 1.003171929053525486E-16 ) ) ;
#51870=DIRECTION ( 'NONE',  ( 0.000000000000000000, -1.000000000000000000, 0.000000000000000000 ) ) ;
#51952=CARTESIAN_POINT ( 'NONE',  ( 1.500000000000000000, 3.812371101874758372E-16, -3.113037248396092416 ) ) ;
#51959=AXIS2_PLACEMENT_3D ( 'NONE', #116221, #39390, #61182 ) ;
#51974=ORIENTED_EDGE ( 'NONE', *, *, #119367, .F. ) ;
#51983=CARTESIAN_POINT ( 'NONE',  ( 0.5743220282099938956, -0.6000000000000000888, 4.263778219380816914 ) ) ;
#52012=EDGE_CURVE ( 'NONE', #16132, #36659, #62309, .T. ) ;
#52024=DIRECTION ( 'NONE',  ( 0.000000000000000000, -1.000000000000000000, 0.000000000000000000 ) ) ;
#52041=CONICAL_SURFACE ( 'NONE', #142398, 2.055000000000001048, 0.9599310885968758145 ) ;
#52051=DIRECTION ( 'NONE',  ( 0.000000000000000000, -1.000000000000000000, 0.000000000000000000 ) ) ;
#52085=CARTESIAN_POINT ( 'NONE',  ( 23.63159235450331863, 9.902892378096218942E-16, 0.000000000000000000 ) ) ;
#52121=CIRCLE ( 'NONE', #77608, 2.500000000000000888 ) ;
#52130=ADVANCED_FACE ( 'NONE', ( #34469 ), #64673, .T. ) ;
#52171=CARTESIAN_POINT ( 'NONE',  ( 21.44840764549667611, 9.139736423841732040E-16, 0.000000000000000000 ) ) ;
#52174=CARTESIAN_POINT ( 'NONE',  ( 22.07159235450331991, 2.500000000000001776, 0.000000000000000000 ) ) ;
#52194=ORIENTED_EDGE ( 'NONE', *, *, #142895, .T. ) ;
#52225=LINE ( 'NONE', #41337, #134911 ) ;
#52238=EDGE_CURVE ( 'NONE', #115828, #119455, #49658, .T. ) ;
#52272=LINE ( 'NONE', #140698, #93840 ) ;
#52276=ORIENTED_EDGE ( 'NONE', *, *, #27556, .T. ) ;
#52290=ORIENTED_EDGE ( 'NONE', *, *, #106090, .F. ) ;
#52337=VECTOR ( 'NONE', #134330, 1000.000000000000000 ) ;
#52359=ADVANCED_FACE ( 'NONE', ( #121297 ), #53164, .T. ) ;
#52375=DIRECTION ( 'NONE',  ( 0.000000000000000000, 1.000000000000000000, 0.000000000000000000 ) ) ;
#52395=ORIENTED_EDGE ( 'NONE', *, *, #108825, .T. ) ;
#52419=EDGE_LOOP ( 'NONE', ( #124088, #5196, #73520, #99839, #15341, #33180 ) ) ;
#52443=CIRCLE ( 'NONE', #8425, 2.500000000000000888 ) ;
#52492=AXIS2_PLACEMENT_3D ( 'NONE', #48702, #94332, #116801 ) ;
#52498=DIRECTION ( 'NONE',  ( -1.000000000000000000, -1.224606353822377258E-16, -0.000000000000000000 ) ) ;
#52510=CIRCLE ( 'NONE', #1562, 2.055000000000001048 ) ;
#52594=CIRCLE ( 'NONE', #1649, 2.500000000000000888 ) ;
#52614=EDGE_LOOP ( 'NONE', ( #34363, #126829, #17285, #17063, #99889, #114925 ) ) ;
#52632=CARTESIAN_POINT ( 'NONE',  ( 8.811592354503320124, 2.500000000000001776, 0.000000000000000000 ) ) ;
#52640=CIRCLE ( 'NONE', #61988, 2.500000000000000888 ) ;
#52652=AXIS2_PLACEMENT_3D ( 'NONE', #16432, #136097, #36779 ) ;
#52653=DIRECTION ( 'NONE',  ( 1.000000000000000000, 1.224606353822377258E-16, 0.000000000000000000 ) ) ;
#52664=ORIENTED_EDGE ( 'NONE', *, *, #40797, .T. ) ;
#52695=ORIENTED_EDGE ( 'NONE', *, *, #22794, .T. ) ;
#52720=ORIENTED_EDGE ( 'NONE', *, *, #120004, .F. ) ;
#52730=AXIS2_PLACEMENT_3D ( 'NONE', #130544, #119614, #64553 ) ;
#52734=DIRECTION ( 'NONE',  ( 0.000000000000000000, 1.000000000000000000, 0.000000000000000000 ) ) ;
#52753=DIRECTION ( 'NONE',  ( 0.000000000000000000, 0.000000000000000000, 1.000000000000000000 ) ) ;
#52775=ORIENTED_EDGE ( 'NONE', *, *, #51503, .T. ) ;
#52807=DIRECTION ( 'NONE',  ( 0.000000000000000000, 1.000000000000000000, 0.000000000000000000 ) ) ;
#52853=VERTEX_POINT ( 'NONE', #380 ) ;
#52856=VERTEX_POINT ( 'NONE', #87428 ) ;
#52876=DIRECTION ( 'NONE',  ( 1.000000000000000000, 1.224606353822377258E-16, 0.000000000000000000 ) ) ;
#52901=EDGE_LOOP ( 'NONE', ( #48557, #36617, #54894, #66743, #111542 ) ) ;
#52944=VERTEX_POINT ( 'NONE', #109877 ) ;
#52958=AXIS2_PLACEMENT_3D ( 'NONE', #41913, #84691, #52753 ) ;
#52962=DIRECTION ( 'NONE',  ( 1.000000000000000000, 0.000000000000000000, 0.000000000000000000 ) ) ;
#52971=CARTESIAN_POINT ( 'NONE',  ( 0.8681510425102002548, -0.5999999999999994227, -4.444131413071504610 ) ) ;
#52980=LINE ( 'NONE', #76193, #60249 ) ;
#52984=DIRECTION ( 'NONE',  ( 0.000000000000000000, 0.000000000000000000, 1.000000000000000000 ) ) ;
#52993=VERTEX_POINT ( 'NONE', #48197 ) ;
#53033=ORIENTED_EDGE ( 'NONE', *, *, #114547, .T. ) ;
#53069=CONICAL_SURFACE ( 'NONE', #82908, 2.500000000000000888, 0.9599310885968822538 ) ;
#53087=FACE_OUTER_BOUND ( 'NONE', #13572, .T. ) ;
#53088=DIRECTION ( 'NONE',  ( 1.000000000000000000, 1.224606353822377258E-16, 0.000000000000000000 ) ) ;
#53105=DIRECTION ( 'NONE',  ( -1.000000000000000000, -1.224606353822377258E-16, -0.000000000000000000 ) ) ;
#53138=AXIS2_PLACEMENT_3D ( 'NONE', #102005, #57103, #113577 ) ;
#53164=CONICAL_SURFACE ( 'NONE', #48529, 2.500000000000000888, 0.9599310885968822538 ) ;
#53195=DIRECTION ( 'NONE',  ( 1.000000000000000000, 0.000000000000000000, 0.000000000000000000 ) ) ;
#53248=CARTESIAN_POINT ( 'NONE',  ( -25.39999999999996305, 3.061616997868383141E-16, -2.500000000000000000 ) ) ;
#53254=ORIENTED_EDGE ( 'NONE', *, *, #101427, .F. ) ;
#53270=DIRECTION ( 'NONE',  ( 0.000000000000000000, -1.000000000000000000, 0.000000000000000000 ) ) ;
#53301=ADVANCED_BREP_SHAPE_REPRESENTATION ( '', ( #42351, #127880 ), #95551 ) ;
#53342=ORIENTED_EDGE ( 'NONE', *, *, #87391, .T. ) ;
#53413=AXIS2_PLACEMENT_3D ( 'NONE', #40628, #86275, #62384 ) ;
#53438=CIRCLE ( 'NONE', #21041, 2.500000000000000888 ) ;
#53461=ORIENTED_EDGE ( 'NONE', *, *, #79742, .T. ) ;
#53469=CIRCLE ( 'NONE', #130174, 2.500000000000000888 ) ;
#53491=ORIENTED_EDGE ( 'NONE', *, *, #39800, .F. ) ;
#53492=DIRECTION ( 'NONE',  ( 1.000000000000000000, -0.000000000000000000, -0.000000000000000000 ) ) ;
#53546=ORIENTED_EDGE ( 'NONE', *, *, #142827, .F. ) ;
#53553=DIRECTION ( 'NONE',  ( -1.000000000000000000, -1.224606353822377258E-16, -0.000000000000000000 ) ) ;
#53557=CARTESIAN_POINT ( 'NONE',  ( -25.39999999999996305, 0.000000000000000000, 2.500000000000000000 ) ) ;
#53562=CARTESIAN_POINT ( 'NONE',  ( 0.02893550784256476716, 0.5999999999999988676, -3.399425482353704453 ) ) ;
#53563=VECTOR ( 'NONE', #38329, 1000.000000000000114 ) ;
#53567=AXIS2_PLACEMENT_3D ( 'NONE', #45570, #47717, #25189 ) ;
#53587=ORIENTED_EDGE ( 'NONE', *, *, #52012, .T. ) ;
#53597=DIRECTION ( 'NONE',  ( -1.000000000000000000, -1.224606353822377258E-16, -0.000000000000000000 ) ) ;
#53611=EDGE_LOOP ( 'NONE', ( #41281, #28934, #34252, #77028, #24757 ) ) ;
#53625=VECTOR ( 'NONE', #61722, 1000.000000000000000 ) ;
#53646=EDGE_CURVE ( 'NONE', #101759, #113128, #109150, .T. ) ;
#53648=ORIENTED_EDGE ( 'NONE', *, *, #127836, .T. ) ;
#53662=AXIS2_PLACEMENT_3D ( 'NONE', #60653, #104075, #25829 ) ;
#53692=EDGE_CURVE ( 'NONE', #80743, #108597, #25843, .T. ) ;
#53717=AXIS2_PLACEMENT_3D ( 'NONE', #132174, #11046, #69059 ) ;
#53719=DIRECTION ( 'NONE',  ( -1.000000000000000000, -0.000000000000000000, -0.000000000000000000 ) ) ;
#53727=DIRECTION ( 'NONE',  ( -1.000000000000000000, -1.224606353822377258E-16, -0.000000000000000000 ) ) ;
#53754=DIRECTION ( 'NONE',  ( 0.000000000000000000, -1.000000000000000000, 0.000000000000000000 ) ) ;
#53764=AXIS2_PLACEMENT_3D ( 'NONE', #103415, #37487, #16396 ) ;
#53787=EDGE_LOOP ( 'NONE', ( #71510, #59624, #104890, #99403, #42316 ) ) ;
#53819=ORIENTED_EDGE ( 'NONE', *, *, #19738, .F. ) ;
#53883=ORIENTED_EDGE ( 'NONE', *, *, #94515, .T. ) ;
#53888=AXIS2_PLACEMENT_3D ( 'NONE', #107381, #141447, #42156 ) ;
#53889=EDGE_CURVE ( 'NONE', #38971, #133114, #95683, .T. ) ;
#53972=ORIENTED_EDGE ( 'NONE', *, *, #17388, .F. ) ;
#54026=DIRECTION ( 'NONE',  ( -1.000000000000000000, -1.224606353822377258E-16, -0.000000000000000000 ) ) ;
#54036=DIRECTION ( 'NONE',  ( 0.000000000000000000, -1.000000000000000000, 0.000000000000000000 ) ) ;
#54076=DIRECTION ( 'NONE',  ( 0.000000000000000000, -1.000000000000000000, 0.000000000000000000 ) ) ;
#54110=VERTEX_POINT ( 'NONE', #40393 ) ;
#54136=CIRCLE ( 'NONE', #128198, 2.500000000000000888 ) ;
#54138=CIRCLE ( 'NONE', #35718, 2.500000000000000888 ) ;
#54156=ORIENTED_EDGE ( 'NONE', *, *, #87663, .F. ) ;
#54168=ORIENTED_EDGE ( 'NONE', *, *, #44872, .F. ) ;
#54169=CARTESIAN_POINT ( 'NONE',  ( -25.39999999999996305, 0.000000000000000000, 0.000000000000000000 ) ) ;
#54216=VECTOR ( 'NONE', #27654, 1000.000000000000114 ) ;
#54219=FACE_OUTER_BOUND ( 'NONE', #97111, .T. ) ;
#54240=CIRCLE ( 'NONE', #109771, 2.055000000000001048 ) ;
#54242=CARTESIAN_POINT ( 'NONE',  ( 8.031592354503320763, 2.500000000000001332, 0.000000000000000000 ) ) ;
#54282=DIRECTION ( 'NONE',  ( 0.000000000000000000, 1.000000000000000000, 0.000000000000000000 ) ) ;
#54322=ORIENTED_EDGE ( 'NONE', *, *, #62147, .T. ) ;
#54345=ORIENTED_EDGE ( 'NONE', *, *, #4204, .F. ) ;
#54366=CARTESIAN_POINT ( 'NONE',  ( -25.39999999999996305, 3.061616997868383141E-16, -2.500000000000000000 ) ) ;
#54389=DIRECTION ( 'NONE',  ( -1.000000000000000000, -1.224606353822377258E-16, -0.000000000000000000 ) ) ;
#54410=ORIENTED_EDGE ( 'NONE', *, *, #24166, .F. ) ;
#54447=EDGE_CURVE ( 'NONE', #75313, #81350, #117716, .T. ) ;
#54452=CARTESIAN_POINT ( 'NONE',  ( 0.000000000000000000, -0.5999999999999994227, -3.054668707061620747 ) ) ;
#54539=EDGE_CURVE ( 'NONE', #39432, #59763, #42363, .T. ) ;
#54592=CARTESIAN_POINT ( 'NONE',  ( 20.51159235450331764, 3.061616997868380183E-16, -2.500000000000001332 ) ) ;
#54618=DIRECTION ( 'NONE',  ( 0.000000000000000000, -1.000000000000000000, 0.000000000000000000 ) ) ;
#54630=ORIENTED_EDGE ( 'NONE', *, *, #18379, .T. ) ;
#54632=DIRECTION ( 'NONE',  ( 0.000000000000000000, -1.000000000000000000, 0.000000000000000000 ) ) ;
#54654=CARTESIAN_POINT ( 'NONE',  ( 11.15159235450332176, -2.500000000000000444, 3.061616997868384620E-16 ) ) ;
#54681=CARTESIAN_POINT ( 'NONE',  ( 11.30840764549667554, 9.139736423841732040E-16, 0.000000000000000000 ) ) ;
#54715=DIRECTION ( 'NONE',  ( 0.000000000000000000, -1.000000000000000000, 0.000000000000000000 ) ) ;
#54739=DIRECTION ( 'NONE',  ( 0.000000000000000000, 1.000000000000000000, 0.000000000000000000 ) ) ;
#54753=CARTESIAN_POINT ( 'NONE',  ( 17.54840764549667398, 9.139736423841732040E-16, 0.000000000000000000 ) ) ;
#54828=ADVANCED_FACE ( 'NONE', ( #84279 ), #42216, .T. ) ;
#54843=CIRCLE ( 'NONE', #135858, 2.500000000000000888 ) ;
#54851=ORIENTED_EDGE ( 'NONE', *, *, #135510, .F. ) ;
#54894=ORIENTED_EDGE ( 'NONE', *, *, #4204, .T. ) ;
#54899=VERTEX_POINT ( 'NONE', #74824 ) ;
#54903=VERTEX_POINT ( 'NONE', #66078 ) ;
#54906=ORIENTED_EDGE ( 'NONE', *, *, #111600, .F. ) ;
#54921=DIRECTION ( 'NONE',  ( 0.000000000000000000, -1.000000000000000000, 0.000000000000000000 ) ) ;
#54942=CONICAL_SURFACE ( 'NONE', #6239, 2.055000000000001048, 0.9599310885968758145 ) ;
#54964=EDGE_LOOP ( 'NONE', ( #84063, #38030, #88564, #85011, #126489, #111189 ) ) ;
#55001=CARTESIAN_POINT ( 'NONE',  ( 0.2265654810057258217, 0.5999999999999987566, -3.877828006771851133 ) ) ;
#55052=CARTESIAN_POINT ( 'NONE',  ( 18.63999999999999702, 9.521314400968980422E-16, 0.000000000000000000 ) ) ;
#55057=DIRECTION ( 'NONE',  ( 0.000000000000000000, -1.000000000000000000, 0.000000000000000000 ) ) ;
#55093=EDGE_CURVE ( 'NONE', #34133, #30243, #16392, .T. ) ;
#55099=EDGE_CURVE ( 'NONE', #61244, #124821, #97427, .T. ) ;
#55101=ORIENTED_EDGE ( 'NONE', *, *, #44319, .F. ) ;
#55104=EDGE_CURVE ( 'NONE', #7326, #85293, #124716, .T. ) ;
#55107=ORIENTED_EDGE ( 'NONE', *, *, #60643, .F. ) ;
#55127=EDGE_CURVE ( 'NONE', #36659, #27842, #53469, .T. ) ;
#55155=ORIENTED_EDGE ( 'NONE', *, *, #29833, .F. ) ;
#55189=CIRCLE ( 'NONE', #45895, 2.500000000000000888 ) ;
#55224=ORIENTED_EDGE ( 'NONE', *, *, #26102, .F. ) ;
#55250=DIRECTION ( 'NONE',  ( 1.000000000000000000, 1.224606353822377258E-16, 0.000000000000000000 ) ) ;
#55253=CARTESIAN_POINT ( 'NONE',  ( 12.08840764549667668, -2.500000000000000888, 0.000000000000000000 ) ) ;
#55271=CARTESIAN_POINT ( 'NONE',  ( 18.95159235450331892, 9.902892378096218942E-16, 0.000000000000000000 ) ) ;
#55316=CYLINDRICAL_SURFACE ( 'NONE', #86703, 2.500000000000000000 ) ;
#55339=CIRCLE ( 'NONE', #57626, 2.055000000000001048 ) ;
#55342=CARTESIAN_POINT ( 'NONE',  ( 15.05159235450332034, 9.902892378096218942E-16, 0.000000000000000000 ) ) ;
#55377=AXIS2_PLACEMENT_3D ( 'NONE', #92509, #17799, #94652 ) ;
#55388=ORIENTED_EDGE ( 'NONE', *, *, #124330, .F. ) ;
#55404=CARTESIAN_POINT ( 'NONE',  ( 19.73159235450332005, 9.902892378096218942E-16, 0.000000000000000000 ) ) ;
#55438=FACE_OUTER_BOUND ( 'NONE', #139481, .T. ) ;
#55481=CARTESIAN_POINT ( 'NONE',  ( 13.49159235450332162, 9.902892378096218942E-16, 0.000000000000000000 ) ) ;
#55508=CARTESIAN_POINT ( 'NONE',  ( 5.848407645496676466, 9.139736423841732040E-16, 0.000000000000000000 ) ) ;
#55533=DIRECTION ( 'NONE',  ( 0.000000000000000000, 1.000000000000000000, 0.000000000000000000 ) ) ;
#55538=EDGE_CURVE ( 'NONE', #9860, #39432, #106737, .T. ) ;
#55590=CONICAL_SURFACE ( 'NONE', #115754, 2.500000000000000888, 0.9599310885968822538 ) ;
#55631=AXIS2_PLACEMENT_3D ( 'NONE', #63648, #88962, #43305 ) ;
#55642=ORIENTED_EDGE ( 'NONE', *, *, #109229, .T. ) ;
#55674=VERTEX_POINT ( 'NONE', #9712 ) ;
#55680=EDGE_CURVE ( 'NONE', #48488, #118031, #25828, .T. ) ;
#55686=CARTESIAN_POINT ( 'NONE',  ( 18.95159235450331892, -2.500000000000000000, 3.061616997868384127E-16 ) ) ;
#55714=ORIENTED_EDGE ( 'NONE', *, *, #41990, .F. ) ;
#55716=DIRECTION ( 'NONE',  ( -1.000000000000000000, -0.000000000000000000, -0.000000000000000000 ) ) ;
#55738=DIRECTION ( 'NONE',  ( -1.000000000000000000, -1.224606353822377258E-16, -0.000000000000000000 ) ) ;
#55748=DIRECTION ( 'NONE',  ( 0.000000000000000000, 1.000000000000000000, 0.000000000000000000 ) ) ;
#55756=DIRECTION ( 'NONE',  ( -1.000000000000000000, -1.224606353822377258E-16, -0.000000000000000000 ) ) ;
#55761=ORIENTED_EDGE ( 'NONE', *, *, #49765, .T. ) ;
#55762=VECTOR ( 'NONE', #104132, 999.9999999999998863 ) ;
#55787=ORIENTED_EDGE ( 'NONE', *, *, #135183, .F. ) ;
#55848=EDGE_CURVE ( 'NONE', #121372, #117339, #51309, .T. ) ;
#55859=FACE_OUTER_BOUND ( 'NONE', #10216, .T. ) ;
#55877=CARTESIAN_POINT ( 'NONE',  ( -25.39999999999996305, 0.000000000000000000, 2.500000000000000000 ) ) ;
#55885=ORIENTED_EDGE ( 'NONE', *, *, #99427, .F. ) ;
#55915=AXIS2_PLACEMENT_3D ( 'NONE', #35331, #79574, #123759 ) ;
#55993=VERTEX_POINT ( 'NONE', #140093 ) ;
#56003=AXIS2_PLACEMENT_3D ( 'NONE', #16039, #60331, #104512 ) ;
#56035=ORIENTED_EDGE ( 'NONE', *, *, #15370, .T. ) ;
#56053=DIRECTION ( 'NONE',  ( -1.000000000000000000, -0.000000000000000000, -0.000000000000000000 ) ) ;
#56065=AXIS2_PLACEMENT_3D ( 'NONE', #85039, #61892, #31382 ) ;
#56069=LINE ( 'NONE', #134321, #127877 ) ;
#56109=CARTESIAN_POINT ( 'NONE',  ( 21.29159235450332233, 9.902892378096218942E-16, 0.000000000000000000 ) ) ;
#56111=AXIS2_PLACEMENT_3D ( 'NONE', #79075, #23191, #67476 ) ;
#56129=CARTESIAN_POINT ( 'NONE',  ( 1.369266385878517678, 0.000000000000000000, 0.000000000000000000 ) ) ;
#56148=VECTOR ( 'NONE', #84759, 1000.000000000000000 ) ;
#56166=CARTESIAN_POINT ( 'NONE',  ( 6.628407645496676714, -3.851859888774471706E-31, 2.500000000000001332 ) ) ;
#56196=ORIENTED_EDGE ( 'NONE', *, *, #33855, .T. ) ;
#56203=AXIS2_PLACEMENT_3D ( 'NONE', #111234, #22771, #77929 ) ;
#56238=CARTESIAN_POINT ( 'NONE',  ( 7.408407645496676963, 9.139736423841732040E-16, 0.000000000000000000 ) ) ;
#56260=AXIS2_PLACEMENT_3D ( 'NONE', #133972, #70198, #113637 ) ;
#56277=CARTESIAN_POINT ( 'NONE',  ( 19.73159235450332005, -2.500000000000000000, 3.061616997868384127E-16 ) ) ;
#56333=ADVANCED_FACE ( 'NONE', ( #111732 ), #27917, .T. ) ;
#56337=EDGE_CURVE ( 'NONE', #103081, #15156, #85757, .T. ) ;
#56381=CONICAL_SURFACE ( 'NONE', #88747, 2.055000000000001048, 0.9599310885968758145 ) ;
#56394=DIRECTION ( 'NONE',  ( -1.000000000000000000, -1.224606353822377258E-16, -0.000000000000000000 ) ) ;
#56405=AXIS2_PLACEMENT_3D ( 'NONE', #83569, #74841, #63942 ) ;
#56418=VERTEX_POINT ( 'NONE', #26846 ) ;
#56468=CARTESIAN_POINT ( 'NONE',  ( -25.39999999999996305, 0.000000000000000000, 0.000000000000000000 ) ) ;
#56548=EDGE_LOOP ( 'NONE', ( #19581, #96185, #124411, #100642, #123519 ) ) ;
#56591=CARTESIAN_POINT ( 'NONE',  ( -25.39999999999996305, 0.000000000000000000, 0.000000000000000000 ) ) ;
#56646=AXIS2_PLACEMENT_3D ( 'NONE', #142095, #63115, #86973 ) ;
#56656=EDGE_CURVE ( 'NONE', #128813, #106215, #127072, .T. ) ;
#56664=ADVANCED_FACE ( 'NONE', ( #110803 ), #59944, .T. ) ;
#56680=EDGE_CURVE ( 'NONE', #112275, #39158, #69256, .T. ) ;
#56685=EDGE_LOOP ( 'NONE', ( #61552, #15669, #23567, #72752, #118404 ) ) ;
#56727=ORIENTED_EDGE ( 'NONE', *, *, #121238, .T. ) ;
#56731=CARTESIAN_POINT ( 'NONE',  ( 17.39159235450332019, 9.902892378096218942E-16, 0.000000000000000000 ) ) ;
#56743=LINE ( 'NONE', #126068, #103763 ) ;
#56758=ORIENTED_EDGE ( 'NONE', *, *, #37322, .F. ) ;
#56778=DIRECTION ( 'NONE',  ( 0.000000000000000000, -1.000000000000000000, 0.000000000000000000 ) ) ;
#56779=DIRECTION ( 'NONE',  ( -1.000000000000000000, -1.224606353822377258E-16, -0.000000000000000000 ) ) ;
#56819=DIRECTION ( 'NONE',  ( -1.000000000000000000, -1.224606353822377258E-16, -0.000000000000000000 ) ) ;
#56823=VERTEX_POINT ( 'NONE', #133861 ) ;
#56843=DIRECTION ( 'NONE',  ( 0.000000000000000000, -1.000000000000000000, 0.000000000000000000 ) ) ;
#56887=DIRECTION ( 'NONE',  ( 0.000000000000000000, -1.000000000000000000, 0.000000000000000000 ) ) ;
#56989=ADVANCED_FACE ( 'NONE', ( #27954 ), #73897, .T. ) ;
#57051=ORIENTED_EDGE ( 'NONE', *, *, #123929, .T. ) ;
#57068=CARTESIAN_POINT ( 'NONE',  ( 18.17159235450331778, -2.500000000000000000, 3.061616997868384127E-16 ) ) ;
#57102=EDGE_CURVE ( 'NONE', #123374, #73777, #57776, .T. ) ;
#57103=DIRECTION ( 'NONE',  ( -1.000000000000000000, -1.224606353822377258E-16, -0.000000000000000000 ) ) ;
#57118=CARTESIAN_POINT ( 'NONE',  ( -25.39999999999996305, 0.000000000000000000, 0.000000000000000000 ) ) ;
#57131=ADVANCED_FACE ( 'NONE', ( #88599 ), #53069, .T. ) ;
#57148=VERTEX_POINT ( 'NONE', #71486 ) ;
#57149=EDGE_LOOP ( 'NONE', ( #28232, #101027, #108979, #11178, #55107 ) ) ;
#57169=VERTEX_POINT ( 'NONE', #106213 ) ;
#57237=AXIS2_PLACEMENT_3D ( 'NONE', #84242, #107379, #41407 ) ;
#57323=DIRECTION ( 'NONE',  ( -1.000000000000000000, -0.000000000000000000, -0.000000000000000000 ) ) ;
#57336=CIRCLE ( 'NONE', #138333, 2.500000000000000888 ) ;
#57361=CARTESIAN_POINT ( 'NONE',  ( 6.628407645496676714, 9.139736423841732040E-16, 0.000000000000000000 ) ) ;
#57488=VECTOR ( 'NONE', #143169, 1000.000000000000000 ) ;
#57509=DIRECTION ( 'NONE',  ( -1.000000000000000000, -1.224606353822377258E-16, -0.000000000000000000 ) ) ;
#57516=CARTESIAN_POINT ( 'NONE',  ( 17.85999999999999943, 9.521314400968980422E-16, 0.000000000000000000 ) ) ;
#57526=AXIS2_PLACEMENT_3D ( 'NONE', #57589, #135156, #33692 ) ;
#57537=VECTOR ( 'NONE', #70408, 999.9999999999998863 ) ;
#57539=EDGE_LOOP ( 'NONE', ( #41435, #105428, #96550, #94614, #66362 ) ) ;
#57540=VERTEX_POINT ( 'NONE', #6010 ) ;
#57543=DIRECTION ( 'NONE',  ( 0.000000000000000000, 0.000000000000000000, 1.000000000000000000 ) ) ;
#57560=ORIENTED_EDGE ( 'NONE', *, *, #128913, .F. ) ;
#57586=CARTESIAN_POINT ( 'NONE',  ( 27.53159235450332076, 9.902892378096218942E-16, 0.000000000000000000 ) ) ;
#57589=CARTESIAN_POINT ( 'NONE',  ( 16.30000000000000071, 9.521314400968980422E-16, 0.000000000000000000 ) ) ;
#57626=AXIS2_PLACEMENT_3D ( 'NONE', #46882, #1828, #133142 ) ;
#57683=EDGE_CURVE ( 'NONE', #33609, #115095, #43566, .T. ) ;
#57746=EDGE_CURVE ( 'NONE', #28445, #63490, #56743, .T. ) ;
#57772=CARTESIAN_POINT ( 'NONE',  ( 16.76840764549667639, 9.139736423841732040E-16, 0.000000000000000000 ) ) ;
#57776=CIRCLE ( 'NONE', #20362, 2.500000000000000888 ) ;
#57911=DIRECTION ( 'NONE',  ( -1.000000000000000000, -1.224606353822377258E-16, -0.000000000000000000 ) ) ;
#57921=ADVANCED_FACE ( 'NONE', ( #97703 ), #128210, .T. ) ;
#57938=CARTESIAN_POINT ( 'NONE',  ( 0.000000000000000000, -0.6000000000000000888, 3.054668707061620747 ) ) ;
#57939=ORIENTED_EDGE ( 'NONE', *, *, #15957, .F. ) ;
#58029=DIRECTION ( 'NONE',  ( -1.000000000000000000, -0.000000000000000000, -0.000000000000000000 ) ) ;
#58054=CONICAL_SURFACE ( 'NONE', #113559, 2.055000000000001048, 0.9599310885968758145 ) ;
#58055=AXIS2_PLACEMENT_3D ( 'NONE', #61377, #125146, #124434 ) ;
#58069=DIRECTION ( 'NONE',  ( -1.000000000000000000, -1.224606353822377258E-16, -0.000000000000000000 ) ) ;
#58073=ORIENTED_EDGE ( 'NONE', *, *, #31040, .T. ) ;
#58077=DIRECTION ( 'NONE',  ( 0.000000000000000000, -1.000000000000000000, 0.000000000000000000 ) ) ;
#58121=ORIENTED_EDGE ( 'NONE', *, *, #79029, .T. ) ;
#58194=VECTOR ( 'NONE', #128841, 1000.000000000000000 ) ;
#58205=EDGE_CURVE ( 'NONE', #118058, #86236, #102714, .T. ) ;
#58211=CARTESIAN_POINT ( 'NONE',  ( 10.52840764549667618, 9.139736423841732040E-16, 0.000000000000000000 ) ) ;
#58236=ORIENTED_EDGE ( 'NONE', *, *, #29833, .T. ) ;
#58243=EDGE_CURVE ( 'NONE', #109156, #129380, #13626, .T. ) ;
#58287=AXIS2_PLACEMENT_3D ( 'NONE', #54681, #32202, #111154 ) ;
#58299=CYLINDRICAL_SURFACE ( 'NONE', #129205, 2.500000000000000000 ) ;
#58323=CARTESIAN_POINT ( 'NONE',  ( 12.71159235450332048, 9.902892378096218942E-16, 0.000000000000000000 ) ) ;
#58330=CARTESIAN_POINT ( 'NONE',  ( 5.848407645496676466, -2.499999999999999556, 0.000000000000000000 ) ) ;
#58331=DIRECTION ( 'NONE',  ( 1.000000000000000000, 1.224606353822377258E-16, 0.000000000000000000 ) ) ;
#58336=DIRECTION ( 'NONE',  ( 0.000000000000000000, -1.000000000000000000, 0.000000000000000000 ) ) ;
#58364=CARTESIAN_POINT ( 'NONE',  ( 8.968407645496675684, 9.139736423841732040E-16, 0.000000000000000000 ) ) ;
#58461=CIRCLE ( 'NONE', #86251, 2.500000000000000888 ) ;
#58462=AXIS2_PLACEMENT_3D ( 'NONE', #100717, #1361, #58692 ) ;
#58466=CIRCLE ( 'NONE', #51485, 2.055000000000001048 ) ;
#58476=VECTOR ( 'NONE', #9464, 1000.000000000000114 ) ;
#58496=LINE ( 'NONE', #136695, #104348 ) ;
#58523=DIRECTION ( 'NONE',  ( 0.5735764363510453823, -0.8191520442889923537, 1.003171929053525486E-16 ) ) ;
#58532=EDGE_CURVE ( 'NONE', #82772, #101759, #85449, .T. ) ;
#58533=DIRECTION ( 'NONE',  ( 0.000000000000000000, 1.000000000000000000, 0.000000000000000000 ) ) ;
#58541=DIRECTION ( 'NONE',  ( 0.000000000000000000, -1.000000000000000000, 0.000000000000000000 ) ) ;
#58587=CARTESIAN_POINT ( 'NONE',  ( 6.471592354503322042, -3.851859888774471706E-31, 2.500000000000001332 ) ) ;
#58633=( NAMED_UNIT ( * ) SI_UNIT ( $, .STERADIAN. ) SOLID_ANGLE_UNIT ( ) );
#58640=AXIS2_PLACEMENT_3D ( 'NONE', #19812, #8882, #61931 ) ;
#58647=DIRECTION ( 'NONE',  ( -0.5735764363510503783, -0.8191520442889886899, 0.000000000000000000 ) ) ;
#58652=CARTESIAN_POINT ( 'NONE',  ( 7.720000000000001528, 9.521314400968980422E-16, 0.000000000000000000 ) ) ;
#58653=DIRECTION ( 'NONE',  ( 1.000000000000000000, 1.224606353822377258E-16, 0.000000000000000000 ) ) ;
#58654=ORIENTED_EDGE ( 'NONE', *, *, #107183, .F. ) ;
#58662=ORIENTED_EDGE ( 'NONE', *, *, #39800, .T. ) ;
#58692=DIRECTION ( 'NONE',  ( 0.000000000000000000, -1.000000000000000000, 0.000000000000000000 ) ) ;
#58702=LINE ( 'NONE', #25282, #130633 ) ;
#58715=CARTESIAN_POINT ( 'NONE',  ( -25.39999999999996305, 0.000000000000000000, 2.500000000000000000 ) ) ;
#58738=CIRCLE ( 'NONE', #49513, 2.500000000000000888 ) ;
#58746=ORIENTED_EDGE ( 'NONE', *, *, #17418, .F. ) ;
#58747=EDGE_CURVE ( 'NONE', #32976, #12574, #134464, .T. ) ;
#58761=AXIS2_PLACEMENT_3D ( 'NONE', #13398, #135237, #12693 ) ;
#58802=DIRECTION ( 'NONE',  ( 0.000000000000000000, -1.000000000000000000, 0.000000000000000000 ) ) ;
#58837=CYLINDRICAL_SURFACE ( 'NONE', #75979, 2.500000000000000000 ) ;
#58851=EDGE_LOOP ( 'NONE', ( #44557, #63969, #85262, #96131, #8928 ) ) ;
#58857=DIRECTION ( 'NONE',  ( -1.000000000000000000, -0.000000000000000000, -0.000000000000000000 ) ) ;
#58877=CARTESIAN_POINT ( 'NONE',  ( 13.96000000000000085, 2.055000000000001492, 2.516649172247811554E-16 ) ) ;
#58888=FACE_OUTER_BOUND ( 'NONE', #90034, .T. ) ;
#58980=AXIS2_PLACEMENT_3D ( 'NONE', #55052, #88396, #42758 ) ;
#58982=PRODUCT_DEFINITION_CONTEXT ( 'detailed design', #139319, 'design' ) ;
#58993=VERTEX_POINT ( 'NONE', #26243 ) ;
#58999=EDGE_LOOP ( 'NONE', ( #97518, #51043, #24547, #76313, #77180 ) ) ;
#59020=ORIENTED_EDGE ( 'NONE', *, *, #27330, .F. ) ;
#59096=ADVANCED_FACE ( 'NONE', ( #68353 ), #39335, .T. ) ;
#59100=ORIENTED_EDGE ( 'NONE', *, *, #38117, .T. ) ;
#59105=DIRECTION ( 'NONE',  ( 0.000000000000000000, 0.000000000000000000, 1.000000000000000000 ) ) ;
#59108=EDGE_LOOP ( 'NONE', ( #20517, #47570, #8677, #139747, #30527, #26248 ) ) ;
#59127=AXIS2_PLACEMENT_3D ( 'NONE', #125117, #69332, #17587 ) ;
#59134=ORIENTED_EDGE ( 'NONE', *, *, #22668, .F. ) ;
#59207=ADVANCED_FACE ( 'NONE', ( #106613 ), #131840, .T. ) ;
#59235=DIRECTION ( 'NONE',  ( 0.000000000000000000, 0.000000000000000000, 1.000000000000000000 ) ) ;
#59242=DIRECTION ( 'NONE',  ( 0.000000000000000000, -1.000000000000000000, 0.000000000000000000 ) ) ;
#59282=ORIENTED_EDGE ( 'NONE', *, *, #2326, .F. ) ;
#59286=FACE_OUTER_BOUND ( 'NONE', #70555, .T. ) ;
#59342=CARTESIAN_POINT ( 'NONE',  ( 26.12840764549667583, 9.139736423841732040E-16, 0.000000000000000000 ) ) ;
#59351=EDGE_CURVE ( 'NONE', #20496, #38971, #69561, .T. ) ;
#59370=CARTESIAN_POINT ( 'NONE',  ( 11.62000000000000099, -2.055000000000000160, 0.000000000000000000 ) ) ;
#59372=EDGE_CURVE ( 'NONE', #138330, #64517, #86342, .T. ) ;
#59381=EDGE_CURVE ( 'NONE', #86236, #113805, #83406, .T. ) ;
#59394=DIRECTION ( 'NONE',  ( 0.5735764363510453823, -0.8191520442889923537, 1.003171929053525486E-16 ) ) ;
#59405=AXIS2_PLACEMENT_3D ( 'NONE', #75317, #53553, #110744 ) ;
#59408=DIRECTION ( 'NONE',  ( 0.000000000000000000, -1.000000000000000000, 0.000000000000000000 ) ) ;
#59474=EDGE_LOOP ( 'NONE', ( #80203, #54168, #65886, #78025, #97710 ) ) ;
#59494=DIRECTION ( 'NONE',  ( 0.000000000000000000, -1.000000000000000000, 0.000000000000000000 ) ) ;
#59502=CARTESIAN_POINT ( 'NONE',  ( 8.811592354503320124, -2.500000000000000000, 3.061616997868384127E-16 ) ) ;
#59513=CIRCLE ( 'NONE', #140502, 2.500000000000000888 ) ;
#59515=DIRECTION ( 'NONE',  ( -1.000000000000000000, -0.000000000000000000, -0.000000000000000000 ) ) ;
#59517=CONICAL_SURFACE ( 'NONE', #91876, 2.500000000000000888, 0.9599310885968822538 ) ;
#59555=DIRECTION ( 'NONE',  ( 0.000000000000000000, -1.000000000000000000, 0.000000000000000000 ) ) ;
#59598=FACE_OUTER_BOUND ( 'NONE', #124749, .T. ) ;
#59617=CARTESIAN_POINT ( 'NONE',  ( 4.288407645496676857, -3.851859888774471706E-31, 2.500000000000001332 ) ) ;
#59624=ORIENTED_EDGE ( 'NONE', *, *, #41950, .F. ) ;
#59632=ORIENTED_EDGE ( 'NONE', *, *, #13757, .F. ) ;
#59639=EDGE_LOOP ( 'NONE', ( #79519, #38838, #30231, #50362, #116520, #29857 ) ) ;
#59644=ADVANCED_FACE ( 'NONE', ( #115170 ), #141232, .T. ) ;
#59658=AXIS2_PLACEMENT_3D ( 'NONE', #129490, #99001, #143237 ) ;
#59709=EDGE_CURVE ( 'NONE', #130192, #122911, #9253, .T. ) ;
#59722=ORIENTED_EDGE ( 'NONE', *, *, #121354, .F. ) ;
#59731=CARTESIAN_POINT ( 'NONE',  ( -25.39999999999996305, 0.000000000000000000, 2.500000000000000000 ) ) ;
#59751=ORIENTED_EDGE ( 'NONE', *, *, #1664, .F. ) ;
#59763=VERTEX_POINT ( 'NONE', #48310 ) ;
#59793=ORIENTED_EDGE ( 'NONE', *, *, #23196, .T. ) ;
#59877=CARTESIAN_POINT ( 'NONE',  ( 13.96000000000000085, 9.521314400968980422E-16, 0.000000000000000000 ) ) ;
#59883=EDGE_LOOP ( 'NONE', ( #110060, #52395, #59958, #62127, #133541 ) ) ;
#59913=ADVANCED_FACE ( 'NONE', ( #128728 ), #51124, .T. ) ;
#59937=CARTESIAN_POINT ( 'NONE',  ( 4.911592354503321545, -2.500000000000000000, 3.061616997868384127E-16 ) ) ;
#59944=CONICAL_SURFACE ( 'NONE', #73789, 2.055000000000001048, 0.9599310885968758145 ) ;
#59951=DIRECTION ( 'NONE',  ( 0.000000000000000000, -1.000000000000000000, 0.000000000000000000 ) ) ;
#59958=ORIENTED_EDGE ( 'NONE', *, *, #74694, .T. ) ;
#59974=DIRECTION ( 'NONE',  ( 0.000000000000000000, 0.000000000000000000, 1.000000000000000000 ) ) ;
#60011=SURFACE_STYLE_FILL_AREA ( #18595 ) ;
#60013=ORIENTED_EDGE ( 'NONE', *, *, #99509, .T. ) ;
#60103=VERTEX_POINT ( 'NONE', #28550 ) ;
#60110=ORIENTED_EDGE ( 'NONE', *, *, #108528, .T. ) ;
#60165=DIRECTION ( 'NONE',  ( -1.000000000000000000, -1.224606353822377258E-16, -0.000000000000000000 ) ) ;
#60209=DIRECTION ( 'NONE',  ( 0.000000000000000000, 0.000000000000000000, 1.000000000000000000 ) ) ;
#60242=ORIENTED_EDGE ( 'NONE', *, *, #18021, .F. ) ;
#60249=VECTOR ( 'NONE', #120354, 1000.000000000000114 ) ;
#60289=CLOSED_SHELL ( 'NONE', ( #136780, #40747, #44563, #86884, #767, #110031, #3830, #69897, #63794, #74783, #135732, #123440, #13722, #120977, #84162, #80307, #92646, #10928, #43764, #123985, #107148, #23995, #35482, #35032, #23692, #103096, #11118, #135962, #132670, #16493, #99237, #26156, #77890, #51575, #109987, #52130, #39802, #62497, #73745, #43203, #37432, #66096, #29220, #94713, #105376, #59207, #1075, #74319, #107280, #134189, #136629, #108422, #20043, #88261, #73224, #77279, #26633, #128635, #89651, #59913, #27376, #18636, #117047, #56333, #57921, #128175, #141480, #12391, #36709, #77865, #71633, #94604, #81511, #11124, #117908, #79290, #79884, #35155, #10800, #29825, #17139, #101974, #33436, #6633, #127766, #107630, #75300, #74789, #107913, #34741, #116879, #36130, #74894, #129780, #10316, #129212, #88006, #3826, #61535, #143359, #113872, #49425, #105725, #134714, #102260, #91349, #67626, #34464, #91999, #124332, #91267, #129577, #101593, #71532, #13456, #14402, #110923, #48256, #46425, #100085, #77676, #67029, #125870, #101944, #135543, #64190, #76644, #91604, #56664, #25386, #130442, #142986, #80989, #104668, #12052, #142591, #35537, #142801, #118651, #29021, #61982, #112573, #126156, #77361, #102446, #123903, #76442, #90111, #4424, #125631, #132211, #52359, #137284, #109567, #45854, #24957, #44886, #127588, #112775, #11739, #59644, #85193, #105087, #54828, #96266, #32266, #57131, #60681, #69390, #45985, #110576, #88214, #110985, #120420, #114234, #59096, #44482, #21504, #23168, #79961, #14520, #21146, #56989, #37185, #133824, #120266, #137992, #100440, #33561, #22863, #37800, #81283, #125952, #135135, #76583 ) ) ;
#60297=CARTESIAN_POINT ( 'NONE',  ( 14.27159235450332098, 9.902892378096218942E-16, 0.000000000000000000 ) ) ;
#60331=DIRECTION ( 'NONE',  ( -1.000000000000000000, -1.224606353822377258E-16, -0.000000000000000000 ) ) ;
#60358=EDGE_CURVE ( 'NONE', #51588, #129879, #129746, .T. ) ;
#60406=EDGE_CURVE ( 'NONE', #110693, #3604, #88269, .T. ) ;
#60446=EDGE_CURVE ( 'NONE', #36066, #119351, #127580, .T. ) ;
#60450=CIRCLE ( 'NONE', #69765, 2.055000000000001048 ) ;
#60465=DIRECTION ( 'NONE',  ( -0.5735764363510507113, 0.8191520442889885789, 1.003171929053520926E-16 ) ) ;
#60477=DIRECTION ( 'NONE',  ( -1.000000000000000000, -1.224606353822377258E-16, -0.000000000000000000 ) ) ;
#60483=EDGE_CURVE ( 'NONE', #78861, #137915, #66174, .T. ) ;
#60576=PRODUCT_CONTEXT ( 'NONE', #121683, 'mechanical' ) ;
#60624=CARTESIAN_POINT ( 'NONE',  ( 24.87999999999999901, 9.521314400968980422E-16, 0.000000000000000000 ) ) ;
#60643=EDGE_CURVE ( 'NONE', #87975, #129879, #8690, .T. ) ;
#60653=CARTESIAN_POINT ( 'NONE',  ( 1.500000000000000000, 0.000000000000000000, 3.113037248396092416 ) ) ;
#60661=DIRECTION ( 'NONE',  ( -1.000000000000000000, -1.224606353822377258E-16, -0.000000000000000000 ) ) ;
#60681=ADVANCED_FACE ( 'NONE', ( #107340 ), #48851, .T. ) ;
#60709=ORIENTED_EDGE ( 'NONE', *, *, #15992, .T. ) ;
#60805=AXIS2_PLACEMENT_3D ( 'NONE', #125421, #34301, #78524 ) ;
#60827=CIRCLE ( 'NONE', #23842, 2.500000000000000888 ) ;
#60828=DIRECTION ( 'NONE',  ( 0.9961946980917455452, 1.067350013832299517E-17, 0.08715574274765836016 ) ) ;
#60850=DIRECTION ( 'NONE',  ( -1.000000000000000000, -1.224606353822377258E-16, -0.000000000000000000 ) ) ;
#60854=VERTEX_POINT ( 'NONE', #76157 ) ;
#60896=ORIENTED_EDGE ( 'NONE', *, *, #86854, .T. ) ;
#60932=DIRECTION ( 'NONE',  ( -1.000000000000000000, -1.224606353822377258E-16, -0.000000000000000000 ) ) ;
#60951=ORIENTED_EDGE ( 'NONE', *, *, #7319, .T. ) ;
#60968=DIRECTION ( 'NONE',  ( 0.000000000000000000, -1.000000000000000000, 0.000000000000000000 ) ) ;
#61033=CARTESIAN_POINT ( 'NONE',  ( 19.73159235450332005, 9.902892378096218942E-16, 0.000000000000000000 ) ) ;
#61035=EDGE_CURVE ( 'NONE', #112837, #71117, #21194, .T. ) ;
#61060=VERTEX_POINT ( 'NONE', #47155 ) ;
#61086=AXIS2_PLACEMENT_3D ( 'NONE', #128001, #28685, #72928 ) ;
#61114=CIRCLE ( 'NONE', #70416, 2.500000000000000888 ) ;
#61124=EDGE_CURVE ( 'NONE', #104583, #137915, #85983, .T. ) ;
#61179=ORIENTED_EDGE ( 'NONE', *, *, #121238, .F. ) ;
#61182=DIRECTION ( 'NONE',  ( 0.000000000000000000, -1.000000000000000000, 0.000000000000000000 ) ) ;
#61189=LINE ( 'NONE', #59731, #92763 ) ;
#61244=VERTEX_POINT ( 'NONE', #89019 ) ;
#61280=AXIS2_PLACEMENT_3D ( 'NONE', #56238, #101107, #87401 ) ;
#61350=ORIENTED_EDGE ( 'NONE', *, *, #20847, .F. ) ;
#61356=DIRECTION ( 'NONE',  ( -1.000000000000000000, -0.000000000000000000, -0.000000000000000000 ) ) ;
#61376=CARTESIAN_POINT ( 'NONE',  ( -25.39999999999996305, 0.000000000000000000, 2.500000000000000000 ) ) ;
#61377=CARTESIAN_POINT ( 'NONE',  ( 15.83159235450332147, 9.902892378096218942E-16, 0.000000000000000000 ) ) ;
#61398=VERTEX_POINT ( 'NONE', #93275 ) ;
#61407=CONICAL_SURFACE ( 'NONE', #130821, 2.500000000000000888, 0.9599310885968822538 ) ;
#61427=FACE_OUTER_BOUND ( 'NONE', #115657, .T. ) ;
#61431=LINE ( 'NONE', #52632, #33617 ) ;
#61459=DIRECTION ( 'NONE',  ( -1.000000000000000000, -1.224606353822377258E-16, -0.000000000000000000 ) ) ;
#61508=ORIENTED_EDGE ( 'NONE', *, *, #72371, .F. ) ;
#61509=EDGE_LOOP ( 'NONE', ( #87136, #33810, #50773, #8236, #61508 ) ) ;
#61515=CARTESIAN_POINT ( 'NONE',  ( 27.22000000000000242, 9.521314400968980422E-16, 0.000000000000000000 ) ) ;
#61535=ADVANCED_FACE ( 'NONE', ( #112543, #87929 ), #135048, .F. ) ;
#61552=ORIENTED_EDGE ( 'NONE', *, *, #120529, .T. ) ;
#61598=AXIS2_PLACEMENT_3D ( 'NONE', #110206, #11593, #110910 ) ;
#61639=DIRECTION ( 'NONE',  ( 0.000000000000000000, -1.000000000000000000, 0.000000000000000000 ) ) ;
#61652=ORIENTED_EDGE ( 'NONE', *, *, #28139, .T. ) ;
#61655=AXIS2_PLACEMENT_3D ( 'NONE', #3437, #47728, #91223 ) ;
#61657=DIRECTION ( 'NONE',  ( -1.000000000000000000, -0.000000000000000000, -0.000000000000000000 ) ) ;
#61669=ORIENTED_EDGE ( 'NONE', *, *, #90091, .T. ) ;
#61675=ORIENTED_EDGE ( 'NONE', *, *, #128694, .F. ) ;
#61706=VERTEX_POINT ( 'NONE', #47349 ) ;
#61722=DIRECTION ( 'NONE',  ( -1.000000000000000000, -0.000000000000000000, -0.000000000000000000 ) ) ;
#61742=DIRECTION ( 'NONE',  ( 0.000000000000000000, 1.000000000000000000, 0.000000000000000000 ) ) ;
#61745=DIRECTION ( 'NONE',  ( 0.000000000000000000, 0.000000000000000000, -1.000000000000000000 ) ) ;
#61765=DIRECTION ( 'NONE',  ( -0.5735764363510503783, -0.8191520442889886899, 0.000000000000000000 ) ) ;
#61786=CARTESIAN_POINT ( 'NONE',  ( -25.39999999999996305, 0.000000000000000000, 0.000000000000000000 ) ) ;
#61789=AXIS2_PLACEMENT_3D ( 'NONE', #119121, #77779, #19802 ) ;
#61857=EDGE_CURVE ( 'NONE', #110059, #107725, #118461, .T. ) ;
#61867=EDGE_CURVE ( 'NONE', #80457, #73777, #139327, .T. ) ;
#61889=AXIS2_PLACEMENT_3D ( 'NONE', #124142, #81389, #24827 ) ;
#61892=DIRECTION ( 'NONE',  ( 1.000000000000000000, 0.000000000000000000, 0.000000000000000000 ) ) ;
#61931=DIRECTION ( 'NONE',  ( 0.000000000000000000, -1.000000000000000000, 0.000000000000000000 ) ) ;
#61953=CARTESIAN_POINT ( 'NONE',  ( 20.19999999999999929, 2.055000000000001492, 2.516649172247811554E-16 ) ) ;
#61955=DIRECTION ( 'NONE',  ( -1.000000000000000000, -1.224606353822377258E-16, -0.000000000000000000 ) ) ;
#61963=VECTOR ( 'NONE', #11041, 1000.000000000000000 ) ;
#61982=ADVANCED_FACE ( 'NONE', ( #85605 ), #134860, .T. ) ;
#61986=CONICAL_SURFACE ( 'NONE', #117506, 2.055000000000001048, 0.9599310885968758145 ) ;
#61987=VECTOR ( 'NONE', #87817, 1000.000000000000000 ) ;
#61988=AXIS2_PLACEMENT_3D ( 'NONE', #58211, #12496, #56778 ) ;
#62036=EDGE_CURVE ( 'NONE', #135574, #111361, #9805, .T. ) ;
#62044=EDGE_CURVE ( 'NONE', #109094, #118163, #44636, .T. ) ;
#62094=CARTESIAN_POINT ( 'NONE',  ( 19.41999999999999815, 2.055000000000001492, 0.000000000000000000 ) ) ;
#62113=ORIENTED_EDGE ( 'NONE', *, *, #3822, .F. ) ;
#62127=ORIENTED_EDGE ( 'NONE', *, *, #91107, .F. ) ;
#62147=EDGE_CURVE ( 'NONE', #57540, #131273, #123261, .T. ) ;
#62150=( NAMED_UNIT ( * ) SI_UNIT ( $, .STERADIAN. ) SOLID_ANGLE_UNIT ( ) );
#62167=LINE ( 'NONE', #106330, #137097 ) ;
#62185=CARTESIAN_POINT ( 'NONE',  ( 23.00840764549667483, 9.139736423841732040E-16, 0.000000000000000000 ) ) ;
#62198=B_SPLINE_CURVE_WITH_KNOTS ( 'NONE', 3,
 ( #132734, #9450, #52971, #141433, #108760, #31258, #20340, #66041, #142859, #54452 ),
 .UNSPECIFIED., .F., .F.,
 ( 4, 2, 2, 2, 4 ),
 ( 0.008920163802561175553, 0.009434751658411365260, 0.009949339514261554968, 0.01046392737011174294, 0.01097851522596193265 ),
 .UNSPECIFIED. ) ;
#62200=EDGE_CURVE ( 'NONE', #97682, #136003, #123978, .T. ) ;
#62210=DIRECTION ( 'NONE',  ( -1.000000000000000000, -1.224606353822377258E-16, -0.000000000000000000 ) ) ;
#62270=CARTESIAN_POINT ( 'NONE',  ( 8.188407645496676324, 9.139736423841732040E-16, 0.000000000000000000 ) ) ;
#62309=CIRCLE ( 'NONE', #25227, 2.500000000000000888 ) ;
#62353=DIRECTION ( 'NONE',  ( 0.5735764363510451602, 0.8191520442889924647, 0.000000000000000000 ) ) ;
#62354=ORIENTED_EDGE ( 'NONE', *, *, #86231, .T. ) ;
#62372=ORIENTED_EDGE ( 'NONE', *, *, #39163, .F. ) ;
#62384=DIRECTION ( 'NONE',  ( 0.000000000000000000, -1.000000000000000000, 0.000000000000000000 ) ) ;
#62387=EDGE_CURVE ( 'NONE', #91753, #113725, #121045, .T. ) ;
#62397=ORIENTED_EDGE ( 'NONE', *, *, #25611, .F. ) ;
#62407=CONICAL_SURFACE ( 'NONE', #27602, 2.055000000000001048, 0.9599310885968758145 ) ;
#62415=ORIENTED_EDGE ( 'NONE', *, *, #103346, .T. ) ;
#62454=ORIENTED_EDGE ( 'NONE', *, *, #107315, .F. ) ;
#62489=FACE_OUTER_BOUND ( 'NONE', #122133, .T. ) ;
#62497=ADVANCED_FACE ( 'NONE', ( #59286 ), #68718, .T. ) ;
#62537=DIRECTION ( 'NONE',  ( 0.5735764363510453823, -0.8191520442889923537, 1.003171929053525486E-16 ) ) ;
#62572=FACE_OUTER_BOUND ( 'NONE', #116010, .T. ) ;
#62600=CARTESIAN_POINT ( 'NONE',  ( 5.691592354503320905, 9.902892378096218942E-16, 0.000000000000000000 ) ) ;
#62680=CARTESIAN_POINT ( 'NONE',  ( 0.4436723136282649804, 0.5999999999999987566, 4.148801034132802990 ) ) ;
#62721=AXIS2_PLACEMENT_3D ( 'NONE', #108737, #140002, #83466 ) ;
#62750=ORIENTED_EDGE ( 'NONE', *, *, #125600, .T. ) ;
#62796=CIRCLE ( 'NONE', #127665, 2.500000000000000888 ) ;
#62811=DIRECTION ( 'NONE',  ( -1.000000000000000000, -0.000000000000000000, -0.000000000000000000 ) ) ;
#62832=DIRECTION ( 'NONE',  ( -0.5735764363510507113, 0.8191520442889885789, 1.003171929053520926E-16 ) ) ;
#62839=DIRECTION ( 'NONE',  ( 0.000000000000000000, -1.000000000000000000, 0.000000000000000000 ) ) ;
#62841=VERTEX_POINT ( 'NONE', #101140 ) ;
#62850=ORIENTED_EDGE ( 'NONE', *, *, #21271, .F. ) ;
#62887=DIRECTION ( 'NONE',  ( -0.5735764363510503783, -0.8191520442889886899, 0.000000000000000000 ) ) ;
#62891=AXIS2_PLACEMENT_3D ( 'NONE', #113224, #24098, #88653 ) ;
#62937=AXIS2_PLACEMENT_3D ( 'NONE', #27911, #137401, #38096 ) ;
#63077=CARTESIAN_POINT ( 'NONE',  ( 23.63159235450331863, 2.500000000000001776, 0.000000000000000000 ) ) ;
#63089=CONICAL_SURFACE ( 'NONE', #120893, 2.055000000000001048, 0.9599310885968758145 ) ;
#63091=CONICAL_SURFACE ( 'NONE', #65374, 2.500000000000000888, 0.9599310885968822538 ) ;
#63105=CARTESIAN_POINT ( 'NONE',  ( 11.15159235450332176, 9.902892378096218942E-16, 0.000000000000000000 ) ) ;
#63115=DIRECTION ( 'NONE',  ( -1.000000000000000000, -1.224606353822377258E-16, -0.000000000000000000 ) ) ;
#63124=CARTESIAN_POINT ( 'NONE',  ( 22.07159235450331991, 9.902892378096218942E-16, 0.000000000000000000 ) ) ;
#63154=CARTESIAN_POINT ( 'NONE',  ( 12.71159235450332048, 9.902892378096218942E-16, 0.000000000000000000 ) ) ;
#63194=VECTOR ( 'NONE', #130396, 1000.000000000000000 ) ;
#63208=DIRECTION ( 'NONE',  ( 0.000000000000000000, -1.000000000000000000, 0.000000000000000000 ) ) ;
#63213=CONICAL_SURFACE ( 'NONE', #33103, 2.055000000000001048, 0.9599310885968758145 ) ;
#63222=CARTESIAN_POINT ( 'NONE',  ( 17.54840764549667398, 3.061616997868385113E-16, -2.500000000000001332 ) ) ;
#63237=EDGE_LOOP ( 'NONE', ( #21640, #30018, #73786, #15154, #29723 ) ) ;
#63254=EDGE_CURVE ( 'NONE', #35625, #30995, #43948, .T. ) ;
#63270=AXIS2_PLACEMENT_3D ( 'NONE', #57516, #943, #103135 ) ;
#63293=VECTOR ( 'NONE', #99893, 1000.000000000000000 ) ;
#63368=CONICAL_SURFACE ( 'NONE', #5350, 2.500000000000000888, 0.9599310885968822538 ) ;
#63373=DIRECTION ( 'NONE',  ( 0.000000000000000000, -1.000000000000000000, 0.000000000000000000 ) ) ;
#63382=CARTESIAN_POINT ( 'NONE',  ( 4.911592354503321545, 9.902892378096218942E-16, 0.000000000000000000 ) ) ;
#63386=DIRECTION ( 'NONE',  ( -1.000000000000000000, -1.224606353822377258E-16, -0.000000000000000000 ) ) ;
#63420=CARTESIAN_POINT ( 'NONE',  ( 0.1429064800270019031, 0.5999999999999986455, 3.726828488909569081 ) ) ;
#63448=ORIENTED_EDGE ( 'NONE', *, *, #31909, .F. ) ;
#63450=ORIENTED_EDGE ( 'NONE', *, *, #120717, .F. ) ;
#63460=EDGE_LOOP ( 'NONE', ( #573, #54322, #96042, #61179, #90686, #77563 ) ) ;
#63490=VERTEX_POINT ( 'NONE', #55253 ) ;
#63554=DIRECTION ( 'NONE',  ( -1.000000000000000000, -1.224606353822377258E-16, -0.000000000000000000 ) ) ;
#63591=EDGE_CURVE ( 'NONE', #111361, #130559, #108672, .T. ) ;
#63604=AXIS2_PLACEMENT_3D ( 'NONE', #52171, #49361, #18819 ) ;
#63627=LINE ( 'NONE', #19373, #58194 ) ;
#63648=CARTESIAN_POINT ( 'NONE',  ( 24.56840764549667355, 9.139736423841732040E-16, 0.000000000000000000 ) ) ;
#63666=CARTESIAN_POINT ( 'NONE',  ( -25.39999999999996305, 0.000000000000000000, 0.000000000000000000 ) ) ;
#63734=EDGE_CURVE ( 'NONE', #29768, #119001, #141191, .T. ) ;
#63735=FACE_OUTER_BOUND ( 'NONE', #47589, .T. ) ;
#63750=AXIS2_PLACEMENT_3D ( 'NONE', #118778, #2704, #113613 ) ;
#63751=CARTESIAN_POINT ( 'NONE',  ( 12.71159235450332048, -5.777789833161707559E-31, 2.500000000000001332 ) ) ;
#63756=LINE ( 'NONE', #97029, #129010 ) ;
#63777=CARTESIAN_POINT ( 'NONE',  ( 9.748407645496676821, 2.500000000000000888, 3.061616997868383141E-16 ) ) ;
#63794=ADVANCED_FACE ( 'NONE', ( #74712 ), #104129, .T. ) ;
#63798=ORIENTED_EDGE ( 'NONE', *, *, #74692, .F. ) ;
#63833=CARTESIAN_POINT ( 'NONE',  ( 5.380000000000000782, 9.521314400968980422E-16, 0.000000000000000000 ) ) ;
#63851=CIRCLE ( 'NONE', #121758, 2.500000000000000888 ) ;
#63867=CARTESIAN_POINT ( 'NONE',  ( 25.97159235450331849, 9.902892378096218942E-16, 0.000000000000000000 ) ) ;
#63868=ORIENTED_EDGE ( 'NONE', *, *, #39113, .T. ) ;
#63881=CARTESIAN_POINT ( 'NONE',  ( 9.591592354503321260, 9.902892378096218942E-16, 0.000000000000000000 ) ) ;
#63925=CARTESIAN_POINT ( 'NONE',  ( 23.32000000000000028, 9.521314400968980422E-16, 0.000000000000000000 ) ) ;
#63942=DIRECTION ( 'NONE',  ( 0.000000000000000000, -1.000000000000000000, 0.000000000000000000 ) ) ;
#63956=AXIS2_PLACEMENT_3D ( 'NONE', #63867, #128401, #8011 ) ;
#63969=ORIENTED_EDGE ( 'NONE', *, *, #28694, .F. ) ;
#63995=FACE_OUTER_BOUND ( 'NONE', #1781, .T. ) ;
#64014=LINE ( 'NONE', #29227, #9747 ) ;
#64043=FACE_OUTER_BOUND ( 'NONE', #2919, .T. ) ;
#64065=DIRECTION ( 'NONE',  ( 0.000000000000000000, -1.000000000000000000, 0.000000000000000000 ) ) ;
#64098=VECTOR ( 'NONE', #77509, 1000.000000000000000 ) ;
#64109=VERTEX_POINT ( 'NONE', #49925 ) ;
#64144=LINE ( 'NONE', #106912, #110707 ) ;
#64177=ORIENTED_EDGE ( 'NONE', *, *, #55093, .F. ) ;
#64186=DIRECTION ( 'NONE',  ( 0.000000000000000000, -1.000000000000000000, 0.000000000000000000 ) ) ;
#64190=ADVANCED_FACE ( 'NONE', ( #107123 ), #74268, .T. ) ;
#64193=AXIS2_PLACEMENT_3D ( 'NONE', #41069, #10557, #96835 ) ;
#64203=AXIS2_PLACEMENT_3D ( 'NONE', #111460, #33241, #77448 ) ;
#64225=CARTESIAN_POINT ( 'NONE',  ( 8.500000000000000000, 2.055000000000001492, 2.516649172247811554E-16 ) ) ;
#64229=CARTESIAN_POINT ( 'NONE',  ( -25.39999999999996305, 0.000000000000000000, 0.000000000000000000 ) ) ;
#64230=ORIENTED_EDGE ( 'NONE', *, *, #34657, .F. ) ;
#64235=CARTESIAN_POINT ( 'NONE',  ( 17.54840764549667398, 9.139736423841732040E-16, 0.000000000000000000 ) ) ;
#64257=DIRECTION ( 'NONE',  ( 0.000000000000000000, -1.000000000000000000, 0.000000000000000000 ) ) ;
#64258=DIRECTION ( 'NONE',  ( 1.000000000000000000, 1.224606353822377258E-16, 0.000000000000000000 ) ) ;
#64283=VERTEX_POINT ( 'NONE', #75941 ) ;
#64292=VERTEX_POINT ( 'NONE', #119411 ) ;
#64296=CARTESIAN_POINT ( 'NONE',  ( 16.61159235450331906, -2.500000000000000444, 3.061616997868384620E-16 ) ) ;
#64306=ORIENTED_EDGE ( 'NONE', *, *, #53646, .F. ) ;
#64309=ORIENTED_EDGE ( 'NONE', *, *, #8897, .F. ) ;
#64337=CIRCLE ( 'NONE', #8707, 4.750000000000000000 ) ;
#64364=CARTESIAN_POINT ( 'NONE',  ( 1.199999999999999956, 0.000000000000000000, 0.000000000000000000 ) ) ;
#64371=CARTESIAN_POINT ( 'NONE',  ( 17.54840764549667398, 2.500000000000003553, 3.061616997868386099E-16 ) ) ;
#64372=ORIENTED_EDGE ( 'NONE', *, *, #85086, .F. ) ;
#64382=DIRECTION ( 'NONE',  ( 0.000000000000000000, -1.000000000000000000, 0.000000000000000000 ) ) ;
#64393=EDGE_CURVE ( 'NONE', #81745, #35625, #122784, .T. ) ;
#64425=CARTESIAN_POINT ( 'NONE',  ( 0.000000000000000000, 0.5999999999999987566, -3.054668707061621191 ) ) ;
#64435=DIRECTION ( 'NONE',  ( 0.000000000000000000, 0.000000000000000000, 1.000000000000000000 ) ) ;
#64442=EDGE_CURVE ( 'NONE', #36267, #124621, #132122, .T. ) ;
#64468=FACE_OUTER_BOUND ( 'NONE', #10174, .T. ) ;
#64499=DIRECTION ( 'NONE',  ( -1.000000000000000000, -1.224606353822377258E-16, -0.000000000000000000 ) ) ;
#64517=VERTEX_POINT ( 'NONE', #105522 ) ;
#64520=DIRECTION ( 'NONE',  ( -1.000000000000000000, -1.224606353822377258E-16, -0.000000000000000000 ) ) ;
#64553=DIRECTION ( 'NONE',  ( 0.000000000000000000, -1.000000000000000000, 0.000000000000000000 ) ) ;
#64559=ORIENTED_EDGE ( 'NONE', *, *, #14480, .F. ) ;
#64584=CARTESIAN_POINT ( 'NONE',  ( 22.53999999999999915, 9.521314400968980422E-16, 0.000000000000000000 ) ) ;
#64587=AXIS2_PLACEMENT_3D ( 'NONE', #46338, #134768, #47078 ) ;
#64595=CARTESIAN_POINT ( 'NONE',  ( 19.73159235450332005, 9.902892378096218942E-16, 0.000000000000000000 ) ) ;
#64632=AXIS2_PLACEMENT_3D ( 'NONE', #25770, #136669, #135966 ) ;
#64673=CONICAL_SURFACE ( 'NONE', #71609, 2.055000000000001048, 0.9599310885968758145 ) ;
#64694=ORIENTED_EDGE ( 'NONE', *, *, #91498, .T. ) ;
#64712=ORIENTED_EDGE ( 'NONE', *, *, #90091, .F. ) ;
#64743=VECTOR ( 'NONE', #100330, 1000.000000000000000 ) ;
#64750=EDGE_LOOP ( 'NONE', ( #105488, #105506, #112514, #25729, #17249 ) ) ;
#64752=FACE_OUTER_BOUND ( 'NONE', #61509, .T. ) ;
#64789=ORIENTED_EDGE ( 'NONE', *, *, #20213, .T. ) ;
#64807=DIRECTION ( 'NONE',  ( 0.000000000000000000, 1.000000000000000000, 0.000000000000000000 ) ) ;
#64808=CARTESIAN_POINT ( 'NONE',  ( 10.52840764549667618, 2.500000000000000888, 3.061616997868383141E-16 ) ) ;
#64817=DIRECTION ( 'NONE',  ( 0.5735764363510451602, 0.8191520442889924647, 0.000000000000000000 ) ) ;
#64827=DIRECTION ( 'NONE',  ( -1.000000000000000000, -1.224606353822377258E-16, -0.000000000000000000 ) ) ;
#64832=VERTEX_POINT ( 'NONE', #103735 ) ;
#64847=CARTESIAN_POINT ( 'NONE',  ( 20.19999999999999929, 9.521314400968980422E-16, 0.000000000000000000 ) ) ;
#64852=CONICAL_SURFACE ( 'NONE', #18545, 2.500000000000000888, 0.9599310885968822538 ) ;
#64880=CARTESIAN_POINT ( 'NONE',  ( 5.691592354503320905, -2.500000000000000000, 3.061616997868384127E-16 ) ) ;
#64947=EDGE_CURVE ( 'NONE', #41180, #78032, #132235, .T. ) ;
#64960=VECTOR ( 'NONE', #136459, 1000.000000000000000 ) ;
#64963=DIRECTION ( 'NONE',  ( 0.000000000000000000, -1.000000000000000000, 0.000000000000000000 ) ) ;
#64968=CARTESIAN_POINT ( 'NONE',  ( 8.500000000000000000, 9.521314400968980422E-16, 0.000000000000000000 ) ) ;
#64995=VERTEX_POINT ( 'NONE', #120309 ) ;
#65024=FACE_OUTER_BOUND ( 'NONE', #142707, .T. ) ;
#65039=CIRCLE ( 'NONE', #127523, 2.500000000000000888 ) ;
#65048=DIRECTION ( 'NONE',  ( -0.5735764363510503783, -0.8191520442889886899, 0.000000000000000000 ) ) ;
#65051=AXIS2_PLACEMENT_3D ( 'NONE', #86981, #107297, #131203 ) ;
#65065=CONICAL_SURFACE ( 'NONE', #32672, 2.055000000000001048, 0.9599310885968758145 ) ;
#65096=AXIS2_PLACEMENT_3D ( 'NONE', #39902, #105808, #74663 ) ;
#65119=DIRECTION ( 'NONE',  ( -1.000000000000000000, -0.000000000000000000, -0.000000000000000000 ) ) ;
#65155=CARTESIAN_POINT ( 'NONE',  ( 22.85159235450332105, 9.902892378096218942E-16, 0.000000000000000000 ) ) ;
#65157=EDGE_LOOP ( 'NONE', ( #134172, #116271, #125098, #90159, #137998 ) ) ;
#65218=ORIENTED_EDGE ( 'NONE', *, *, #53646, .T. ) ;
#65234=DIRECTION ( 'NONE',  ( 0.000000000000000000, -1.000000000000000000, 0.000000000000000000 ) ) ;
#65272=DIRECTION ( 'NONE',  ( 0.000000000000000000, -1.000000000000000000, 0.000000000000000000 ) ) ;
#65279=AXIS2_PLACEMENT_3D ( 'NONE', #119327, #75168, #96841 ) ;
#65359=ORIENTED_EDGE ( 'NONE', *, *, #18454, .F. ) ;
#65374=AXIS2_PLACEMENT_3D ( 'NONE', #36276, #89228, #122545 ) ;
#65380=AXIS2_PLACEMENT_3D ( 'NONE', #122706, #103110, #12513 ) ;
#65391=ORIENTED_EDGE ( 'NONE', *, *, #59709, .T. ) ;
#65401=DIRECTION ( 'NONE',  ( 0.000000000000000000, -1.000000000000000000, 0.000000000000000000 ) ) ;
#65408=LINE ( 'NONE', #99397, #87621 ) ;
#65426=CARTESIAN_POINT ( 'NONE',  ( 13.64840764549667540, 9.139736423841732040E-16, 0.000000000000000000 ) ) ;
#65545=CONICAL_SURFACE ( 'NONE', #88703, 2.500000000000000888, 0.9599310885968822538 ) ;
#65550=DIRECTION ( 'NONE',  ( -1.000000000000000000, -1.224606353822377258E-16, -0.000000000000000000 ) ) ;
#65650=LINE ( 'NONE', #109816, #65944 ) ;
#65687=VERTEX_POINT ( 'NONE', #30138 ) ;
#65720=CIRCLE ( 'NONE', #56405, 2.500000000000000888 ) ;
#65727=ORIENTED_EDGE ( 'NONE', *, *, #123549, .T. ) ;
#65735=DIRECTION ( 'NONE',  ( -1.000000000000000000, -1.224606353822377258E-16, -0.000000000000000000 ) ) ;
#65738=AXIS2_PLACEMENT_3D ( 'NONE', #26197, #115287, #50096 ) ;
#65817=LINE ( 'NONE', #109979, #118411 ) ;
#65821=VERTEX_POINT ( 'NONE', #41745 ) ;
#65833=ORIENTED_EDGE ( 'NONE', *, *, #76400, .T. ) ;
#65886=ORIENTED_EDGE ( 'NONE', *, *, #31045, .T. ) ;
#65893=LINE ( 'NONE', #53557, #104455 ) ;
#65939=EDGE_CURVE ( 'NONE', #114073, #29586, #141846, .T. ) ;
#65944=VECTOR ( 'NONE', #143153, 1000.000000000000000 ) ;
#65959=VERTEX_POINT ( 'NONE', #91663 ) ;
#65962=LINE ( 'NONE', #23856, #28675 ) ;
#65969=DIRECTION ( 'NONE',  ( -1.000000000000000000, -1.224606353822377258E-16, -0.000000000000000000 ) ) ;
#66002=DIRECTION ( 'NONE',  ( 0.000000000000000000, 1.000000000000000000, 0.000000000000000000 ) ) ;
#66031=DIRECTION ( 'NONE',  ( 0.000000000000000000, 0.000000000000000000, 1.000000000000000000 ) ) ;
#66041=CARTESIAN_POINT ( 'NONE',  ( 0.02857727139928691387, -0.5999999999999994227, -3.398545894033870418 ) ) ;
#66043=AXIS2_PLACEMENT_3D ( 'NONE', #76183, #10187, #21062 ) ;
#66078=CARTESIAN_POINT ( 'NONE',  ( 12.86840764549667604, 2.500000000000003553, 3.061616997868386099E-16 ) ) ;
#66096=ADVANCED_FACE ( 'NONE', ( #64752 ), #90836, .T. ) ;
#66174=LINE ( 'NONE', #76327, #51230 ) ;
#66197=DIRECTION ( 'NONE',  ( -1.000000000000000000, -0.000000000000000000, -0.000000000000000000 ) ) ;
#66238=CONICAL_SURFACE ( 'NONE', #61598, 2.500000000000000888, 0.9599310885968822538 ) ;
#66279=DIRECTION ( 'NONE',  ( 0.000000000000000000, -1.000000000000000000, 0.000000000000000000 ) ) ;
#66300=EDGE_LOOP ( 'NONE', ( #125586, #22228, #118021, #29031, #37971 ) ) ;
#66301=VECTOR ( 'NONE', #36801, 1000.000000000000000 ) ;
#66314=FACE_OUTER_BOUND ( 'NONE', #25299, .T. ) ;
#66319=CARTESIAN_POINT ( 'NONE',  ( 1.199999999999999956, 0.000000000000000000, 4.582731094065999322 ) ) ;
#66359=DIRECTION ( 'NONE',  ( -1.000000000000000000, -0.000000000000000000, -0.000000000000000000 ) ) ;
#66362=ORIENTED_EDGE ( 'NONE', *, *, #95376, .F. ) ;
#66386=ORIENTED_EDGE ( 'NONE', *, *, #81553, .T. ) ;
#66389=DIRECTION ( 'NONE',  ( -1.000000000000000000, -1.224606353822377258E-16, -0.000000000000000000 ) ) ;
#66416=CARTESIAN_POINT ( 'NONE',  ( 9.591592354503321260, 3.061616997868378211E-16, -2.500000000000001332 ) ) ;
#66431=AXIS2_PLACEMENT_3D ( 'NONE', #88169, #132419, #85279 ) ;
#66513=ORIENTED_EDGE ( 'NONE', *, *, #42517, .T. ) ;
#66528=AXIS2_PLACEMENT_3D ( 'NONE', #56109, #77147, #32927 ) ;
#66530=DIRECTION ( 'NONE',  ( -1.000000000000000000, -1.224606353822377258E-16, -0.000000000000000000 ) ) ;
#66580=ORIENTED_EDGE ( 'NONE', *, *, #2889, .F. ) ;
#66581=DIRECTION ( 'NONE',  ( -0.5735764363510503783, -0.8191520442889886899, 0.000000000000000000 ) ) ;
#66685=ORIENTED_EDGE ( 'NONE', *, *, #6709, .F. ) ;
#66712=ORIENTED_EDGE ( 'NONE', *, *, #91486, .F. ) ;
#66724=EDGE_LOOP ( 'NONE', ( #46854, #136068, #62372, #9015, #10601 ) ) ;
#66743=ORIENTED_EDGE ( 'NONE', *, *, #15385, .T. ) ;
#66744=EDGE_CURVE ( 'NONE', #32976, #79589, #114087, .T. ) ;
#66748=DIRECTION ( 'NONE',  ( 1.000000000000000000, 1.224606353822377258E-16, 0.000000000000000000 ) ) ;
#66799=EDGE_CURVE ( 'NONE', #75381, #3378, #95550, .T. ) ;
#66878=CARTESIAN_POINT ( 'NONE',  ( 14.42840764549667476, 9.139736423841732040E-16, 0.000000000000000000 ) ) ;
#66914=FACE_OUTER_BOUND ( 'NONE', #50242, .T. ) ;
#66938=ORIENTED_EDGE ( 'NONE', *, *, #135385, .F. ) ;
#66958=VECTOR ( 'NONE', #40211, 1000.000000000000000 ) ;
#66981=AXIS2_PLACEMENT_3D ( 'NONE', #37251, #4548, #127096 ) ;
#66991=ORIENTED_EDGE ( 'NONE', *, *, #130833, .F. ) ;
#66999=ORIENTED_EDGE ( 'NONE', *, *, #126855, .F. ) ;
#67029=ADVANCED_FACE ( 'NONE', ( #137267 ), #37844, .T. ) ;
#67060=FACE_OUTER_BOUND ( 'NONE', #75656, .T. ) ;
#67087=CIRCLE ( 'NONE', #134241, 2.500000000000000888 ) ;
#67110=ORIENTED_EDGE ( 'NONE', *, *, #100842, .T. ) ;
#67135=FACE_OUTER_BOUND ( 'NONE', #86547, .T. ) ;
#67159=AXIS2_PLACEMENT_3D ( 'NONE', #110196, #32678, #10867 ) ;
#67170=AXIS2_PLACEMENT_3D ( 'NONE', #71988, #114027, #69121 ) ;
#67188=ORIENTED_EDGE ( 'NONE', *, *, #32522, .F. ) ;
#67208=PLANE ( 'NONE',  #130698 ) ;
#67309=CARTESIAN_POINT ( 'NONE',  ( -25.39999999999996305, 3.061616997868383141E-16, -2.500000000000000000 ) ) ;
#67337=CIRCLE ( 'NONE', #41871, 2.055000000000001048 ) ;
#67371=AXIS2_PLACEMENT_3D ( 'NONE', #42753, #112279, #86949 ) ;
#67452=EDGE_LOOP ( 'NONE', ( #129826, #127408, #113617, #59100, #14006 ) ) ;
#67465=DIRECTION ( 'NONE',  ( 0.000000000000000000, -1.000000000000000000, 0.000000000000000000 ) ) ;
#67476=DIRECTION ( 'NONE',  ( 0.000000000000000000, -1.000000000000000000, 0.000000000000000000 ) ) ;
#67485=CARTESIAN_POINT ( 'NONE',  ( 22.07159235450331991, 9.902892378096218942E-16, 0.000000000000000000 ) ) ;
#67486=FACE_OUTER_BOUND ( 'NONE', #80993, .T. ) ;
#67503=EDGE_CURVE ( 'NONE', #119351, #129380, #134900, .T. ) ;
#67507=DIRECTION ( 'NONE',  ( 0.000000000000000000, -1.000000000000000000, 0.000000000000000000 ) ) ;
#67543=CARTESIAN_POINT ( 'NONE',  ( 15.05159235450332034, 9.902892378096218942E-16, 0.000000000000000000 ) ) ;
#67571=VERTEX_POINT ( 'NONE', #112405 ) ;
#67590=VECTOR ( 'NONE', #20432, 1000.000000000000114 ) ;
#67626=ADVANCED_FACE ( 'NONE', ( #100102 ), #63091, .T. ) ;
#67657=AXIS2_PLACEMENT_3D ( 'NONE', #71329, #15464, #115486 ) ;
#67722=CIRCLE ( 'NONE', #139539, 2.055000000000001048 ) ;
#67735=ORIENTED_EDGE ( 'NONE', *, *, #131677, .T. ) ;
#67736=FACE_OUTER_BOUND ( 'NONE', #13468, .T. ) ;
#67777=CONICAL_SURFACE ( 'NONE', #65380, 2.500000000000000888, 0.9599310885968822538 ) ;
#67825=LINE ( 'NONE', #75815, #22581 ) ;
#67841=CARTESIAN_POINT ( 'NONE',  ( 18.95159235450331892, 3.061616997868380183E-16, -2.500000000000001332 ) ) ;
#67848=CARTESIAN_POINT ( 'NONE',  ( 11.15159235450332176, 9.902892378096218942E-16, 0.000000000000000000 ) ) ;
#67863=CARTESIAN_POINT ( 'NONE',  ( 13.18000000000000149, 9.521314400968980422E-16, 0.000000000000000000 ) ) ;
#67865=CARTESIAN_POINT ( 'NONE',  ( 15.83159235450332147, -3.851859888774471706E-31, 2.500000000000001332 ) ) ;
#68015=AXIS2_PLACEMENT_3D ( 'NONE', #80064, #1701, #56887 ) ;
#68035=LINE ( 'NONE', #91193, #101182 ) ;
#68074=EDGE_LOOP ( 'NONE', ( #27, #7513, #82122, #124091, #54906 ) ) ;
#68082=CARTESIAN_POINT ( 'NONE',  ( 12.71159235450332048, 9.902892378096218942E-16, 0.000000000000000000 ) ) ;
#68118=DIRECTION ( 'NONE',  ( 0.5735764363510453823, -0.8191520442889923537, 1.003171929053525486E-16 ) ) ;
#68197=CARTESIAN_POINT ( 'NONE',  ( -25.39999999999996305, 0.000000000000000000, 0.000000000000000000 ) ) ;
#68279=ORIENTED_EDGE ( 'NONE', *, *, #68435, .T. ) ;
#68294=AXIS2_PLACEMENT_3D ( 'NONE', #76739, #10018, #54282 ) ;
#68319=DIRECTION ( 'NONE',  ( 0.000000000000000000, 0.000000000000000000, 1.000000000000000000 ) ) ;
#68345=ORIENTED_EDGE ( 'NONE', *, *, #125134, .T. ) ;
#68353=FACE_OUTER_BOUND ( 'NONE', #116048, .T. ) ;
#68383=CARTESIAN_POINT ( 'NONE',  ( 16.30000000000000071, -2.055000000000000160, 2.789133085058098087E-16 ) ) ;
#68427=VECTOR ( 'NONE', #58029, 1000.000000000000000 ) ;
#68435=EDGE_CURVE ( 'NONE', #135110, #77074, #91562, .T. ) ;
#68446=LINE ( 'NONE', #90897, #64743 ) ;
#68482=DIRECTION ( 'NONE',  ( -1.000000000000000000, -1.224606353822377258E-16, -0.000000000000000000 ) ) ;
#68483=ORIENTED_EDGE ( 'NONE', *, *, #121521, .T. ) ;
#68485=VERTEX_POINT ( 'NONE', #39333 ) ;
#68529=AXIS2_PLACEMENT_3D ( 'NONE', #56129, #106148, #97426 ) ;
#68540=ORIENTED_EDGE ( 'NONE', *, *, #106738, .T. ) ;
#68556=ORIENTED_EDGE ( 'NONE', *, *, #90328, .T. ) ;
#68561=EDGE_CURVE ( 'NONE', #87397, #36671, #83062, .T. ) ;
#68614=AXIS2_PLACEMENT_3D ( 'NONE', #126310, #81414, #116141 ) ;
#68620=ORIENTED_EDGE ( 'NONE', *, *, #90738, .F. ) ;
#68624=ORIENTED_EDGE ( 'NONE', *, *, #59372, .F. ) ;
#68658=LINE ( 'NONE', #135347, #114906 ) ;
#68713=CARTESIAN_POINT ( 'NONE',  ( 18.95159235450331892, -3.851859888774471706E-31, 2.500000000000001332 ) ) ;
#68718=CYLINDRICAL_SURFACE ( 'NONE', #90968, 2.500000000000000000 ) ;
#68729=CARTESIAN_POINT ( 'NONE',  ( 15.83159235450332147, 3.061616997868380183E-16, -2.500000000000001332 ) ) ;
#68783=DIRECTION ( 'NONE',  ( 0.000000000000000000, -1.000000000000000000, 0.000000000000000000 ) ) ;
#68807=ORIENTED_EDGE ( 'NONE', *, *, #119367, .T. ) ;
#68822=AXIS2_PLACEMENT_3D ( 'NONE', #81368, #2309, #111077 ) ;
#68872=ORIENTED_EDGE ( 'NONE', *, *, #92157, .T. ) ;
#68896=ORIENTED_EDGE ( 'NONE', *, *, #58243, .F. ) ;
#68916=AXIS2_PLACEMENT_3D ( 'NONE', #110813, #118862, #65234 ) ;
#68961=CONICAL_SURFACE ( 'NONE', #73503, 2.055000000000001048, 0.9599310885968758145 ) ;
#69059=DIRECTION ( 'NONE',  ( -0.000000000000000000, 0.000000000000000000, 1.000000000000000000 ) ) ;
#69062=ORIENTED_EDGE ( 'NONE', *, *, #55848, .T. ) ;
#69095=CARTESIAN_POINT ( 'NONE',  ( 6.160000000000001030, 9.521314400968980422E-16, 0.000000000000000000 ) ) ;
#69116=CARTESIAN_POINT ( 'NONE',  ( -25.39999999999996305, 0.000000000000000000, 2.500000000000000000 ) ) ;
#69121=DIRECTION ( 'NONE',  ( 0.000000000000000000, -1.000000000000000000, 0.000000000000000000 ) ) ;
#69161=ORIENTED_EDGE ( 'NONE', *, *, #39163, .T. ) ;
#69169=CARTESIAN_POINT ( 'NONE',  ( -25.39999999999996305, 0.000000000000000000, 0.000000000000000000 ) ) ;
#69176=CARTESIAN_POINT ( 'NONE',  ( -25.39999999999996305, 0.000000000000000000, 0.000000000000000000 ) ) ;
#69204=CARTESIAN_POINT ( 'NONE',  ( 11.15159235450332176, 3.061616997868380183E-16, -2.500000000000001332 ) ) ;
#69236=EDGE_CURVE ( 'NONE', #39945, #16237, #32039, .T. ) ;
#69252=CARTESIAN_POINT ( 'NONE',  ( 7.408407645496676963, 9.139736423841732040E-16, 0.000000000000000000 ) ) ;
#69256=CIRCLE ( 'NONE', #64587, 2.500000000000000888 ) ;
#69309=ORIENTED_EDGE ( 'NONE', *, *, #74247, .F. ) ;
#69325=ORIENTED_EDGE ( 'NONE', *, *, #43332, .F. ) ;
#69332=DIRECTION ( 'NONE',  ( -1.000000000000000000, -0.000000000000000000, -0.000000000000000000 ) ) ;
#69338=ORIENTED_EDGE ( 'NONE', *, *, #88718, .F. ) ;
#69360=LINE ( 'NONE', #57068, #16576 ) ;
#69365=DIRECTION ( 'NONE',  ( -1.000000000000000000, -1.224606353822377258E-16, -0.000000000000000000 ) ) ;
#69381=DIRECTION ( 'NONE',  ( -1.000000000000000000, -0.000000000000000000, -0.000000000000000000 ) ) ;
#69390=ADVANCED_FACE ( 'NONE', ( #65024 ), #10593, .T. ) ;
#69468=CARTESIAN_POINT ( 'NONE',  ( 26.12840764549667583, -3.851859888774471706E-31, 2.500000000000001332 ) ) ;
#69477=CARTESIAN_POINT ( 'NONE',  ( 25.65999999999999659, 2.055000000000001492, 0.000000000000000000 ) ) ;
#69491=ORIENTED_EDGE ( 'NONE', *, *, #26150, .F. ) ;
#69555=EDGE_CURVE ( 'NONE', #110525, #138330, #55339, .T. ) ;
#69561=CIRCLE ( 'NONE', #81041, 3.113037248396092416 ) ;
#69568=VECTOR ( 'NONE', #117807, 1000.000000000000000 ) ;
#69575=EDGE_CURVE ( 'NONE', #15438, #132789, #115499, .T. ) ;
#69583=DIRECTION ( 'NONE',  ( -1.000000000000000000, -1.224606353822377258E-16, -0.000000000000000000 ) ) ;
#69611=CIRCLE ( 'NONE', #41842, 2.500000000000000888 ) ;
#69640=EDGE_CURVE ( 'NONE', #130911, #23774, #39079, .T. ) ;
#69678=ORIENTED_EDGE ( 'NONE', *, *, #98802, .T. ) ;
#69679=AXIS2_PLACEMENT_3D ( 'NONE', #3355, #70808, #59235 ) ;
#69684=LINE ( 'NONE', #101549, #16750 ) ;
#69724=CARTESIAN_POINT ( 'NONE',  ( 14.42840764549667476, -3.851859888774471706E-31, 2.500000000000001332 ) ) ;
#69735=AXIS2_PLACEMENT_3D ( 'NONE', #55481, #9047, #141781 ) ;
#69765=AXIS2_PLACEMENT_3D ( 'NONE', #107420, #139383, #118280 ) ;
#69772=CIRCLE ( 'NONE', #67371, 2.500000000000000888 ) ;
#69799=VERTEX_POINT ( 'NONE', #128661 ) ;
#69819=VERTEX_POINT ( 'NONE', #140257 ) ;
#69897=ADVANCED_FACE ( 'NONE', ( #95308 ), #74294, .T. ) ;
#69916=CIRCLE ( 'NONE', #30564, 2.500000000000000888 ) ;
#69928=CIRCLE ( 'NONE', #130008, 2.500000000000000888 ) ;
#69994=ORIENTED_EDGE ( 'NONE', *, *, #115481, .T. ) ;
#70009=VERTEX_POINT ( 'NONE', #122043 ) ;
#70012=ORIENTED_EDGE ( 'NONE', *, *, #13862, .F. ) ;
#70049=DIRECTION ( 'NONE',  ( -1.000000000000000000, -1.224606353822377258E-16, -0.000000000000000000 ) ) ;
#70090=AXIS2_PLACEMENT_3D ( 'NONE', #74228, #63386, #140880 ) ;
#70106=ORIENTED_EDGE ( 'NONE', *, *, #69575, .T. ) ;
#70129=VERTEX_POINT ( 'NONE', #18818 ) ;
#70188=CARTESIAN_POINT ( 'NONE',  ( 8.811592354503320124, 9.902892378096218942E-16, 0.000000000000000000 ) ) ;
#70198=DIRECTION ( 'NONE',  ( -1.000000000000000000, -1.224606353822377258E-16, -0.000000000000000000 ) ) ;
#70222=DIRECTION ( 'NONE',  ( -1.000000000000000000, -1.224606353822377258E-16, -0.000000000000000000 ) ) ;
#70236=EDGE_LOOP ( 'NONE', ( #132102, #131514, #119975, #67110, #16677, #17762 ) ) ;
#70302=DIRECTION ( 'NONE',  ( -1.000000000000000000, -1.224606353822377258E-16, -0.000000000000000000 ) ) ;
#70309=FACE_OUTER_BOUND ( 'NONE', #102716, .T. ) ;
#70325=EDGE_LOOP ( 'NONE', ( #86010, #129293, #68279, #97960, #76025, #124585 ) ) ;
#70361=VERTEX_POINT ( 'NONE', #82879 ) ;
#70367=ORIENTED_EDGE ( 'NONE', *, *, #43700, .F. ) ;
#70368=ORIENTED_EDGE ( 'NONE', *, *, #83978, .F. ) ;
#70373=AXIS2_PLACEMENT_3D ( 'NONE', #58652, #102103, #135454 ) ;
#70382=CARTESIAN_POINT ( 'NONE',  ( 14.74000000000000021, 9.521314400968980422E-16, 0.000000000000000000 ) ) ;
#70385=ORIENTED_EDGE ( 'NONE', *, *, #50014, .F. ) ;
#70407=ORIENTED_EDGE ( 'NONE', *, *, #91494, .F. ) ;
#70408=DIRECTION ( 'NONE',  ( 0.5735764363510453823, -0.8191520442889923537, 1.003171929053525486E-16 ) ) ;
#70413=EDGE_LOOP ( 'NONE', ( #67188, #20208 ) ) ;
#70416=AXIS2_PLACEMENT_3D ( 'NONE', #70434, #5796, #50068 ) ;
#70434=CARTESIAN_POINT ( 'NONE',  ( 19.10840764549667270, 9.139736423841732040E-16, 0.000000000000000000 ) ) ;
#70435=ORIENTED_EDGE ( 'NONE', *, *, #41990, .T. ) ;
#70450=EDGE_CURVE ( 'NONE', #30243, #60103, #83367, .T. ) ;
#70492=ORIENTED_EDGE ( 'NONE', *, *, #75185, .F. ) ;
#70499=VECTOR ( 'NONE', #79002, 1000.000000000000114 ) ;
#70523=ORIENTED_EDGE ( 'NONE', *, *, #20731, .T. ) ;
#70555=EDGE_LOOP ( 'NONE', ( #60709, #102768, #70598, #37253, #37095, #112488 ) ) ;
#70556=ORIENTED_EDGE ( 'NONE', *, *, #55848, .F. ) ;
#70590=DIRECTION ( 'NONE',  ( -1.000000000000000000, -0.000000000000000000, -0.000000000000000000 ) ) ;
#70598=ORIENTED_EDGE ( 'NONE', *, *, #79415, .T. ) ;
#70600=ORIENTED_EDGE ( 'NONE', *, *, #22668, .T. ) ;
#70615=EDGE_CURVE ( 'NONE', #128260, #44264, #120364, .T. ) ;
#70808=DIRECTION ( 'NONE',  ( -1.000000000000000000, -0.000000000000000000, -0.000000000000000000 ) ) ;
#70814=ORIENTED_EDGE ( 'NONE', *, *, #131884, .F. ) ;
#70846=DIRECTION ( 'NONE',  ( 0.000000000000000000, -1.000000000000000000, 0.000000000000000000 ) ) ;
#70890=CARTESIAN_POINT ( 'NONE',  ( 11.15159235450332176, 9.902892378096218942E-16, 0.000000000000000000 ) ) ;
#70930=DIRECTION ( 'NONE',  ( 0.000000000000000000, -1.000000000000000000, 0.000000000000000000 ) ) ;
#70941=ORIENTED_EDGE ( 'NONE', *, *, #39503, .F. ) ;
#70965=DIRECTION ( 'NONE',  ( -1.000000000000000000, -1.224606353822377258E-16, -0.000000000000000000 ) ) ;
#70971=CARTESIAN_POINT ( 'NONE',  ( 17.07999999999999829, -2.055000000000000160, 0.000000000000000000 ) ) ;
#71010=EDGE_LOOP ( 'NONE', ( #121546, #3141, #8668, #70367, #15579 ) ) ;
#71020=EDGE_LOOP ( 'NONE', ( #92490, #101557, #61652, #34703, #81423, #7720 ) ) ;
#71061=DIRECTION ( 'NONE',  ( -1.000000000000000000, -1.224606353822377258E-16, -0.000000000000000000 ) ) ;
#71089=DIRECTION ( 'NONE',  ( 1.000000000000000000, -0.000000000000000000, -0.000000000000000000 ) ) ;
#71117=VERTEX_POINT ( 'NONE', #80400 ) ;
#71181=EDGE_CURVE ( 'NONE', #9860, #15339, #91283, .T. ) ;
#71200=AXIS2_PLACEMENT_3D ( 'NONE', #73223, #95657, #139914 ) ;
#71236=CIRCLE ( 'NONE', #131448, 2.500000000000000888 ) ;
#71329=CARTESIAN_POINT ( 'NONE',  ( 25.97159235450331849, 9.902892378096218942E-16, 0.000000000000000000 ) ) ;
#71379=DIRECTION ( 'NONE',  ( 0.000000000000000000, 1.000000000000000000, 0.000000000000000000 ) ) ;
#71450=EDGE_CURVE ( 'NONE', #64832, #52944, #61189, .T. ) ;
#71486=CARTESIAN_POINT ( 'NONE',  ( 26.12840764549667583, 2.499999999999998224, 3.061616997868380183E-16 ) ) ;
#71506=FACE_OUTER_BOUND ( 'NONE', #120349, .T. ) ;
#71510=ORIENTED_EDGE ( 'NONE', *, *, #108159, .F. ) ;
#71528=VERTEX_POINT ( 'NONE', #5994 ) ;
#71532=ADVANCED_FACE ( 'NONE', ( #37975 ), #65065, .T. ) ;
#71542=CIRCLE ( 'NONE', #8959, 2.500000000000000888 ) ;
#71572=DIRECTION ( 'NONE',  ( -1.000000000000000000, -1.224606353822377258E-16, -0.000000000000000000 ) ) ;
#71609=AXIS2_PLACEMENT_3D ( 'NONE', #112040, #78686, #122904 ) ;
#71633=ADVANCED_FACE ( 'NONE', ( #53087 ), #118350, .T. ) ;
#71634=FACE_OUTER_BOUND ( 'NONE', #2413, .T. ) ;
#71652=DIRECTION ( 'NONE',  ( -1.000000000000000000, -1.224606353822377258E-16, -0.000000000000000000 ) ) ;
#71655=ORIENTED_EDGE ( 'NONE', *, *, #43820, .F. ) ;
#71677=EDGE_LOOP ( 'NONE', ( #29978, #104959, #82644, #20092, #104963 ) ) ;
#71705=CARTESIAN_POINT ( 'NONE',  ( 21.44840764549667611, 9.139736423841732040E-16, 0.000000000000000000 ) ) ;
#71710=VECTOR ( 'NONE', #85589, 1000.000000000000000 ) ;
#71732=VECTOR ( 'NONE', #65119, 1000.000000000000000 ) ;
#71737=CARTESIAN_POINT ( 'NONE',  ( 18.63999999999999702, 2.055000000000001492, 2.516649172247811554E-16 ) ) ;
#71761=ORIENTED_EDGE ( 'NONE', *, *, #47991, .T. ) ;
#71771=FACE_OUTER_BOUND ( 'NONE', #19174, .T. ) ;
#71801=ORIENTED_EDGE ( 'NONE', *, *, #130756, .T. ) ;
#71804=EDGE_LOOP ( 'NONE', ( #44421, #4961, #111358, #112505, #20757 ) ) ;
#71816=CARTESIAN_POINT ( 'NONE',  ( 12.86840764549667604, 3.061616997868380183E-16, -2.500000000000001332 ) ) ;
#71855=DIRECTION ( 'NONE',  ( 1.000000000000000000, 1.224606353822377258E-16, 0.000000000000000000 ) ) ;
#71900=ORIENTED_EDGE ( 'NONE', *, *, #14229, .F. ) ;
#71921=CARTESIAN_POINT ( 'NONE',  ( 25.19159235450331735, 9.902892378096218942E-16, 0.000000000000000000 ) ) ;
#71964=ORIENTED_EDGE ( 'NONE', *, *, #19738, .T. ) ;
#71988=CARTESIAN_POINT ( 'NONE',  ( 11.15159235450332176, 9.902892378096218942E-16, 0.000000000000000000 ) ) ;
#71989=VERTEX_POINT ( 'NONE', #137101 ) ;
#72012=AXIS2_PLACEMENT_3D ( 'NONE', #83672, #38709, #7483 ) ;
#72079=CIRCLE ( 'NONE', #9496, 2.055000000000001048 ) ;
#72087=CIRCLE ( 'NONE', #4830, 2.500000000000000888 ) ;
#72133=CARTESIAN_POINT ( 'NONE',  ( 11.93159235450332112, 9.902892378096218942E-16, 0.000000000000000000 ) ) ;
#72170=SHAPE_DEFINITION_REPRESENTATION ( #10783, #428 ) ;
#72194=CARTESIAN_POINT ( 'NONE',  ( -25.39999999999996305, 0.000000000000000000, 0.000000000000000000 ) ) ;
#72221=DIRECTION ( 'NONE',  ( 0.000000000000000000, -1.000000000000000000, 0.000000000000000000 ) ) ;
#72349=VERTEX_POINT ( 'NONE', #115126 ) ;
#72365=DIRECTION ( 'NONE',  ( -1.000000000000000000, -1.224606353822377258E-16, -0.000000000000000000 ) ) ;
#72371=EDGE_CURVE ( 'NONE', #117002, #88966, #15114, .T. ) ;
#72403=ORIENTED_EDGE ( 'NONE', *, *, #30602, .T. ) ;
#72409=DIRECTION ( 'NONE',  ( -0.5735764363510503783, -0.8191520442889886899, 0.000000000000000000 ) ) ;
#72451=DIRECTION ( 'NONE',  ( 0.000000000000000000, -1.000000000000000000, 0.000000000000000000 ) ) ;
#72456=CYLINDRICAL_SURFACE ( 'NONE', #38600, 2.500000000000000000 ) ;
#72460=DIRECTION ( 'NONE',  ( 0.5735764363510451602, 0.8191520442889924647, 0.000000000000000000 ) ) ;
#72499=ORIENTED_EDGE ( 'NONE', *, *, #87092, .T. ) ;
#72540=CARTESIAN_POINT ( 'NONE',  ( 19.41999999999999815, 9.521314400968980422E-16, 0.000000000000000000 ) ) ;
#72620=DIRECTION ( 'NONE',  ( -1.000000000000000000, -1.224606353822377258E-16, -0.000000000000000000 ) ) ;
#72716=CONICAL_SURFACE ( 'NONE', #10143, 2.055000000000001048, 0.9599310885968758145 ) ;
#72729=VERTEX_POINT ( 'NONE', #3356 ) ;
#72752=ORIENTED_EDGE ( 'NONE', *, *, #20605, .F. ) ;
#72765=EDGE_LOOP ( 'NONE', ( #59282, #34049, #131221, #36822, #100739 ) ) ;
#72788=DIRECTION ( 'NONE',  ( -1.000000000000000000, -1.224606353822377258E-16, -0.000000000000000000 ) ) ;
#72810=EDGE_CURVE ( 'NONE', #36267, #75381, #5500, .T. ) ;
#72887=DIRECTION ( 'NONE',  ( 0.000000000000000000, -1.000000000000000000, 0.000000000000000000 ) ) ;
#72902=CYLINDRICAL_SURFACE ( 'NONE', #62937, 2.500000000000000000 ) ;
#72928=DIRECTION ( 'NONE',  ( 0.000000000000000000, -1.000000000000000000, 0.000000000000000000 ) ) ;
#72968=AXIS2_PLACEMENT_3D ( 'NONE', #26559, #80252, #136730 ) ;
#73010=EDGE_LOOP ( 'NONE', ( #78393, #105678, #126279, #127886, #46675 ) ) ;
#73016=ORIENTED_EDGE ( 'NONE', *, *, #44364, .T. ) ;
#73025=ORIENTED_EDGE ( 'NONE', *, *, #31909, .T. ) ;
#73128=DIRECTION ( 'NONE',  ( -1.000000000000000000, -1.224606353822377258E-16, -0.000000000000000000 ) ) ;
#73149=DIRECTION ( 'NONE',  ( -1.000000000000000000, -0.000000000000000000, -0.000000000000000000 ) ) ;
#73211=DIRECTION ( 'NONE',  ( -0.5735764363510507113, 0.8191520442889885789, 1.003171929053520926E-16 ) ) ;
#73223=CARTESIAN_POINT ( 'NONE',  ( 5.380000000000000782, 9.521314400968980422E-16, 0.000000000000000000 ) ) ;
#73224=ADVANCED_FACE ( 'NONE', ( #17467 ), #99689, .T. ) ;
#73234=VECTOR ( 'NONE', #6982, 1000.000000000000000 ) ;
#73236=CARTESIAN_POINT ( 'NONE',  ( 13.49159235450332162, 9.902892378096218942E-16, 0.000000000000000000 ) ) ;
#73239=LINE ( 'NONE', #52174, #75062 ) ;
#73245=AXIS2_PLACEMENT_3D ( 'NONE', #139492, #29249, #108930 ) ;
#73253=LINE ( 'NONE', #29019, #51428 ) ;
#73302=EDGE_CURVE ( 'NONE', #99607, #100020, #129807, .T. ) ;
#73331=CARTESIAN_POINT ( 'NONE',  ( 7.720000000000001528, 9.521314400968980422E-16, 0.000000000000000000 ) ) ;
#73377=AXIS2_PLACEMENT_3D ( 'NONE', #76957, #78358, #67507 ) ;
#73395=ORIENTED_EDGE ( 'NONE', *, *, #3075, .F. ) ;
#73437=CARTESIAN_POINT ( 'NONE',  ( 20.19999999999999929, 2.055000000000001492, 0.000000000000000000 ) ) ;
#73467=CIRCLE ( 'NONE', #27181, 2.055000000000001048 ) ;
#73469=DIRECTION ( 'NONE',  ( -1.000000000000000000, -0.000000000000000000, -0.000000000000000000 ) ) ;
#73474=AXIS2_PLACEMENT_3D ( 'NONE', #49117, #27320, #15699 ) ;
#73477=DIRECTION ( 'NONE',  ( 0.000000000000000000, -1.000000000000000000, 0.000000000000000000 ) ) ;
#73503=AXIS2_PLACEMENT_3D ( 'NONE', #50625, #81865, #17274 ) ;
#73520=ORIENTED_EDGE ( 'NONE', *, *, #96857, .T. ) ;
#73545=ORIENTED_EDGE ( 'NONE', *, *, #51367, .T. ) ;
#73663=AXIS2_PLACEMENT_3D ( 'NONE', #85315, #75205, #20057 ) ;
#73670=DIRECTION ( 'NONE',  ( -0.5735764363510507113, 0.8191520442889885789, 1.003171929053520926E-16 ) ) ;
#73714=DIRECTION ( 'NONE',  ( 0.000000000000000000, 1.000000000000000000, 0.000000000000000000 ) ) ;
#73734=AXIS2_PLACEMENT_3D ( 'NONE', #54169, #98357, #30224 ) ;
#73745=ADVANCED_FACE ( 'NONE', ( #110140 ), #48908, .T. ) ;
#73746=EDGE_CURVE ( 'NONE', #1673, #75381, #21034, .T. ) ;
#73747=DIRECTION ( 'NONE',  ( 0.000000000000000000, -1.000000000000000000, 0.000000000000000000 ) ) ;
#73770=ORIENTED_EDGE ( 'NONE', *, *, #51218, .F. ) ;
#73776=CIRCLE ( 'NONE', #122283, 2.055000000000001048 ) ;
#73777=VERTEX_POINT ( 'NONE', #142790 ) ;
#73786=ORIENTED_EDGE ( 'NONE', *, *, #136312, .T. ) ;
#73789=AXIS2_PLACEMENT_3D ( 'NONE', #101385, #44171, #23835 ) ;
#73876=DIRECTION ( 'NONE',  ( 0.000000000000000000, -1.000000000000000000, 0.000000000000000000 ) ) ;
#73890=ORIENTED_EDGE ( 'NONE', *, *, #120485, .T. ) ;
#73891=ORIENTED_EDGE ( 'NONE', *, *, #23596, .F. ) ;
#73897=CONICAL_SURFACE ( 'NONE', #11341, 2.055000000000001048, 0.9599310885968758145 ) ;
#73922=DIRECTION ( 'NONE',  ( 0.000000000000000000, 0.000000000000000000, 1.000000000000000000 ) ) ;
#73923=ORIENTED_EDGE ( 'NONE', *, *, #50054, .F. ) ;
#73940=LINE ( 'NONE', #86259, #84101 ) ;
#73945=ORIENTED_EDGE ( 'NONE', *, *, #54447, .T. ) ;
#73961=ORIENTED_EDGE ( 'NONE', *, *, #79285, .T. ) ;
#74005=DIRECTION ( 'NONE',  ( -1.000000000000000000, -1.224606353822377258E-16, -0.000000000000000000 ) ) ;
#74020=ORIENTED_EDGE ( 'NONE', *, *, #118482, .F. ) ;
#74029=DIRECTION ( 'NONE',  ( -1.000000000000000000, -1.224606353822377258E-16, -0.000000000000000000 ) ) ;
#74036=FACE_OUTER_BOUND ( 'NONE', #59883, .T. ) ;
#74048=FACE_OUTER_BOUND ( 'NONE', #70325, .T. ) ;
#74073=AXIS2_PLACEMENT_3D ( 'NONE', #14092, #74029, #94339 ) ;
#74083=EDGE_CURVE ( 'NONE', #80743, #27726, #74528, .T. ) ;
#74096=DIRECTION ( 'NONE',  ( 0.5735764363510451602, 0.8191520442889924647, 0.000000000000000000 ) ) ;
#74113=EDGE_CURVE ( 'NONE', #32976, #3234, #65817, .T. ) ;
#74160=VECTOR ( 'NONE', #117461, 1000.000000000000114 ) ;
#74224=DIRECTION ( 'NONE',  ( -1.000000000000000000, -1.224606353822377258E-16, -0.000000000000000000 ) ) ;
#74227=CIRCLE ( 'NONE', #9286, 2.500000000000000888 ) ;
#74228=CARTESIAN_POINT ( 'NONE',  ( 20.97999999999999687, 9.521314400968980422E-16, 0.000000000000000000 ) ) ;
#74247=EDGE_CURVE ( 'NONE', #124621, #121207, #69360, .T. ) ;
#74260=CIRCLE ( 'NONE', #2391, 2.500000000000000888 ) ;
#74268=CONICAL_SURFACE ( 'NONE', #20941, 2.055000000000001048, 0.9599310885968758145 ) ;
#74294=CYLINDRICAL_SURFACE ( 'NONE', #108569, 2.500000000000000000 ) ;
#74308=ORIENTED_EDGE ( 'NONE', *, *, #103245, .T. ) ;
#74319=ADVANCED_FACE ( 'NONE', ( #49034 ), #102198, .T. ) ;
#74321=CARTESIAN_POINT ( 'NONE',  ( 13.18000000000000149, -2.055000000000000160, 0.000000000000000000 ) ) ;
#74322=ORIENTED_EDGE ( 'NONE', *, *, #105046, .F. ) ;
#74341=DIRECTION ( 'NONE',  ( 0.5735764363510451602, 0.8191520442889924647, 0.000000000000000000 ) ) ;
#74379=CONICAL_SURFACE ( 'NONE', #18767, 2.055000000000001048, 0.9599310885968758145 ) ;
#74413=AXIS2_PLACEMENT_3D ( 'NONE', #2109, #125370, #26058 ) ;
#74426=EDGE_LOOP ( 'NONE', ( #68620, #12492, #96867, #104576, #115228 ) ) ;
#74438=AXIS2_PLACEMENT_3D ( 'NONE', #22247, #44041, #89672 ) ;
#74441=EDGE_CURVE ( 'NONE', #31644, #32667, #9642, .T. ) ;
#74506=AXIS2_PLACEMENT_3D ( 'NONE', #9318, #86937, #55748 ) ;
#74516=VECTOR ( 'NONE', #142171, 1000.000000000000000 ) ;
#74528=LINE ( 'NONE', #142623, #106819 ) ;
#74542=DIRECTION ( 'NONE',  ( 0.000000000000000000, -1.000000000000000000, 0.000000000000000000 ) ) ;
#74552=AXIS2_PLACEMENT_3D ( 'NONE', #89702, #12836, #11385 ) ;
#74592=CYLINDRICAL_SURFACE ( 'NONE', #63750, 2.500000000000000000 ) ;
#74599=EDGE_LOOP ( 'NONE', ( #9075, #88833, #27558, #36655, #110980 ) ) ;
#74613=DIRECTION ( 'NONE',  ( 0.000000000000000000, -1.000000000000000000, 0.000000000000000000 ) ) ;
#74616=AXIS2_PLACEMENT_3D ( 'NONE', #13036, #12335, #46451 ) ;
#74663=DIRECTION ( 'NONE',  ( 0.000000000000000000, -1.000000000000000000, 0.000000000000000000 ) ) ;
#74683=ORIENTED_EDGE ( 'NONE', *, *, #126927, .F. ) ;
#74687=DIRECTION ( 'NONE',  ( -1.000000000000000000, -1.224606353822377258E-16, -0.000000000000000000 ) ) ;
#74692=EDGE_CURVE ( 'NONE', #85310, #106451, #30586, .T. ) ;
#74694=EDGE_CURVE ( 'NONE', #6269, #81442, #10488, .T. ) ;
#74712=FACE_OUTER_BOUND ( 'NONE', #23422, .T. ) ;
#74721=VECTOR ( 'NONE', #74341, 1000.000000000000000 ) ;
#74749=DIRECTION ( 'NONE',  ( 0.5735764363510451602, 0.8191520442889924647, 0.000000000000000000 ) ) ;
#74783=ADVANCED_FACE ( 'NONE', ( #3190 ), #125469, .T. ) ;
#74789=ADVANCED_FACE ( 'NONE', ( #135864 ), #83791, .T. ) ;
#74821=ORIENTED_EDGE ( 'NONE', *, *, #17475, .F. ) ;
#74824=CARTESIAN_POINT ( 'NONE',  ( 22.53999999999999915, 2.055000000000001492, 0.000000000000000000 ) ) ;
#74841=DIRECTION ( 'NONE',  ( -1.000000000000000000, -1.224606353822377258E-16, -0.000000000000000000 ) ) ;
#74875=EDGE_LOOP ( 'NONE', ( #137464, #3690, #68345, #28152, #70814, #32984 ) ) ;
#74894=ADVANCED_FACE ( 'NONE', ( #106049 ), #37526, .T. ) ;
#74982=EDGE_CURVE ( 'NONE', #29768, #31472, #64014, .T. ) ;
#74999=ORIENTED_EDGE ( 'NONE', *, *, #76400, .F. ) ;
#75001=CARTESIAN_POINT ( 'NONE',  ( 0.5732283800867132850, 0.5999999999999989786, 4.263122468548287358 ) ) ;
#75032=DIRECTION ( 'NONE',  ( -1.000000000000000000, -1.224606353822377258E-16, -0.000000000000000000 ) ) ;
#75062=VECTOR ( 'NONE', #8621, 1000.000000000000000 ) ;
#75091=CARTESIAN_POINT ( 'NONE',  ( -25.39999999999996305, 0.000000000000000000, 0.000000000000000000 ) ) ;
#75143=CIRCLE ( 'NONE', #19528, 2.500000000000000888 ) ;
#75158=VECTOR ( 'NONE', #135438, 1000.000000000000000 ) ;
#75168=DIRECTION ( 'NONE',  ( -1.000000000000000000, -1.224606353822377258E-16, -0.000000000000000000 ) ) ;
#75185=EDGE_CURVE ( 'NONE', #65687, #21154, #58461, .T. ) ;
#75205=DIRECTION ( 'NONE',  ( -1.000000000000000000, -1.224606353822377258E-16, -0.000000000000000000 ) ) ;
#75219=LINE ( 'NONE', #20796, #115992 ) ;
#75254=DIRECTION ( 'NONE',  ( 0.000000000000000000, -1.000000000000000000, 0.000000000000000000 ) ) ;
#75300=ADVANCED_FACE ( 'NONE', ( #27432 ), #63089, .T. ) ;
#75306=CARTESIAN_POINT ( 'NONE',  ( 18.32840764549667512, 9.139736423841732040E-16, 0.000000000000000000 ) ) ;
#75313=VERTEX_POINT ( 'NONE', #130355 ) ;
#75317=CARTESIAN_POINT ( 'NONE',  ( 21.76000000000000156, 9.521314400968980422E-16, 0.000000000000000000 ) ) ;
#75326=DIRECTION ( 'NONE',  ( -1.000000000000000000, -0.000000000000000000, -0.000000000000000000 ) ) ;
#75352=LINE ( 'NONE', #43426, #64098 ) ;
#75370=DIRECTION ( 'NONE',  ( 0.000000000000000000, -1.000000000000000000, 0.000000000000000000 ) ) ;
#75381=VERTEX_POINT ( 'NONE', #64371 ) ;
#75408=CARTESIAN_POINT ( 'NONE',  ( 7.408407645496676963, 9.139736423841732040E-16, 0.000000000000000000 ) ) ;
#75433=CIRCLE ( 'NONE', #31454, 2.055000000000001048 ) ;
#75481=DIRECTION ( 'NONE',  ( 1.000000000000000000, 1.224606353822377258E-16, 0.000000000000000000 ) ) ;
#75565=ORIENTED_EDGE ( 'NONE', *, *, #7229, .T. ) ;
#75635=CARTESIAN_POINT ( 'NONE',  ( 17.39159235450332019, -2.500000000000000444, 3.061616997868384620E-16 ) ) ;
#75636=DIRECTION ( 'NONE',  ( 0.000000000000000000, 1.000000000000000000, 0.000000000000000000 ) ) ;
#75656=EDGE_LOOP ( 'NONE', ( #110004, #99383, #64694, #54410, #132737, #38220 ) ) ;
#75659=ORIENTED_EDGE ( 'NONE', *, *, #140869, .T. ) ;
#75660=CARTESIAN_POINT ( 'NONE',  ( 0.000000000000000000, 0.000000000000000000, -4.487534009422227577 ) ) ;
#75675=EDGE_CURVE ( 'NONE', #29061, #136372, #11591, .T. ) ;
#75715=DIRECTION ( 'NONE',  ( 0.000000000000000000, -1.000000000000000000, 0.000000000000000000 ) ) ;
#75722=DIRECTION ( 'NONE',  ( -1.000000000000000000, -1.224606353822377258E-16, -0.000000000000000000 ) ) ;
#75738=AXIS2_PLACEMENT_3D ( 'NONE', #84919, #138601, #52984 ) ;
#75747=DIRECTION ( 'NONE',  ( -1.000000000000000000, -1.224606353822377258E-16, -0.000000000000000000 ) ) ;
#75763=DIRECTION ( 'NONE',  ( -1.000000000000000000, -0.000000000000000000, -0.000000000000000000 ) ) ;
#75815=CARTESIAN_POINT ( 'NONE',  ( 15.05159235450332034, -2.500000000000000000, 3.061616997868384127E-16 ) ) ;
#75825=ORIENTED_EDGE ( 'NONE', *, *, #39468, .T. ) ;
#75833=DIRECTION ( 'NONE',  ( -1.000000000000000000, -1.224606353822377258E-16, -0.000000000000000000 ) ) ;
#75925=AXIS2_PLACEMENT_3D ( 'NONE', #103148, #80709, #124904 ) ;
#75941=CARTESIAN_POINT ( 'NONE',  ( 12.71159235450332048, 3.061616997868378211E-16, -2.500000000000001332 ) ) ;
#75959=VERTEX_POINT ( 'NONE', #11944 ) ;
#75979=AXIS2_PLACEMENT_3D ( 'NONE', #126179, #81265, #125468 ) ;
#76025=ORIENTED_EDGE ( 'NONE', *, *, #106180, .F. ) ;
#76095=CARTESIAN_POINT ( 'NONE',  ( 21.76000000000000156, 9.521314400968980422E-16, 0.000000000000000000 ) ) ;
#76114=ORIENTED_EDGE ( 'NONE', *, *, #22794, .F. ) ;
#76137=EDGE_LOOP ( 'NONE', ( #73016, #133353, #6684, #48608, #110095, #83035 ) ) ;
#76140=EDGE_CURVE ( 'NONE', #42229, #31468, #65039, .T. ) ;
#76157=CARTESIAN_POINT ( 'NONE',  ( 24.41159235450331977, -3.851859888774471706E-31, 2.500000000000001332 ) ) ;
#76159=VERTEX_POINT ( 'NONE', #141598 ) ;
#76173=VECTOR ( 'NONE', #69381, 1000.000000000000000 ) ;
#76175=CIRCLE ( 'NONE', #36825, 2.500000000000000888 ) ;
#76183=CARTESIAN_POINT ( 'NONE',  ( 27.99999999999999645, 9.521314400968980422E-16, 0.000000000000000000 ) ) ;
#76193=CARTESIAN_POINT ( 'NONE',  ( 20.19999999999999929, -2.055000000000000160, 0.000000000000000000 ) ) ;
#76232=AXIS2_PLACEMENT_3D ( 'NONE', #13792, #79124, #34887 ) ;
#76259=EDGE_CURVE ( 'NONE', #92905, #49830, #69611, .T. ) ;
#76273=VECTOR ( 'NONE', #35886, 1000.000000000000000 ) ;
#76281=CARTESIAN_POINT ( 'NONE',  ( 24.56840764549667355, 9.139736423841732040E-16, 0.000000000000000000 ) ) ;
#76313=ORIENTED_EDGE ( 'NONE', *, *, #86854, .F. ) ;
#76316=EDGE_LOOP ( 'NONE', ( #32923, #128973, #135487, #81878, #62850 ) ) ;
#76327=CARTESIAN_POINT ( 'NONE',  ( 23.63159235450331863, -2.500000000000000000, 3.061616997868384127E-16 ) ) ;
#76334=CARTESIAN_POINT ( 'NONE',  ( 9.591592354503321260, -2.500000000000000444, 3.061616997868384620E-16 ) ) ;
#76357=EDGE_LOOP ( 'NONE', ( #78211, #26064, #7328, #111960, #125226 ) ) ;
#76400=EDGE_CURVE ( 'NONE', #78627, #27619, #113645, .T. ) ;
#76439=VECTOR ( 'NONE', #131742, 1000.000000000000114 ) ;
#76442=ADVANCED_FACE ( 'NONE', ( #48710 ), #30350, .T. ) ;
#76460=CIRCLE ( 'NONE', #74073, 2.500000000000000888 ) ;
#76466=ORIENTED_EDGE ( 'NONE', *, *, #87301, .T. ) ;
#76475=VERTEX_POINT ( 'NONE', #124832 ) ;
#76498=DIRECTION ( 'NONE',  ( 1.000000000000000000, 1.224606353822377258E-16, 0.000000000000000000 ) ) ;
#76550=CARTESIAN_POINT ( 'NONE',  ( 5.691592354503320905, 2.500000000000001332, 0.000000000000000000 ) ) ;
#76555=EDGE_CURVE ( 'NONE', #99234, #143251, #48892, .T. ) ;
#76583=ADVANCED_FACE ( 'NONE', ( #18921 ), #29093, .T. ) ;
#76586=VERTEX_POINT ( 'NONE', #7312 ) ;
#76590=CARTESIAN_POINT ( 'NONE',  ( 12.86840764549667604, 9.139736423841732040E-16, 0.000000000000000000 ) ) ;
#76592=EDGE_CURVE ( 'NONE', #106721, #116046, #21133, .T. ) ;
#76610=CARTESIAN_POINT ( 'NONE',  ( 1.199999999999999956, -0.6000000000000001998, 4.543283425070392845 ) ) ;
#76637=EDGE_LOOP ( 'NONE', ( #4644, #55642, #82923, #114428, #10369 ) ) ;
#76644=ADVANCED_FACE ( 'NONE', ( #13027 ), #133418, .T. ) ;
#76692=CONICAL_SURFACE ( 'NONE', #65096, 2.055000000000001048, 0.9599310885968758145 ) ;
#76696=DIRECTION ( 'NONE',  ( 0.000000000000000000, 0.000000000000000000, 1.000000000000000000 ) ) ;
#76739=CARTESIAN_POINT ( 'NONE',  ( 12.71159235450332048, 9.902892378096218942E-16, 0.000000000000000000 ) ) ;
#76744=DIRECTION ( 'NONE',  ( -1.000000000000000000, -1.224606353822377258E-16, -0.000000000000000000 ) ) ;
#76771=ORIENTED_EDGE ( 'NONE', *, *, #137897, .F. ) ;
#76790=EDGE_CURVE ( 'NONE', #21344, #13457, #132209, .T. ) ;
#76857=DIRECTION ( 'NONE',  ( 0.000000000000000000, 1.000000000000000000, 0.000000000000000000 ) ) ;
#76914=DIRECTION ( 'NONE',  ( -1.000000000000000000, -0.000000000000000000, -0.000000000000000000 ) ) ;
#76919=VECTOR ( 'NONE', #59515, 1000.000000000000000 ) ;
#76940=ORIENTED_EDGE ( 'NONE', *, *, #58747, .F. ) ;
#76956=ORIENTED_EDGE ( 'NONE', *, *, #105983, .T. ) ;
#76957=CARTESIAN_POINT ( 'NONE',  ( 10.06000000000000050, 9.521314400968980422E-16, 0.000000000000000000 ) ) ;
#76965=AXIS2_PLACEMENT_3D ( 'NONE', #136701, #114918, #49737 ) ;
#76966=AXIS2_PLACEMENT_3D ( 'NONE', #11478, #55756, #99957 ) ;
#76975=CARTESIAN_POINT ( 'NONE',  ( 27.22000000000000242, -2.055000000000000160, 0.000000000000000000 ) ) ;
#76980=CARTESIAN_POINT ( 'NONE',  ( 14.42840764549667476, -2.500000000000000888, 0.000000000000000000 ) ) ;
#76987=( NAMED_UNIT ( * ) SI_UNIT ( $, .STERADIAN. ) SOLID_ANGLE_UNIT ( ) );
#77006=AXIS2_PLACEMENT_3D ( 'NONE', #122520, #100785, #35572 ) ;
#77016=CARTESIAN_POINT ( 'NONE',  ( 16.76840764549667639, 3.061616997868385113E-16, -2.500000000000001332 ) ) ;
#77018=CARTESIAN_POINT ( 'NONE',  ( 21.29159235450332233, 9.902892378096218942E-16, 0.000000000000000000 ) ) ;
#77028=ORIENTED_EDGE ( 'NONE', *, *, #120717, .T. ) ;
#77035=VERTEX_POINT ( 'NONE', #39832 ) ;
#77049=ORIENTED_EDGE ( 'NONE', *, *, #123629, .F. ) ;
#77073=EDGE_CURVE ( 'NONE', #47703, #29768, #69928, .T. ) ;
#77074=VERTEX_POINT ( 'NONE', #67841 ) ;
#77111=AXIS2_PLACEMENT_3D ( 'NONE', #65155, #120178, #32511 ) ;
#77140=EDGE_CURVE ( 'NONE', #124621, #36518, #102584, .T. ) ;
#77143=VERTEX_POINT ( 'NONE', #45366 ) ;
#77147=DIRECTION ( 'NONE',  ( -1.000000000000000000, -1.224606353822377258E-16, -0.000000000000000000 ) ) ;
#77160=EDGE_CURVE ( 'NONE', #7890, #85293, #42062, .T. ) ;
#77164=DIRECTION ( 'NONE',  ( -1.000000000000000000, -1.224606353822377258E-16, -0.000000000000000000 ) ) ;
#77180=ORIENTED_EDGE ( 'NONE', *, *, #71181, .F. ) ;
#77204=ORIENTED_EDGE ( 'NONE', *, *, #135385, .T. ) ;
#77211=CARTESIAN_POINT ( 'NONE',  ( 8.811592354503320124, -5.777789833161707559E-31, 2.500000000000001332 ) ) ;
#77279=ADVANCED_FACE ( 'NONE', ( #6059 ), #48185, .T. ) ;
#77319=AXIS2_PLACEMENT_3D ( 'NONE', #86543, #100264, #64065 ) ;
#77321=DIRECTION ( 'NONE',  ( 0.000000000000000000, 1.000000000000000000, 0.000000000000000000 ) ) ;
#77361=ADVANCED_FACE ( 'NONE', ( #96428 ), #39794, .T. ) ;
#77389=VERTEX_POINT ( 'NONE', #5858 ) ;
#77408=DIRECTION ( 'NONE',  ( -1.000000000000000000, -1.224606353822377258E-16, -0.000000000000000000 ) ) ;
#77429=EDGE_CURVE ( 'NONE', #139966, #124257, #95750, .T. ) ;
#77448=DIRECTION ( 'NONE',  ( 0.000000000000000000, 0.000000000000000000, 1.000000000000000000 ) ) ;
#77474=CARTESIAN_POINT ( 'NONE',  ( 8.500000000000000000, -2.055000000000000160, 0.000000000000000000 ) ) ;
#77498=AXIS2_PLACEMENT_3D ( 'NONE', #111259, #100418, #89526 ) ;
#77509=DIRECTION ( 'NONE',  ( -0.5735764363510507113, 0.8191520442889885789, 1.003171929053520926E-16 ) ) ;
#77563=ORIENTED_EDGE ( 'NONE', *, *, #111097, .F. ) ;
#77608=AXIS2_PLACEMENT_3D ( 'NONE', #105705, #82564, #39054 ) ;
#77619=ORIENTED_EDGE ( 'NONE', *, *, #52238, .F. ) ;
#77676=ADVANCED_FACE ( 'NONE', ( #2105 ), #90602, .T. ) ;
#77706=DIRECTION ( 'NONE',  ( 0.000000000000000000, -1.000000000000000000, 0.000000000000000000 ) ) ;
#77744=EDGE_CURVE ( 'NONE', #26004, #143241, #123191, .T. ) ;
#77760=DIRECTION ( 'NONE',  ( -1.000000000000000000, -1.224606353822377258E-16, -0.000000000000000000 ) ) ;
#77779=DIRECTION ( 'NONE',  ( 1.000000000000000000, 0.000000000000000000, 0.000000000000000000 ) ) ;
#77840=FACE_OUTER_BOUND ( 'NONE', #47887, .T. ) ;
#77842=DIRECTION ( 'NONE',  ( -1.000000000000000000, -0.000000000000000000, -0.000000000000000000 ) ) ;
#77846=ORIENTED_EDGE ( 'NONE', *, *, #21443, .T. ) ;
#77847=DIRECTION ( 'NONE',  ( 0.000000000000000000, -1.000000000000000000, 0.000000000000000000 ) ) ;
#77862=AXIS2_PLACEMENT_3D ( 'NONE', #125733, #11938, #135196 ) ;
#77865=ADVANCED_FACE ( 'NONE', ( #26596 ), #79244, .T. ) ;
#77890=ADVANCED_FACE ( 'NONE', ( #49807 ), #90806, .T. ) ;
#77929=DIRECTION ( 'NONE',  ( 0.000000000000000000, 1.000000000000000000, 0.000000000000000000 ) ) ;
#77958=AXIS2_PLACEMENT_3D ( 'NONE', #76095, #97080, #120264 ) ;
#77969=DIRECTION ( 'NONE',  ( 0.000000000000000000, 0.000000000000000000, 1.000000000000000000 ) ) ;
#77983=DIRECTION ( 'NONE',  ( 0.000000000000000000, -1.000000000000000000, 0.000000000000000000 ) ) ;
#78011=EDGE_CURVE ( 'NONE', #44918, #138069, #45882, .T. ) ;
#78025=ORIENTED_EDGE ( 'NONE', *, *, #79441, .T. ) ;
#78032=VERTEX_POINT ( 'NONE', #21244 ) ;
#78066=CARTESIAN_POINT ( 'NONE',  ( 18.63999999999999702, -2.055000000000000160, 2.789133085058098087E-16 ) ) ;
#78096=DIRECTION ( 'NONE',  ( 0.000000000000000000, 1.065814103640150279E-14, 1.000000000000000000 ) ) ;
#78202=CIRCLE ( 'NONE', #96672, 2.500000000000000888 ) ;
#78211=ORIENTED_EDGE ( 'NONE', *, *, #46730, .T. ) ;
#78219=CARTESIAN_POINT ( 'NONE',  ( 25.97159235450331849, -3.851859888774471706E-31, 2.500000000000001332 ) ) ;
#78249=ORIENTED_EDGE ( 'NONE', *, *, #26150, .T. ) ;
#78272=EDGE_LOOP ( 'NONE', ( #102950, #97329, #45345, #10552, #33937, #13762 ) ) ;
#78281=DIRECTION ( 'NONE',  ( 0.000000000000000000, -1.000000000000000000, 0.000000000000000000 ) ) ;
#78290=CARTESIAN_POINT ( 'NONE',  ( -25.39999999999996305, 0.000000000000000000, 0.000000000000000000 ) ) ;
#78316=CARTESIAN_POINT ( 'NONE',  ( 5.068407645496677105, 9.139736423841732040E-16, 0.000000000000000000 ) ) ;
#78323=AXIS2_PLACEMENT_3D ( 'NONE', #128831, #122776, #119364 ) ;
#78358=DIRECTION ( 'NONE',  ( -1.000000000000000000, -1.224606353822377258E-16, -0.000000000000000000 ) ) ;
#78393=ORIENTED_EDGE ( 'NONE', *, *, #47128, .F. ) ;
#78524=DIRECTION ( 'NONE',  ( 0.000000000000000000, -1.000000000000000000, 0.000000000000000000 ) ) ;
#78563=EDGE_CURVE ( 'NONE', #143251, #47888, #7554, .T. ) ;
#78573=CARTESIAN_POINT ( 'NONE',  ( 26.90840764549667696, 2.500000000000003553, 3.061616997868386099E-16 ) ) ;
#78614=DIRECTION ( 'NONE',  ( -1.000000000000000000, -1.224606353822377258E-16, -0.000000000000000000 ) ) ;
#78623=CIRCLE ( 'NONE', #53138, 2.500000000000000888 ) ;
#78627=VERTEX_POINT ( 'NONE', #23946 ) ;
#78686=DIRECTION ( 'NONE',  ( -1.000000000000000000, -1.224606353822377258E-16, -0.000000000000000000 ) ) ;
#78691=ORIENTED_EDGE ( 'NONE', *, *, #122511, .F. ) ;
#78702=ORIENTED_EDGE ( 'NONE', *, *, #46954, .T. ) ;
#78772=EDGE_LOOP ( 'NONE', ( #56758, #109957, #5412, #113589, #39696 ) ) ;
#78802=EDGE_CURVE ( 'NONE', #7326, #19604, #110732, .T. ) ;
#78821=CIRCLE ( 'NONE', #97191, 2.500000000000000888 ) ;
#78839=AXIS2_PLACEMENT_3D ( 'NONE', #32681, #131261, #42134 ) ;
#78847=EDGE_CURVE ( 'NONE', #131273, #115014, #21625, .T. ) ;
#78861=VERTEX_POINT ( 'NONE', #10708 ) ;
#78866=CARTESIAN_POINT ( 'NONE',  ( 17.85999999999999943, 2.055000000000001492, 0.000000000000000000 ) ) ;
#78881=CARTESIAN_POINT ( 'NONE',  ( 6.940000000000001279, -2.055000000000000160, 2.789133085058098087E-16 ) ) ;
#78894=CYLINDRICAL_SURFACE ( 'NONE', #105853, 2.500000000000000000 ) ;
#78944=DIRECTION ( 'NONE',  ( 0.000000000000000000, -1.000000000000000000, 0.000000000000000000 ) ) ;
#78945=EDGE_LOOP ( 'NONE', ( #36272, #2050, #126869, #30030, #108820, #55224 ) ) ;
#78956=CARTESIAN_POINT ( 'NONE',  ( 17.39159235450332019, 9.902892378096218942E-16, 0.000000000000000000 ) ) ;
#78991=FACE_OUTER_BOUND ( 'NONE', #26840, .T. ) ;
#78996=AXIS2_PLACEMENT_3D ( 'NONE', #64968, #75833, #32327 ) ;
#79001=AXIS2_PLACEMENT_3D ( 'NONE', #28882, #97693, #129594 ) ;
#79002=DIRECTION ( 'NONE',  ( -0.5735764363510503783, -0.8191520442889886899, 0.000000000000000000 ) ) ;
#79007=CARTESIAN_POINT ( 'NONE',  ( 27.53159235450332076, 2.500000000000001332, 0.000000000000000000 ) ) ;
#79029=EDGE_CURVE ( 'NONE', #29586, #132528, #128058, .T. ) ;
#79056=CONICAL_SURFACE ( 'NONE', #69735, 2.500000000000000888, 0.9599310885968822538 ) ;
#79064=CARTESIAN_POINT ( 'NONE',  ( 14.27159235450332098, 9.902892378096218942E-16, 0.000000000000000000 ) ) ;
#79065=ORIENTED_EDGE ( 'NONE', *, *, #95218, .F. ) ;
#79075=CARTESIAN_POINT ( 'NONE',  ( 16.76840764549667639, 9.139736423841732040E-16, 0.000000000000000000 ) ) ;
#79109=AXIS2_PLACEMENT_3D ( 'NONE', #67485, #66748, #23959 ) ;
#79124=DIRECTION ( 'NONE',  ( -1.000000000000000000, -1.224606353822377258E-16, -0.000000000000000000 ) ) ;
#79138=ORIENTED_EDGE ( 'NONE', *, *, #23128, .F. ) ;
#79157=CARTESIAN_POINT ( 'NONE',  ( 11.93159235450332112, -3.851859888774471706E-31, 2.500000000000001332 ) ) ;
#79169=CARTESIAN_POINT ( 'NONE',  ( 20.51159235450331764, 9.902892378096218942E-16, 0.000000000000000000 ) ) ;
#79230=CONICAL_SURFACE ( 'NONE', #97697, 2.500000000000000888, 0.9599310885968822538 ) ;
#79244=CONICAL_SURFACE ( 'NONE', #53764, 2.500000000000000888, 0.9599310885968822538 ) ;
#79257=VERTEX_POINT ( 'NONE', #22836 ) ;
#79259=VECTOR ( 'NONE', #123578, 1000.000000000000000 ) ;
#79285=EDGE_CURVE ( 'NONE', #36518, #1673, #726, .T. ) ;
#79290=ADVANCED_FACE ( 'NONE', ( #24997 ), #121185, .T. ) ;
#79334=ORIENTED_EDGE ( 'NONE', *, *, #104878, .F. ) ;
#79396=DIRECTION ( 'NONE',  ( 0.000000000000000000, -1.000000000000000000, 0.000000000000000000 ) ) ;
#79399=AXIS2_PLACEMENT_3D ( 'NONE', #142073, #110810, #44180 ) ;
#79415=EDGE_CURVE ( 'NONE', #136372, #23774, #138067, .T. ) ;
#79441=EDGE_CURVE ( 'NONE', #45804, #47923, #107321, .T. ) ;
#79444=CONICAL_SURFACE ( 'NONE', #56260, 2.055000000000001048, 0.9599310885968758145 ) ;
#79454=DIRECTION ( 'NONE',  ( -1.000000000000000000, -1.224606353822377258E-16, -0.000000000000000000 ) ) ;
#79466=CARTESIAN_POINT ( 'NONE',  ( -25.39999999999996305, 0.000000000000000000, 2.500000000000000000 ) ) ;
#79517=EDGE_LOOP ( 'NONE', ( #69309, #95124, #73545, #1369, #24184 ) ) ;
#79519=ORIENTED_EDGE ( 'NONE', *, *, #118571, .F. ) ;
#79532=CIRCLE ( 'NONE', #40090, 2.500000000000000888 ) ;
#79541=ORIENTED_EDGE ( 'NONE', *, *, #27514, .F. ) ;
#79561=EDGE_LOOP ( 'NONE', ( #137936, #12718, #63798, #38234, #142256 ) ) ;
#79574=DIRECTION ( 'NONE',  ( -1.000000000000000000, -1.224606353822377258E-16, -0.000000000000000000 ) ) ;
#79589=VERTEX_POINT ( 'NONE', #119844 ) ;
#79613=FACE_OUTER_BOUND ( 'NONE', #110522, .T. ) ;
#79683=EDGE_CURVE ( 'NONE', #129879, #31472, #28385, .T. ) ;
#79716=AXIS2_PLACEMENT_3D ( 'NONE', #45842, #90772, #100207 ) ;
#79730=DIRECTION ( 'NONE',  ( -1.000000000000000000, -0.000000000000000000, -0.000000000000000000 ) ) ;
#79742=EDGE_CURVE ( 'NONE', #24873, #93367, #105077, .T. ) ;
#79848=DIRECTION ( 'NONE',  ( -1.000000000000000000, -1.224606353822377258E-16, -0.000000000000000000 ) ) ;
#79870=DIRECTION ( 'NONE',  ( -1.000000000000000000, -1.224606353822377258E-16, -0.000000000000000000 ) ) ;
#79884=ADVANCED_FACE ( 'NONE', ( #111502 ), #23034, .T. ) ;
#79885=VERTEX_POINT ( 'NONE', #108606 ) ;
#79921=CARTESIAN_POINT ( 'NONE',  ( 4.600000000000001421, 9.521314400968980422E-16, 0.000000000000000000 ) ) ;
#79940=ORIENTED_EDGE ( 'NONE', *, *, #61035, .F. ) ;
#79961=ADVANCED_FACE ( 'NONE', ( #45576 ), #79444, .T. ) ;
#79991=AXIS2_PLACEMENT_3D ( 'NONE', #130947, #10543, #77983 ) ;
#79992=DIRECTION ( 'NONE',  ( -1.000000000000000000, -1.224606353822377258E-16, -0.000000000000000000 ) ) ;
#80023=AXIS2_PLACEMENT_3D ( 'NONE', #126115, #102933, #39839 ) ;
#80064=CARTESIAN_POINT ( 'NONE',  ( 11.30840764549667554, 9.139736423841732040E-16, 0.000000000000000000 ) ) ;
#80159=DIRECTION ( 'NONE',  ( -1.000000000000000000, -1.224606353822377258E-16, -0.000000000000000000 ) ) ;
#80166=CARTESIAN_POINT ( 'NONE',  ( 20.66840764549667497, 0.000000000000000000, 2.500000000000001332 ) ) ;
#80194=CIRCLE ( 'NONE', #17634, 2.055000000000001048 ) ;
#80203=ORIENTED_EDGE ( 'NONE', *, *, #44696, .F. ) ;
#80236=DIRECTION ( 'NONE',  ( -1.000000000000000000, -1.224606353822377258E-16, -0.000000000000000000 ) ) ;
#80248=ORIENTED_EDGE ( 'NONE', *, *, #136312, .F. ) ;
#80252=DIRECTION ( 'NONE',  ( -1.000000000000000000, -0.000000000000000000, -0.000000000000000000 ) ) ;
#80304=CONICAL_SURFACE ( 'NONE', #45544, 2.500000000000000888, 0.9599310885968822538 ) ;
#80307=ADVANCED_FACE ( 'NONE', ( #86013 ), #95513, .T. ) ;
#80315=AXIS2_PLACEMENT_3D ( 'NONE', #94375, #50895, #96488 ) ;
#80400=CARTESIAN_POINT ( 'NONE',  ( 24.87999999999999901, 2.055000000000001492, 0.000000000000000000 ) ) ;
#80412=CARTESIAN_POINT ( 'NONE',  ( 9.279999999999999361, 9.521314400968980422E-16, 0.000000000000000000 ) ) ;
#80440=ORIENTED_EDGE ( 'NONE', *, *, #39785, .T. ) ;
#80457=VERTEX_POINT ( 'NONE', #80166 ) ;
#80486=VECTOR ( 'NONE', #134190, 999.9999999999998863 ) ;
#80513=DIRECTION ( 'NONE',  ( 0.000000000000000000, -1.000000000000000000, 0.000000000000000000 ) ) ;
#80520=DIRECTION ( 'NONE',  ( -1.000000000000000000, -1.224606353822377258E-16, -0.000000000000000000 ) ) ;
#80531=CARTESIAN_POINT ( 'NONE',  ( 14.27159235450332098, 9.902892378096218942E-16, 0.000000000000000000 ) ) ;
#80532=LINE ( 'NONE', #124727, #49225 ) ;
#80579=DIRECTION ( 'NONE',  ( -1.000000000000000000, -0.000000000000000000, -0.000000000000000000 ) ) ;
#80582=FACE_OUTER_BOUND ( 'NONE', #79517, .T. ) ;
#80584=CARTESIAN_POINT ( 'NONE',  ( 10.52840764549667618, 9.139736423841732040E-16, 0.000000000000000000 ) ) ;
#80592=VECTOR ( 'NONE', #66197, 1000.000000000000000 ) ;
#80595=EDGE_LOOP ( 'NONE', ( #131312, #76956, #126153, #87921, #115213 ) ) ;
#80604=LINE ( 'NONE', #11008, #96805 ) ;
#80627=DIRECTION ( 'NONE',  ( 0.000000000000000000, -1.000000000000000000, 0.000000000000000000 ) ) ;
#80639=CARTESIAN_POINT ( 'NONE',  ( 27.99999999999999645, -2.055000000000000160, 0.000000000000000000 ) ) ;
#80709=DIRECTION ( 'NONE',  ( -1.000000000000000000, -0.000000000000000000, -0.000000000000000000 ) ) ;
#80735=CARTESIAN_POINT ( 'NONE',  ( 24.87999999999999901, 2.055000000000001492, 2.516649172247811554E-16 ) ) ;
#80743=VERTEX_POINT ( 'NONE', #24390 ) ;
#80827=VERTEX_POINT ( 'NONE', #7613 ) ;
#80830=VECTOR ( 'NONE', #62811, 1000.000000000000000 ) ;
#80835=ORIENTED_EDGE ( 'NONE', *, *, #17388, .T. ) ;
#80928=ORIENTED_EDGE ( 'NONE', *, *, #31562, .F. ) ;
#80938=ORIENTED_EDGE ( 'NONE', *, *, #140769, .T. ) ;
#80964=DIRECTION ( 'NONE',  ( 0.000000000000000000, -1.000000000000000000, 0.000000000000000000 ) ) ;
#80989=ADVANCED_FACE ( 'NONE', ( #98223 ), #107650, .T. ) ;
#80993=EDGE_LOOP ( 'NONE', ( #7061, #56035, #87934, #142439, #69338, #71900 ) ) ;
#80996=DIRECTION ( 'NONE',  ( -1.000000000000000000, -1.224606353822377258E-16, -0.000000000000000000 ) ) ;
#81001=AXIS2_PLACEMENT_3D ( 'NONE', #76281, #98026, #128516 ) ;
#81002=CONICAL_SURFACE ( 'NONE', #125060, 2.500000000000000888, 0.9599310885968822538 ) ;
#81026=CIRCLE ( 'NONE', #11529, 2.500000000000000888 ) ;
#81041=AXIS2_PLACEMENT_3D ( 'NONE', #20328, #53719, #66031 ) ;
#81111=EDGE_CURVE ( 'NONE', #9966, #77074, #14803, .T. ) ;
#81144=FACE_OUTER_BOUND ( 'NONE', #83012, .T. ) ;
#81170=ORIENTED_EDGE ( 'NONE', *, *, #106090, .T. ) ;
#81206=AXIS2_PLACEMENT_3D ( 'NONE', #20548, #65550, #106854 ) ;
#81253=LINE ( 'NONE', #59502, #57537 ) ;
#81265=DIRECTION ( 'NONE',  ( -1.000000000000000000, -0.000000000000000000, -0.000000000000000000 ) ) ;
#81276=AXIS2_PLACEMENT_3D ( 'NONE', #57772, #80236, #25092 ) ;
#81283=ADVANCED_FACE ( 'NONE', ( #62572 ), #72716, .T. ) ;
#81296=CARTESIAN_POINT ( 'NONE',  ( 17.39159235450332019, 9.902892378096218942E-16, 0.000000000000000000 ) ) ;
#81311=DIRECTION ( 'NONE',  ( 0.000000000000000000, -1.000000000000000000, 0.000000000000000000 ) ) ;
#81312=ORIENTED_EDGE ( 'NONE', *, *, #84272, .T. ) ;
#81324=DIRECTION ( 'NONE',  ( -1.000000000000000000, -1.224606353822377258E-16, -0.000000000000000000 ) ) ;
#81350=VERTEX_POINT ( 'NONE', #139446 ) ;
#81362=CIRCLE ( 'NONE', #9587, 2.500000000000000888 ) ;
#81368=CARTESIAN_POINT ( 'NONE',  ( 10.37159235450332062, 9.902892378096218942E-16, 0.000000000000000000 ) ) ;
#81384=LINE ( 'NONE', #33769, #135700 ) ;
#81389=DIRECTION ( 'NONE',  ( -1.000000000000000000, -1.224606353822377258E-16, -0.000000000000000000 ) ) ;
#81399=CARTESIAN_POINT ( 'NONE',  ( 21.29159235450332233, 2.500000000000001776, 0.000000000000000000 ) ) ;
#81414=DIRECTION ( 'NONE',  ( -1.000000000000000000, -1.224606353822377258E-16, -0.000000000000000000 ) ) ;
#81420=AXIS2_PLACEMENT_3D ( 'NONE', #29180, #50951, #116903 ) ;
#81423=ORIENTED_EDGE ( 'NONE', *, *, #7319, .F. ) ;
#81442=VERTEX_POINT ( 'NONE', #118349 ) ;
#81489=DIRECTION ( 'NONE',  ( 0.000000000000000000, -1.000000000000000000, 0.000000000000000000 ) ) ;
#81511=ADVANCED_FACE ( 'NONE', ( #110144 ), #100505, .T. ) ;
#81545=EDGE_LOOP ( 'NONE', ( #32173, #99389, #12200, #98445 ) ) ;
#81553=EDGE_CURVE ( 'NONE', #112837, #61060, #58702, .T. ) ;
#81572=DIRECTION ( 'NONE',  ( -1.000000000000000000, -0.000000000000000000, -0.000000000000000000 ) ) ;
#81654=EDGE_LOOP ( 'NONE', ( #47969, #117152 ) ) ;
#81660=ORIENTED_EDGE ( 'NONE', *, *, #143335, .F. ) ;
#81664=EDGE_CURVE ( 'NONE', #87975, #31572, #24130, .T. ) ;
#81704=DIRECTION ( 'NONE',  ( 0.5735764363510453823, -0.8191520442889923537, 1.003171929053525486E-16 ) ) ;
#81714=DIRECTION ( 'NONE',  ( -0.5735764363510507113, 0.8191520442889885789, 1.003171929053520926E-16 ) ) ;
#81719=CARTESIAN_POINT ( 'NONE',  ( 15.05159235450332034, -2.500000000000000444, 3.061616997868384620E-16 ) ) ;
#81725=EDGE_CURVE ( 'NONE', #68485, #29586, #18671, .T. ) ;
#81745=VERTEX_POINT ( 'NONE', #7062 ) ;
#81767=EDGE_CURVE ( 'NONE', #11132, #24858, #113498, .T. ) ;
#81865=DIRECTION ( 'NONE',  ( -1.000000000000000000, -1.224606353822377258E-16, -0.000000000000000000 ) ) ;
#81870=EDGE_CURVE ( 'NONE', #57148, #55993, #108822, .T. ) ;
#81878=ORIENTED_EDGE ( 'NONE', *, *, #63254, .T. ) ;
#81896=CARTESIAN_POINT ( 'NONE',  ( 4.911592354503321545, 3.061616997868380183E-16, -2.500000000000001332 ) ) ;
#81915=DIRECTION ( 'NONE',  ( 0.000000000000000000, 1.000000000000000000, 0.000000000000000000 ) ) ;
#81923=LINE ( 'NONE', #71737, #35799 ) ;
#81926=DIRECTION ( 'NONE',  ( -1.000000000000000000, -1.224606353822377258E-16, -0.000000000000000000 ) ) ;
#81927=CARTESIAN_POINT ( 'NONE',  ( 10.37159235450332062, -2.500000000000000444, 3.061616997868384620E-16 ) ) ;
#81938=ORIENTED_EDGE ( 'NONE', *, *, #94394, .T. ) ;
#81945=EDGE_LOOP ( 'NONE', ( #123177, #65727, #139657, #3266, #4265, #101341 ) ) ;
#82012=VERTEX_POINT ( 'NONE', #140313 ) ;
#82018=DIRECTION ( 'NONE',  ( -0.5735764363510503783, -0.8191520442889886899, 0.000000000000000000 ) ) ;
#82028=ORIENTED_EDGE ( 'NONE', *, *, #20605, .T. ) ;
#82055=EDGE_CURVE ( 'NONE', #58993, #51758, #107671, .T. ) ;
#82081=ORIENTED_EDGE ( 'NONE', *, *, #108825, .F. ) ;
#82097=CIRCLE ( 'NONE', #19540, 2.055000000000001048 ) ;
#82122=ORIENTED_EDGE ( 'NONE', *, *, #18021, .T. ) ;
#82193=AXIS2_PLACEMENT_3D ( 'NONE', #10754, #55738, #141289 ) ;
#82197=DIRECTION ( 'NONE',  ( 0.000000000000000000, -1.000000000000000000, 0.000000000000000000 ) ) ;
#82207=DIRECTION ( 'NONE',  ( 0.000000000000000000, -1.000000000000000000, 0.000000000000000000 ) ) ;
#82216=ORIENTED_EDGE ( 'NONE', *, *, #20091, .F. ) ;
#82301=CARTESIAN_POINT ( 'NONE',  ( 17.85999999999999943, 9.521314400968980422E-16, 0.000000000000000000 ) ) ;
#82384=CARTESIAN_POINT ( 'NONE',  ( 13.96000000000000085, 9.521314400968980422E-16, 0.000000000000000000 ) ) ;
#82433=CARTESIAN_POINT ( 'NONE',  ( 16.61159235450331906, 9.902892378096218942E-16, 0.000000000000000000 ) ) ;
#82525=ORIENTED_EDGE ( 'NONE', *, *, #42449, .F. ) ;
#82564=DIRECTION ( 'NONE',  ( -1.000000000000000000, -1.224606353822377258E-16, -0.000000000000000000 ) ) ;
#82617=EDGE_CURVE ( 'NONE', #34870, #96749, #81362, .T. ) ;
#82632=DIRECTION ( 'NONE',  ( 0.000000000000000000, -1.000000000000000000, 0.000000000000000000 ) ) ;
#82644=ORIENTED_EDGE ( 'NONE', *, *, #142827, .T. ) ;
#82660=AXIS2_PLACEMENT_3D ( 'NONE', #29653, #41994, #50719 ) ;
#82701=DIRECTION ( 'NONE',  ( 0.000000000000000000, -1.000000000000000000, 0.000000000000000000 ) ) ;
#82705=AXIS2_PLACEMENT_3D ( 'NONE', #69169, #123569, #113348 ) ;
#82727=CONICAL_SURFACE ( 'NONE', #87065, 2.055000000000001048, 0.9599310885968758145 ) ;
#82748=LINE ( 'NONE', #113932, #53625 ) ;
#82762=VERTEX_POINT ( 'NONE', #50827 ) ;
#82772=VERTEX_POINT ( 'NONE', #26920 ) ;
#82774=DIRECTION ( 'NONE',  ( 0.000000000000000000, -1.000000000000000000, 0.000000000000000000 ) ) ;
#82813=EDGE_CURVE ( 'NONE', #39592, #64109, #102144, .T. ) ;
#82823=CARTESIAN_POINT ( 'NONE',  ( 5.068407645496677105, -3.851859888774471706E-31, 2.500000000000001332 ) ) ;
#82879=CARTESIAN_POINT ( 'NONE',  ( 12.86840764549667604, -3.851859888774471706E-31, 2.500000000000001332 ) ) ;
#82882=CIRCLE ( 'NONE', #73663, 2.500000000000000888 ) ;
#82908=AXIS2_PLACEMENT_3D ( 'NONE', #77018, #32795, #132830 ) ;
#82914=CIRCLE ( 'NONE', #36537, 2.055000000000001048 ) ;
#82923=ORIENTED_EDGE ( 'NONE', *, *, #36788, .F. ) ;
#83012=EDGE_LOOP ( 'NONE', ( #13501, #15926, #50227, #131979, #66991 ) ) ;
#83016=CARTESIAN_POINT ( 'NONE',  ( 11.62000000000000099, 9.521314400968980422E-16, 0.000000000000000000 ) ) ;
#83035=ORIENTED_EDGE ( 'NONE', *, *, #88012, .F. ) ;
#83050=LINE ( 'NONE', #25801, #111702 ) ;
#83056=ORIENTED_EDGE ( 'NONE', *, *, #68561, .T. ) ;
#83062=CIRCLE ( 'NONE', #50665, 2.500000000000000888 ) ;
#83096=VECTOR ( 'NONE', #92166, 1000.000000000000000 ) ;
#83123=AXIS2_PLACEMENT_3D ( 'NONE', #96059, #9011, #53270 ) ;
#83244=EDGE_CURVE ( 'NONE', #41073, #65687, #20871, .T. ) ;
#83277=CARTESIAN_POINT ( 'NONE',  ( 16.76840764549667639, -2.499999999999996003, 0.000000000000000000 ) ) ;
#83290=TOROIDAL_SURFACE ( 'NONE', #20764, 3.113037248396092416, 1.500000000000000000 ) ;
#83354=ORIENTED_EDGE ( 'NONE', *, *, #124799, .T. ) ;
#83355=FACE_OUTER_BOUND ( 'NONE', #56685, .T. ) ;
#83367=CIRCLE ( 'NONE', #81001, 2.500000000000000888 ) ;
#83390=CARTESIAN_POINT ( 'NONE',  ( -25.39999999999996305, 0.000000000000000000, 0.000000000000000000 ) ) ;
#83406=CIRCLE ( 'NONE', #67159, 2.500000000000000888 ) ;
#83466=DIRECTION ( 'NONE',  ( 0.000000000000000000, -1.000000000000000000, 0.000000000000000000 ) ) ;
#83497=CIRCLE ( 'NONE', #102001, 2.055000000000001048 ) ;
#83511=DIRECTION ( 'NONE',  ( 0.5735764363510451602, 0.8191520442889924647, 0.000000000000000000 ) ) ;
#83569=CARTESIAN_POINT ( 'NONE',  ( 20.51159235450331764, 9.902892378096218942E-16, 0.000000000000000000 ) ) ;
#83625=ORIENTED_EDGE ( 'NONE', *, *, #24034, .F. ) ;
#83656=CIRCLE ( 'NONE', #78996, 2.055000000000001048 ) ;
#83663=CARTESIAN_POINT ( 'NONE',  ( 5.068407645496677105, 2.500000000000000888, 3.061616997868383141E-16 ) ) ;
#83672=CARTESIAN_POINT ( 'NONE',  ( 11.15159235450332176, 9.902892378096218942E-16, 0.000000000000000000 ) ) ;
#83731=DIRECTION ( 'NONE',  ( -1.000000000000000000, -1.224606353822377258E-16, -0.000000000000000000 ) ) ;
#83786=LINE ( 'NONE', #40967, #139731 ) ;
#83791=CONICAL_SURFACE ( 'NONE', #18976, 2.500000000000000888, 0.9599310885968822538 ) ;
#83802=ORIENTED_EDGE ( 'NONE', *, *, #10470, .F. ) ;
#83815=ORIENTED_EDGE ( 'NONE', *, *, #120004, .T. ) ;
#83835=DIRECTION ( 'NONE',  ( -1.000000000000000000, -1.224606353822377258E-16, -0.000000000000000000 ) ) ;
#83869=AXIS2_PLACEMENT_3D ( 'NONE', #71705, #4215, #126762 ) ;
#83961=CARTESIAN_POINT ( 'NONE',  ( 16.61159235450331906, 3.061616997868375253E-16, -2.500000000000001332 ) ) ;
#83968=CARTESIAN_POINT ( 'NONE',  ( 6.471592354503322042, 9.902892378096218942E-16, 0.000000000000000000 ) ) ;
#83978=EDGE_CURVE ( 'NONE', #49830, #139177, #95075, .T. ) ;
#83983=DIRECTION ( 'NONE',  ( -1.000000000000000000, -1.224606353822377258E-16, -0.000000000000000000 ) ) ;
#84019=EDGE_CURVE ( 'NONE', #42322, #34870, #25637, .T. ) ;
#84063=ORIENTED_EDGE ( 'NONE', *, *, #41971, .F. ) ;
#84092=ORIENTED_EDGE ( 'NONE', *, *, #118683, .T. ) ;
#84101=VECTOR ( 'NONE', #42045, 1000.000000000000000 ) ;
#84162=ADVANCED_FACE ( 'NONE', ( #30427 ), #76692, .T. ) ;
#84176=ORIENTED_EDGE ( 'NONE', *, *, #124705, .T. ) ;
#84216=CYLINDRICAL_SURFACE ( 'NONE', #32379, 2.500000000000000000 ) ;
#84232=CARTESIAN_POINT ( 'NONE',  ( 13.96000000000000085, 9.521314400968980422E-16, 0.000000000000000000 ) ) ;
#84242=CARTESIAN_POINT ( 'NONE',  ( 26.43999999999999773, 9.521314400968980422E-16, 0.000000000000000000 ) ) ;
#84272=EDGE_CURVE ( 'NONE', #119001, #114079, #69772, .T. ) ;
#84279=FACE_OUTER_BOUND ( 'NONE', #59474, .T. ) ;
#84338=LINE ( 'NONE', #106746, #119187 ) ;
#84355=CONICAL_SURFACE ( 'NONE', #93529, 2.500000000000000888, 0.9599310885968822538 ) ;
#84450=CARTESIAN_POINT ( 'NONE',  ( 10.37159235450332062, 9.902892378096218942E-16, 0.000000000000000000 ) ) ;
#84475=CARTESIAN_POINT ( 'NONE',  ( 16.30000000000000071, -2.055000000000000160, 0.000000000000000000 ) ) ;
#84478=EDGE_CURVE ( 'NONE', #97682, #95787, #63627, .T. ) ;
#84492=DIRECTION ( 'NONE',  ( -1.000000000000000000, -1.224606353822377258E-16, -0.000000000000000000 ) ) ;
#84494=ORIENTED_EDGE ( 'NONE', *, *, #89673, .F. ) ;
#84520=ORIENTED_EDGE ( 'NONE', *, *, #60446, .T. ) ;
#84561=LINE ( 'NONE', #64225, #90890 ) ;
#84573=CARTESIAN_POINT ( 'NONE',  ( 6.940000000000001279, 2.055000000000001492, 2.516649172247811554E-16 ) ) ;
#84613=CONICAL_SURFACE ( 'NONE', #29028, 2.055000000000001048, 0.9599310885968758145 ) ;
#84686=CARTESIAN_POINT ( 'NONE',  ( 5.848407645496676466, 3.061616997868380183E-16, -2.500000000000001332 ) ) ;
#84691=DIRECTION ( 'NONE',  ( -1.000000000000000000, -0.000000000000000000, -0.000000000000000000 ) ) ;
#84709=DIRECTION ( 'NONE',  ( -1.000000000000000000, -1.224606353822377258E-16, -0.000000000000000000 ) ) ;
#84743=ORIENTED_EDGE ( 'NONE', *, *, #72810, .F. ) ;
#84759=DIRECTION ( 'NONE',  ( 0.5735764363510451602, 0.8191520442889924647, 0.000000000000000000 ) ) ;
#84878=CARTESIAN_POINT ( 'NONE',  ( 19.41999999999999815, 2.055000000000001492, 2.516649172247811554E-16 ) ) ;
#84890=VERTEX_POINT ( 'NONE', #40793 ) ;
#84914=CIRCLE ( 'NONE', #133557, 2.055000000000001048 ) ;
#84916=FACE_OUTER_BOUND ( 'NONE', #120975, .T. ) ;
#84919=CARTESIAN_POINT ( 'NONE',  ( -25.39999999999996305, 0.000000000000000000, 0.000000000000000000 ) ) ;
#84943=CONICAL_SURFACE ( 'NONE', #133593, 2.055000000000001048, 0.9599310885968758145 ) ;
#84952=AXIS2_PLACEMENT_3D ( 'NONE', #95799, #108067, #139346 ) ;
#84953=EDGE_CURVE ( 'NONE', #1660, #35704, #32045, .T. ) ;
#85011=ORIENTED_EDGE ( 'NONE', *, *, #3822, .T. ) ;
#85014=DIRECTION ( 'NONE',  ( 0.000000000000000000, -1.000000000000000000, 0.000000000000000000 ) ) ;
#85039=CARTESIAN_POINT ( 'NONE',  ( 0.000000000000000000, 0.000000000000000000, 0.000000000000000000 ) ) ;
#85061=LINE ( 'NONE', #130002, #105593 ) ;
#85086=EDGE_CURVE ( 'NONE', #113725, #130192, #49051, .T. ) ;
#85101=DIRECTION ( 'NONE',  ( 0.000000000000000000, 1.000000000000000000, 0.000000000000000000 ) ) ;
#85120=CIRCLE ( 'NONE', #6310, 2.500000000000000888 ) ;
#85141=ORIENTED_EDGE ( 'NONE', *, *, #71450, .F. ) ;
#85172=LINE ( 'NONE', #120646, #90924 ) ;
#85193=ADVANCED_FACE ( 'NONE', ( #129031 ), #28239, .T. ) ;
#85241=EDGE_CURVE ( 'NONE', #76159, #104096, #73253, .T. ) ;
#85262=ORIENTED_EDGE ( 'NONE', *, *, #21271, .T. ) ;
#85275=DIRECTION ( 'NONE',  ( -1.000000000000000000, -0.000000000000000000, -0.000000000000000000 ) ) ;
#85279=DIRECTION ( 'NONE',  ( 0.000000000000000000, -1.000000000000000000, 0.000000000000000000 ) ) ;
#85290=PRESENTATION_STYLE_ASSIGNMENT (( #107059 ) ) ;
#85293=VERTEX_POINT ( 'NONE', #39930 ) ;
#85300=ORIENTED_EDGE ( 'NONE', *, *, #55099, .F. ) ;
#85310=VERTEX_POINT ( 'NONE', #29706 ) ;
#85312=CARTESIAN_POINT ( 'NONE',  ( 11.62000000000000099, 9.521314400968980422E-16, 0.000000000000000000 ) ) ;
#85315=CARTESIAN_POINT ( 'NONE',  ( 23.63159235450331863, 9.902892378096218942E-16, 0.000000000000000000 ) ) ;
#85449=CIRCLE ( 'NONE', #127162, 2.500000000000000888 ) ;
#85475=DIRECTION ( 'NONE',  ( 0.000000000000000000, -1.000000000000000000, 0.000000000000000000 ) ) ;
#85520=CARTESIAN_POINT ( 'NONE',  ( 21.29159235450332233, -3.851859888774471706E-31, 2.500000000000001332 ) ) ;
#85589=DIRECTION ( 'NONE',  ( 0.5735764363510451602, 0.8191520442889924647, 0.000000000000000000 ) ) ;
#85594=DIRECTION ( 'NONE',  ( 0.000000000000000000, -1.000000000000000000, 0.000000000000000000 ) ) ;
#85600=DIRECTION ( 'NONE',  ( -0.5735764363510507113, 0.8191520442889885789, 1.003171929053520926E-16 ) ) ;
#85605=FACE_OUTER_BOUND ( 'NONE', #21223, .T. ) ;
#85613=CARTESIAN_POINT ( 'NONE',  ( 13.49159235450332162, -2.500000000000000444, 3.061616997868384620E-16 ) ) ;
#85645=CIRCLE ( 'NONE', #50906, 2.500000000000000888 ) ;
#85661=CARTESIAN_POINT ( 'NONE',  ( -25.39999999999996305, 3.061616997868383141E-16, -2.500000000000000000 ) ) ;
#85701=LINE ( 'NONE', #129946, #137567 ) ;
#85723=AXIS2_PLACEMENT_3D ( 'NONE', #61786, #118259, #107400 ) ;
#85757=CIRCLE ( 'NONE', #104260, 2.500000000000000888 ) ;
#85764=AXIS2_PLACEMENT_3D ( 'NONE', #62600, #95206, #73477 ) ;
#85852=VERTEX_POINT ( 'NONE', #120838 ) ;
#85870=CARTESIAN_POINT ( 'NONE',  ( 8.500000000000000000, 9.521314400968980422E-16, 0.000000000000000000 ) ) ;
#85918=AXIS2_PLACEMENT_3D ( 'NONE', #79064, #123268, #23939 ) ;
#85970=CARTESIAN_POINT ( 'NONE',  ( 5.691592354503320905, 3.061616997868380183E-16, -2.500000000000001332 ) ) ;
#85973=ORIENTED_EDGE ( 'NONE', *, *, #1508, .F. ) ;
#85982=ORIENTED_EDGE ( 'NONE', *, *, #54447, .F. ) ;
#85983=CIRCLE ( 'NONE', #39750, 2.500000000000000888 ) ;
#86010=ORIENTED_EDGE ( 'NONE', *, *, #100693, .T. ) ;
#86013=FACE_OUTER_BOUND ( 'NONE', #3309, .T. ) ;
#86057=EDGE_LOOP ( 'NONE', ( #3913, #120458, #7521, #8745, #142881, #18882 ) ) ;
#86085=AXIS2_PLACEMENT_3D ( 'NONE', #135647, #92114, #125488 ) ;
#86104=AXIS2_PLACEMENT_3D ( 'NONE', #107893, #8561, #52807 ) ;
#86127=EDGE_CURVE ( 'NONE', #82762, #21344, #19229, .T. ) ;
#86157=DIRECTION ( 'NONE',  ( 0.000000000000000000, 0.000000000000000000, 1.000000000000000000 ) ) ;
#86176=ORIENTED_EDGE ( 'NONE', *, *, #142033, .F. ) ;
#86231=EDGE_CURVE ( 'NONE', #64832, #42322, #95586, .T. ) ;
#86236=VERTEX_POINT ( 'NONE', #77211 ) ;
#86251=AXIS2_PLACEMENT_3D ( 'NONE', #94121, #73128, #93431 ) ;
#86259=CARTESIAN_POINT ( 'NONE',  ( 25.19159235450331735, 2.500000000000001776, 0.000000000000000000 ) ) ;
#86275=DIRECTION ( 'NONE',  ( -1.000000000000000000, -1.224606353822377258E-16, -0.000000000000000000 ) ) ;
#86297=DIRECTION ( 'NONE',  ( 0.000000000000000000, -1.000000000000000000, 0.000000000000000000 ) ) ;
#86342=LINE ( 'NONE', #130560, #120395 ) ;
#86392=DIRECTION ( 'NONE',  ( 0.000000000000000000, -1.000000000000000000, 0.000000000000000000 ) ) ;
#86435=ORIENTED_EDGE ( 'NONE', *, *, #114929, .F. ) ;
#86459=VECTOR ( 'NONE', #139813, 1000.000000000000000 ) ;
#86524=AXIS2_PLACEMENT_3D ( 'NONE', #63105, #74687, #40618 ) ;
#86539=DIRECTION ( 'NONE',  ( 0.000000000000000000, -1.000000000000000000, 0.000000000000000000 ) ) ;
#86543=CARTESIAN_POINT ( 'NONE',  ( 24.41159235450331977, 9.902892378096218942E-16, 0.000000000000000000 ) ) ;
#86547=EDGE_LOOP ( 'NONE', ( #143433, #18571, #45385, #34596, #115568 ) ) ;
#86550=ORIENTED_EDGE ( 'NONE', *, *, #82617, .T. ) ;
#86601=AXIS2_PLACEMENT_3D ( 'NONE', #140800, #55250, #52375 ) ;
#86649=CARTESIAN_POINT ( 'NONE',  ( 15.98840764549667703, 3.061616997868380183E-16, -2.500000000000001332 ) ) ;
#86700=ORIENTED_EDGE ( 'NONE', *, *, #92613, .F. ) ;
#86703=AXIS2_PLACEMENT_3D ( 'NONE', #99490, #56053, #90056 ) ;
#86722=CARTESIAN_POINT ( 'NONE',  ( 2.999999999999999112, 0.000000000000000000, -4.750000000000000000 ) ) ;
#86735=CARTESIAN_POINT ( 'NONE',  ( 10.37159235450332062, 9.902892378096218942E-16, 0.000000000000000000 ) ) ;
#86747=ORIENTED_EDGE ( 'NONE', *, *, #65939, .T. ) ;
#86756=CARTESIAN_POINT ( 'NONE',  ( 0.4425134659199910780, -0.6000000000000000888, 4.147378741781976075 ) ) ;
#86778=FACE_OUTER_BOUND ( 'NONE', #58999, .T. ) ;
#86782=VERTEX_POINT ( 'NONE', #43129 ) ;
#86795=ORIENTED_EDGE ( 'NONE', *, *, #127643, .F. ) ;
#86800=DIRECTION ( 'NONE',  ( -1.000000000000000000, -1.224606353822377258E-16, -0.000000000000000000 ) ) ;
#86828=DIRECTION ( 'NONE',  ( -1.000000000000000000, -1.224606353822377258E-16, -0.000000000000000000 ) ) ;
#86854=EDGE_CURVE ( 'NONE', #15339, #9148, #111961, .T. ) ;
#86884=ADVANCED_FACE ( 'NONE', ( #13313 ), #17051, .T. ) ;
#86891=AXIS2_PLACEMENT_3D ( 'NONE', #72133, #16996, #54632 ) ;
#86908=CARTESIAN_POINT ( 'NONE',  ( 0.4414465083558353209, 0.5999999999999986455, -4.146294842461982100 ) ) ;
#86920=CIRCLE ( 'NONE', #107700, 2.500000000000000888 ) ;
#86923=CIRCLE ( 'NONE', #80023, 2.500000000000000888 ) ;
#86937=DIRECTION ( 'NONE',  ( 1.000000000000000000, 1.224606353822377258E-16, 0.000000000000000000 ) ) ;
#86949=DIRECTION ( 'NONE',  ( 0.000000000000000000, -1.000000000000000000, 0.000000000000000000 ) ) ;
#86964=ORIENTED_EDGE ( 'NONE', *, *, #52238, .T. ) ;
#86973=DIRECTION ( 'NONE',  ( 0.000000000000000000, -1.000000000000000000, 0.000000000000000000 ) ) ;
#86981=CARTESIAN_POINT ( 'NONE',  ( 17.54840764549667398, 9.139736423841732040E-16, 0.000000000000000000 ) ) ;
#86989=CARTESIAN_POINT ( 'NONE',  ( 24.41159235450331977, -2.500000000000000444, 3.061616997868384620E-16 ) ) ;
#87017=DIRECTION ( 'NONE',  ( -0.5735764363510507113, 0.8191520442889885789, 1.003171929053520926E-16 ) ) ;
#87065=AXIS2_PLACEMENT_3D ( 'NONE', #23931, #133412, #12317 ) ;
#87092=EDGE_CURVE ( 'NONE', #125050, #42229, #125926, .T. ) ;
#87097=DIRECTION ( 'NONE',  ( -1.000000000000000000, -1.224606353822377258E-16, -0.000000000000000000 ) ) ;
#87136=ORIENTED_EDGE ( 'NONE', *, *, #8974, .T. ) ;
#87187=CONICAL_SURFACE ( 'NONE', #135738, 2.500000000000000888, 0.9599310885968822538 ) ;
#87235=CARTESIAN_POINT ( 'NONE',  ( 27.68840764549667455, 9.139736423841732040E-16, 0.000000000000000000 ) ) ;
#87251=EDGE_LOOP ( 'NONE', ( #30563, #95490, #43729, #34, #42624, #133720 ) ) ;
#87301=EDGE_CURVE ( 'NONE', #40245, #4422, #54138, .T. ) ;
#87340=DIRECTION ( 'NONE',  ( 0.000000000000000000, 0.000000000000000000, 1.000000000000000000 ) ) ;
#87372=CYLINDRICAL_SURFACE ( 'NONE', #125713, 2.500000000000000000 ) ;
#87382=FACE_OUTER_BOUND ( 'NONE', #136601, .T. ) ;
#87391=EDGE_CURVE ( 'NONE', #96831, #64517, #28657, .T. ) ;
#87397=VERTEX_POINT ( 'NONE', #37057 ) ;
#87401=DIRECTION ( 'NONE',  ( 0.000000000000000000, -1.000000000000000000, 0.000000000000000000 ) ) ;
#87423=CIRCLE ( 'NONE', #6644, 2.500000000000000888 ) ;
#87428=CARTESIAN_POINT ( 'NONE',  ( 20.66840764549667497, -2.499999999999996003, 0.000000000000000000 ) ) ;
#87430=ORIENTED_EDGE ( 'NONE', *, *, #33628, .T. ) ;
#87506=AXIS2_PLACEMENT_3D ( 'NONE', #108213, #34271, #109681 ) ;
#87542=VERTEX_POINT ( 'NONE', #86989 ) ;
#87582=LINE ( 'NONE', #55686, #23264 ) ;
#87621=VECTOR ( 'NONE', #141514, 1000.000000000000000 ) ;
#87637=DIRECTION ( 'NONE',  ( 0.000000000000000000, -1.000000000000000000, 0.000000000000000000 ) ) ;
#87663=EDGE_CURVE ( 'NONE', #92828, #97144, #22417, .T. ) ;
#87716=CIRCLE ( 'NONE', #22898, 2.500000000000000888 ) ;
#87721=EDGE_CURVE ( 'NONE', #1792, #115214, #33441, .T. ) ;
#87727=AXIS2_PLACEMENT_3D ( 'NONE', #10319, #53105, #21208 ) ;
#87777=VECTOR ( 'NONE', #8593, 1000.000000000000000 ) ;
#87817=DIRECTION ( 'NONE',  ( 0.5735764363510451602, 0.8191520442889924647, 0.000000000000000000 ) ) ;
#87819=EDGE_LOOP ( 'NONE', ( #142375, #77846, #22852, #64372, #41522, #51627 ) ) ;
#87849=AXIS2_PLACEMENT_3D ( 'NONE', #17486, #118211, #61742 ) ;
#87854=DIRECTION ( 'NONE',  ( -1.000000000000000000, -1.224606353822377258E-16, -0.000000000000000000 ) ) ;
#87921=ORIENTED_EDGE ( 'NONE', *, *, #131677, .F. ) ;
#87929=FACE_BOUND ( 'NONE', #81654, .T. ) ;
#87934=ORIENTED_EDGE ( 'NONE', *, *, #143335, .T. ) ;
#87975=VERTEX_POINT ( 'NONE', #109279 ) ;
#88006=ADVANCED_FACE ( 'NONE', ( #9956 ), #67208, .T. ) ;
#88012=EDGE_CURVE ( 'NONE', #100733, #108418, #5628, .T. ) ;
#88013=AXIS2_PLACEMENT_3D ( 'NONE', #107811, #91108, #92486 ) ;
#88078=CARTESIAN_POINT ( 'NONE',  ( 25.65999999999999659, -2.055000000000000160, 0.000000000000000000 ) ) ;
#88094=ORIENTED_EDGE ( 'NONE', *, *, #22221, .T. ) ;
#88107=DIRECTION ( 'NONE',  ( -1.000000000000000000, -1.224606353822377258E-16, -0.000000000000000000 ) ) ;
#88126=CONICAL_SURFACE ( 'NONE', #104336, 2.500000000000000888, 0.9599310885968822538 ) ;
#88168=AXIS2_PLACEMENT_3D ( 'NONE', #108046, #131265, #8713 ) ;
#88169=CARTESIAN_POINT ( 'NONE',  ( 12.08840764549667668, 9.139736423841732040E-16, 0.000000000000000000 ) ) ;
#88214=ADVANCED_FACE ( 'NONE', ( #25837 ), #13507, .T. ) ;
#88219=VERTEX_POINT ( 'NONE', #104085 ) ;
#88261=ADVANCED_FACE ( 'NONE', ( #38164 ), #109868, .T. ) ;
#88269=CIRCLE ( 'NONE', #44306, 2.500000000000000888 ) ;
#88311=CYLINDRICAL_SURFACE ( 'NONE', #11781, 2.500000000000000000 ) ;
#88315=DIRECTION ( 'NONE',  ( 0.000000000000000000, 0.000000000000000000, -1.000000000000000000 ) ) ;
#88318=CARTESIAN_POINT ( 'NONE',  ( -25.39999999999996305, 3.061616997868383141E-16, -2.500000000000000000 ) ) ;
#88320=AXIS2_PLACEMENT_3D ( 'NONE', #117478, #116067, #93623 ) ;
#88345=DIRECTION ( 'NONE',  ( 0.000000000000000000, 0.000000000000000000, 1.000000000000000000 ) ) ;
#88381=ORIENTED_EDGE ( 'NONE', *, *, #132767, .F. ) ;
#88389=ORIENTED_EDGE ( 'NONE', *, *, #128334, .T. ) ;
#88396=DIRECTION ( 'NONE',  ( -1.000000000000000000, -1.224606353822377258E-16, -0.000000000000000000 ) ) ;
#88398=VECTOR ( 'NONE', #10201, 1000.000000000000114 ) ;
#88506=AXIS2_PLACEMENT_3D ( 'NONE', #36264, #4260, #124688 ) ;
#88511=FACE_OUTER_BOUND ( 'NONE', #63237, .T. ) ;
#88563=SURFACE_SIDE_STYLE ('',( #2767 ) ) ;
#88564=ORIENTED_EDGE ( 'NONE', *, *, #25611, .T. ) ;
#88599=FACE_OUTER_BOUND ( 'NONE', #119241, .T. ) ;
#88653=DIRECTION ( 'NONE',  ( 0.000000000000000000, 0.000000000000000000, 1.000000000000000000 ) ) ;
#88690=CARTESIAN_POINT ( 'NONE',  ( 26.12840764549667583, -2.499999999999996003, 0.000000000000000000 ) ) ;
#88703=AXIS2_PLACEMENT_3D ( 'NONE', #134828, #34782, #66002 ) ;
#88718=EDGE_CURVE ( 'NONE', #52993, #98020, #47520, .T. ) ;
#88735=DIRECTION ( 'NONE',  ( -1.000000000000000000, -1.224606353822377258E-16, -0.000000000000000000 ) ) ;
#88744=CARTESIAN_POINT ( 'NONE',  ( 20.66840764549667497, 9.139736423841732040E-16, 0.000000000000000000 ) ) ;
#88747=AXIS2_PLACEMENT_3D ( 'NONE', #35639, #79870, #10956 ) ;
#88755=MECHANICAL_DESIGN_GEOMETRIC_PRESENTATION_REPRESENTATION('',(#35479),#44707);
#88782=DIRECTION ( 'NONE',  ( 0.000000000000000000, 1.000000000000000000, 0.000000000000000000 ) ) ;
#88833=ORIENTED_EDGE ( 'NONE', *, *, #121392, .T. ) ;
#88903=CARTESIAN_POINT ( 'NONE',  ( 7.408407645496676963, -1.925929944387235853E-31, 2.500000000000001332 ) ) ;
#88962=DIRECTION ( 'NONE',  ( -1.000000000000000000, -1.224606353822377258E-16, -0.000000000000000000 ) ) ;
#88963=EDGE_CURVE ( 'NONE', #114079, #47703, #52121, .T. ) ;
#88966=VERTEX_POINT ( 'NONE', #83277 ) ;
#89019=CARTESIAN_POINT ( 'NONE',  ( 0.000000000000000000, -0.5999999999999994227, -3.054668707061620747 ) ) ;
#89051=ORIENTED_EDGE ( 'NONE', *, *, #88963, .F. ) ;
#89089=DIRECTION ( 'NONE',  ( 0.000000000000000000, -1.000000000000000000, 0.000000000000000000 ) ) ;
#89117=CARTESIAN_POINT ( 'NONE',  ( 19.88840764549667384, 9.139736423841732040E-16, 0.000000000000000000 ) ) ;
#89123=EDGE_LOOP ( 'NONE', ( #95988, #123335, #101556, #7542, #41050, #74999 ) ) ;
#89198=CARTESIAN_POINT ( 'NONE',  ( 8.968407645496675684, 9.139736423841732040E-16, 0.000000000000000000 ) ) ;
#89210=VECTOR ( 'NONE', #117599, 1000.000000000000000 ) ;
#89228=DIRECTION ( 'NONE',  ( 1.000000000000000000, 1.224606353822377258E-16, 0.000000000000000000 ) ) ;
#89231=EDGE_CURVE ( 'NONE', #17414, #16132, #119056, .T. ) ;
#89251=CARTESIAN_POINT ( 'NONE',  ( 18.32840764549667512, 9.139736423841732040E-16, 0.000000000000000000 ) ) ;
#89258=CIRCLE ( 'NONE', #79991, 2.055000000000001048 ) ;
#89346=CYLINDRICAL_SURFACE ( 'NONE', #62891, 2.500000000000000000 ) ;
#89401=CARTESIAN_POINT ( 'NONE',  ( 8.031592354503320763, 9.902892378096218942E-16, 0.000000000000000000 ) ) ;
#89486=CIRCLE ( 'NONE', #66431, 2.500000000000000888 ) ;
#89494=DIRECTION ( 'NONE',  ( 0.000000000000000000, -1.000000000000000000, 0.000000000000000000 ) ) ;
#89499=UNCERTAINTY_MEASURE_WITH_UNIT (LENGTH_MEASURE( 1.000000000000000082E-05 ), #92601, 'distance_accuracy_value', 'NONE');
#89526=DIRECTION ( 'NONE',  ( 0.000000000000000000, 0.000000000000000000, 1.000000000000000000 ) ) ;
#89554=DIRECTION ( 'NONE',  ( 0.000000000000000000, -1.000000000000000000, 0.000000000000000000 ) ) ;
#89568=CARTESIAN_POINT ( 'NONE',  ( -25.39999999999996305, 0.000000000000000000, 0.000000000000000000 ) ) ;
#89589=CIRCLE ( 'NONE', #117302, 2.500000000000000888 ) ;
#89596=CONICAL_SURFACE ( 'NONE', #84952, 2.055000000000001048, 0.9599310885968758145 ) ;
#89624=CONICAL_SURFACE ( 'NONE', #17781, 2.500000000000000888, 0.9599310885968822538 ) ;
#89651=ADVANCED_FACE ( 'NONE', ( #22110 ), #12665, .T. ) ;
#89672=DIRECTION ( 'NONE',  ( 0.000000000000000000, -1.000000000000000000, 0.000000000000000000 ) ) ;
#89673=EDGE_CURVE ( 'NONE', #72349, #91883, #19610, .T. ) ;
#89702=CARTESIAN_POINT ( 'NONE',  ( 14.74000000000000021, 9.521314400968980422E-16, 0.000000000000000000 ) ) ;
#89703=CONICAL_SURFACE ( 'NONE', #45759, 2.500000000000000888, 0.9599310885968822538 ) ;
#89714=CYLINDRICAL_SURFACE ( 'NONE', #108087, 2.500000000000000000 ) ;
#89730=ORIENTED_EDGE ( 'NONE', *, *, #44364, .F. ) ;
#89891=CARTESIAN_POINT ( 'NONE',  ( 4.911592354503321545, 9.902892378096218942E-16, 0.000000000000000000 ) ) ;
#89914=AXIS2_PLACEMENT_3D ( 'NONE', #133331, #2041, #55057 ) ;
#89934=DIRECTION ( 'NONE',  ( 0.5735764363510453823, -0.8191520442889923537, 1.003171929053525486E-16 ) ) ;
#89995=DIRECTION ( 'NONE',  ( 0.000000000000000000, -1.000000000000000000, 0.000000000000000000 ) ) ;
#90013=DIRECTION ( 'NONE',  ( 1.000000000000000000, 1.224606353822377258E-16, 0.000000000000000000 ) ) ;
#90034=EDGE_LOOP ( 'NONE', ( #140452, #46242, #99740, #49859, #107690, #14429 ) ) ;
#90056=DIRECTION ( 'NONE',  ( 0.000000000000000000, 0.000000000000000000, 1.000000000000000000 ) ) ;
#90091=EDGE_CURVE ( 'NONE', #75313, #97144, #112249, .T. ) ;
#90111=ADVANCED_FACE ( 'NONE', ( #32863 ), #55316, .T. ) ;
#90159=ORIENTED_EDGE ( 'NONE', *, *, #122059, .T. ) ;
#90188=LINE ( 'NONE', #110492, #79259 ) ;
#90228=VECTOR ( 'NONE', #59394, 999.9999999999998863 ) ;
#90248=DIRECTION ( 'NONE',  ( -1.000000000000000000, -1.224606353822377258E-16, -0.000000000000000000 ) ) ;
#90257=CARTESIAN_POINT ( 'NONE',  ( -25.39999999999996305, 0.000000000000000000, 0.000000000000000000 ) ) ;
#90258=ORIENTED_EDGE ( 'NONE', *, *, #74694, .F. ) ;
#90273=LINE ( 'NONE', #79466, #15449 ) ;
#90291=LINE ( 'NONE', #134545, #114980 ) ;
#90319=AXIS2_PLACEMENT_3D ( 'NONE', #43894, #88107, #132357 ) ;
#90322=AXIS2_PLACEMENT_3D ( 'NONE', #28724, #83835, #127292 ) ;
#90328=EDGE_CURVE ( 'NONE', #35419, #27726, #47514, .T. ) ;
#90333=ORIENTED_EDGE ( 'NONE', *, *, #132277, .F. ) ;
#90378=DIRECTION ( 'NONE',  ( 1.000000000000000000, -0.000000000000000000, -0.000000000000000000 ) ) ;
#90385=LINE ( 'NONE', #3353, #29883 ) ;
#90426=AXIS2_PLACEMENT_3D ( 'NONE', #34899, #24708, #112444 ) ;
#90453=VERTEX_POINT ( 'NONE', #33929 ) ;
#90494=AXIS2_PLACEMENT_3D ( 'NONE', #60297, #49430, #1738 ) ;
#90505=CIRCLE ( 'NONE', #72012, 2.500000000000000888 ) ;
#90540=DIRECTION ( 'NONE',  ( -1.000000000000000000, -1.224606353822377258E-16, -0.000000000000000000 ) ) ;
#90588=FACE_OUTER_BOUND ( 'NONE', #107968, .T. ) ;
#90602=CYLINDRICAL_SURFACE ( 'NONE', #18969, 2.500000000000000000 ) ;
#90685=CARTESIAN_POINT ( 'NONE',  ( 25.65999999999999659, 2.055000000000001492, 2.516649172247811554E-16 ) ) ;
#90686=ORIENTED_EDGE ( 'NONE', *, *, #90328, .F. ) ;
#90705=DIRECTION ( 'NONE',  ( -1.000000000000000000, -1.224606353822377258E-16, -0.000000000000000000 ) ) ;
#90718=EDGE_CURVE ( 'NONE', #1660, #125050, #23593, .T. ) ;
#90721=ORIENTED_EDGE ( 'NONE', *, *, #137632, .F. ) ;
#90738=EDGE_CURVE ( 'NONE', #103631, #76159, #35990, .T. ) ;
#90772=DIRECTION ( 'NONE',  ( -1.000000000000000000, 0.000000000000000000, -0.000000000000000000 ) ) ;
#90786=VERTEX_POINT ( 'NONE', #111302 ) ;
#90806=CONICAL_SURFACE ( 'NONE', #28288, 2.055000000000001048, 0.9599310885968758145 ) ;
#90835=AXIS2_PLACEMENT_3D ( 'NONE', #64229, #110552, #77969 ) ;
#90836=CONICAL_SURFACE ( 'NONE', #46890, 2.055000000000001048, 0.9599310885968758145 ) ;
#90890=VECTOR ( 'NONE', #73670, 1000.000000000000000 ) ;
#90897=CARTESIAN_POINT ( 'NONE',  ( 6.160000000000001030, 2.055000000000001492, 2.516649172247811554E-16 ) ) ;
#90924=VECTOR ( 'NONE', #139607, 1000.000000000000000 ) ;
#90962=AXIS2_PLACEMENT_3D ( 'NONE', #109075, #78614, #54036 ) ;
#90967=DIRECTION ( 'NONE',  ( -1.000000000000000000, -1.224606353822377258E-16, -0.000000000000000000 ) ) ;
#90968=AXIS2_PLACEMENT_3D ( 'NONE', #115012, #15690, #59974 ) ;
#90981=AXIS2_PLACEMENT_3D ( 'NONE', #103731, #81324, #137836 ) ;
#91029=VERTEX_POINT ( 'NONE', #96659 ) ;
#91049=DIRECTION ( 'NONE',  ( 0.000000000000000000, -1.000000000000000000, 0.000000000000000000 ) ) ;
#91064=DIRECTION ( 'NONE',  ( 0.000000000000000000, -1.000000000000000000, 0.000000000000000000 ) ) ;
#91065=CARTESIAN_POINT ( 'NONE',  ( 18.17159235450331778, 9.902892378096218942E-16, 0.000000000000000000 ) ) ;
#91098=CARTESIAN_POINT ( 'NONE',  ( -25.39999999999996305, 3.061616997868383141E-16, -2.500000000000000000 ) ) ;
#91106=CARTESIAN_POINT ( 'NONE',  ( 11.30840764549667554, -3.851859888774471706E-31, 2.500000000000001332 ) ) ;
#91107=EDGE_CURVE ( 'NONE', #76586, #81442, #107853, .T. ) ;
#91108=DIRECTION ( 'NONE',  ( 1.000000000000000000, 0.000000000000000000, 0.000000000000000000 ) ) ;
#91180=DIRECTION ( 'NONE',  ( 0.5735764363510453823, -0.8191520442889923537, 1.003171929053525486E-16 ) ) ;
#91193=CARTESIAN_POINT ( 'NONE',  ( 17.39159235450332019, -2.500000000000000000, 3.061616997868384127E-16 ) ) ;
#91204=EDGE_CURVE ( 'NONE', #59763, #109094, #45417, .T. ) ;
#91212=DIRECTION ( 'NONE',  ( 0.000000000000000000, -1.000000000000000000, 0.000000000000000000 ) ) ;
#91223=DIRECTION ( 'NONE',  ( 0.000000000000000000, -1.000000000000000000, 0.000000000000000000 ) ) ;
#91227=LINE ( 'NONE', #23048, #75158 ) ;
#91267=ADVANCED_FACE ( 'NONE', ( #71771 ), #94005, .T. ) ;
#91283=LINE ( 'NONE', #59370, #136644 ) ;
#91296=ORIENTED_EDGE ( 'NONE', *, *, #40405, .T. ) ;
#91349=ADVANCED_FACE ( 'NONE', ( #9292 ), #110064, .T. ) ;
#91426=EDGE_LOOP ( 'NONE', ( #23895, #91296, #71761, #41609, #38159 ) ) ;
#91469=DIRECTION ( 'NONE',  ( 1.000000000000000000, 1.224606353822377258E-16, 0.000000000000000000 ) ) ;
#91474=EDGE_CURVE ( 'NONE', #29352, #43087, #128785, .T. ) ;
#91486=EDGE_CURVE ( 'NONE', #33609, #132528, #44887, .T. ) ;
#91494=EDGE_CURVE ( 'NONE', #50481, #52944, #114882, .T. ) ;
#91498=EDGE_CURVE ( 'NONE', #40538, #78627, #25204, .T. ) ;
#91562=LINE ( 'NONE', #135097, #114072 ) ;
#91564=EDGE_CURVE ( 'NONE', #68485, #106451, #112933, .T. ) ;
#91604=ADVANCED_FACE ( 'NONE', ( #117192 ), #87187, .T. ) ;
#91605=ORIENTED_EDGE ( 'NONE', *, *, #115481, .F. ) ;
#91663=CARTESIAN_POINT ( 'NONE',  ( 9.591592354503321260, -5.777789833161707559E-31, 2.500000000000001332 ) ) ;
#91675=VECTOR ( 'NONE', #97932, 1000.000000000000000 ) ;
#91739=EDGE_LOOP ( 'NONE', ( #124192, #52695, #10177, #12315, #138392 ) ) ;
#91753=VERTEX_POINT ( 'NONE', #118644 ) ;
#91768=CARTESIAN_POINT ( 'NONE',  ( -25.39999999999996305, 0.000000000000000000, 2.500000000000000000 ) ) ;
#91832=ORIENTED_EDGE ( 'NONE', *, *, #61867, .T. ) ;
#91850=ORIENTED_EDGE ( 'NONE', *, *, #111540, .T. ) ;
#91851=CARTESIAN_POINT ( 'NONE',  ( 6.471592354503322042, -2.500000000000000000, 3.061616997868384127E-16 ) ) ;
#91865=AXIS2_PLACEMENT_3D ( 'NONE', #97342, #42309, #75636 ) ;
#91876=AXIS2_PLACEMENT_3D ( 'NONE', #63382, #6061, #97363 ) ;
#91883=VERTEX_POINT ( 'NONE', #88903 ) ;
#91895=CIRCLE ( 'NONE', #124295, 2.500000000000000888 ) ;
#91908=DIRECTION ( 'NONE',  ( -1.000000000000000000, -1.224606353822377258E-16, -0.000000000000000000 ) ) ;
#91914=CARTESIAN_POINT ( 'NONE',  ( 15.52000000000000135, -2.055000000000000160, 0.000000000000000000 ) ) ;
#91935=EDGE_CURVE ( 'NONE', #85852, #3387, #90291, .T. ) ;
#91942=CARTESIAN_POINT ( 'NONE',  ( 8.968407645496675684, -1.925929944387235853E-31, 2.500000000000001332 ) ) ;
#91981=FACE_OUTER_BOUND ( 'NONE', #140043, .T. ) ;
#91999=ADVANCED_FACE ( 'NONE', ( #139554 ), #25753, .T. ) ;
#92028=FACE_OUTER_BOUND ( 'NONE', #42457, .T. ) ;
#92038=AXIS2_PLACEMENT_3D ( 'NONE', #27534, #114552, #137764 ) ;
#92062=DIRECTION ( 'NONE',  ( 0.000000000000000000, -1.000000000000000000, 0.000000000000000000 ) ) ;
#92064=EDGE_CURVE ( 'NONE', #124621, #36267, #84914, .T. ) ;
#92092=ORIENTED_EDGE ( 'NONE', *, *, #10344, .T. ) ;
#92114=DIRECTION ( 'NONE',  ( -1.000000000000000000, -1.224606353822377258E-16, -0.000000000000000000 ) ) ;
#92130=ORIENTED_EDGE ( 'NONE', *, *, #102059, .F. ) ;
#92132=CARTESIAN_POINT ( 'NONE',  ( 18.17159235450331778, 9.902892378096218942E-16, 0.000000000000000000 ) ) ;
#92157=EDGE_CURVE ( 'NONE', #82012, #101812, #52510, .T. ) ;
#92163=DIRECTION ( 'NONE',  ( -1.000000000000000000, -1.224606353822377258E-16, -0.000000000000000000 ) ) ;
#92166=DIRECTION ( 'NONE',  ( -1.000000000000000000, -0.000000000000000000, -0.000000000000000000 ) ) ;
#92179=DIRECTION ( 'NONE',  ( 0.000000000000000000, 0.000000000000000000, 1.000000000000000000 ) ) ;
#92199=VERTEX_POINT ( 'NONE', #32186 ) ;
#92277=ORIENTED_EDGE ( 'NONE', *, *, #104858, .T. ) ;
#92315=FACE_OUTER_BOUND ( 'NONE', #71020, .T. ) ;
#92332=DIRECTION ( 'NONE',  ( -1.000000000000000000, -1.224606353822377258E-16, -0.000000000000000000 ) ) ;
#92382=CARTESIAN_POINT ( 'NONE',  ( 1.199999999999999956, 0.000000000000000000, 0.000000000000000000 ) ) ;
#92421=EDGE_CURVE ( 'NONE', #67571, #92905, #124428, .T. ) ;
#92438=AXIS2_PLACEMENT_3D ( 'NONE', #117193, #27336, #17871 ) ;
#92474=ORIENTED_EDGE ( 'NONE', *, *, #73746, .T. ) ;
#92486=DIRECTION ( 'NONE',  ( 0.000000000000000000, 0.000000000000000000, 1.000000000000000000 ) ) ;
#92490=ORIENTED_EDGE ( 'NONE', *, *, #78847, .F. ) ;
#92501=CARTESIAN_POINT ( 'NONE',  ( 17.85999999999999943, 9.521314400968980422E-16, 0.000000000000000000 ) ) ;
#92509=CARTESIAN_POINT ( 'NONE',  ( 9.279999999999999361, 9.521314400968980422E-16, 0.000000000000000000 ) ) ;
#92512=DIRECTION ( 'NONE',  ( -0.5735764363510507113, 0.8191520442889885789, 1.003171929053520926E-16 ) ) ;
#92518=CARTESIAN_POINT ( 'NONE',  ( 9.279999999999999361, 9.521314400968980422E-16, 0.000000000000000000 ) ) ;
#92522=CARTESIAN_POINT ( 'NONE',  ( 24.09999999999999787, 2.055000000000001492, 0.000000000000000000 ) ) ;
#92552=LINE ( 'NONE', #28042, #55762 ) ;
#92557=EDGE_LOOP ( 'NONE', ( #66999, #12764, #112083, #124221, #65391 ) ) ;
#92599=LINE ( 'NONE', #19862, #99832 ) ;
#92601=( LENGTH_UNIT ( ) NAMED_UNIT ( * ) SI_UNIT ( .MILLI., .METRE. ) );
#92613=EDGE_CURVE ( 'NONE', #9860, #118163, #40068, .T. ) ;
#92629=AXIS2_PLACEMENT_3D ( 'NONE', #28737, #17813, #40338 ) ;
#92646=ADVANCED_FACE ( 'NONE', ( #23992 ), #111716, .T. ) ;
#92711=DIRECTION ( 'NONE',  ( 0.000000000000000000, 0.000000000000000000, 1.000000000000000000 ) ) ;
#92721=ORIENTED_EDGE ( 'NONE', *, *, #110071, .T. ) ;
#92730=CARTESIAN_POINT ( 'NONE',  ( 19.73159235450332005, 9.902892378096218942E-16, 0.000000000000000000 ) ) ;
#92741=FACE_OUTER_BOUND ( 'NONE', #124333, .T. ) ;
#92763=VECTOR ( 'NONE', #103892, 1000.000000000000000 ) ;
#92777=EDGE_CURVE ( 'NONE', #86782, #114073, #10979, .T. ) ;
#92778=ORIENTED_EDGE ( 'NONE', *, *, #38022, .T. ) ;
#92798=DIRECTION ( 'NONE',  ( -1.000000000000000000, -1.224606353822377258E-16, -0.000000000000000000 ) ) ;
#92819=CARTESIAN_POINT ( 'NONE',  ( -25.39999999999996305, 0.000000000000000000, 2.500000000000000000 ) ) ;
#92822=CIRCLE ( 'NONE', #111339, 2.500000000000000888 ) ;
#92828=VERTEX_POINT ( 'NONE', #94229 ) ;
#92840=CARTESIAN_POINT ( 'NONE',  ( -25.39999999999996305, 0.000000000000000000, 2.500000000000000000 ) ) ;
#92885=CARTESIAN_POINT ( 'NONE',  ( 25.19159235450331735, 3.061616997868380183E-16, -2.500000000000001332 ) ) ;
#92905=VERTEX_POINT ( 'NONE', #103653 ) ;
#92957=ORIENTED_EDGE ( 'NONE', *, *, #121556, .F. ) ;
#92968=LINE ( 'NONE', #102444, #64960 ) ;
#92977=CIRCLE ( 'NONE', #130026, 2.500000000000000888 ) ;
#93019=ORIENTED_EDGE ( 'NONE', *, *, #60483, .F. ) ;
#93039=EDGE_LOOP ( 'NONE', ( #114958, #125443, #10227, #64309, #124194 ) ) ;
#93067=CARTESIAN_POINT ( 'NONE',  ( 22.85159235450332105, -2.500000000000000000, 3.061616997868384127E-16 ) ) ;
#93099=CARTESIAN_POINT ( 'NONE',  ( 18.32840764549667512, -3.851859888774471706E-31, 2.500000000000001332 ) ) ;
#93111=VERTEX_POINT ( 'NONE', #111346 ) ;
#93190=ORIENTED_EDGE ( 'NONE', *, *, #23338, .F. ) ;
#93234=DIRECTION ( 'NONE',  ( -1.000000000000000000, -1.224606353822377258E-16, -0.000000000000000000 ) ) ;
#93253=CARTESIAN_POINT ( 'NONE',  ( 14.27159235450332098, 9.902892378096218942E-16, 0.000000000000000000 ) ) ;
#93275=CARTESIAN_POINT ( 'NONE',  ( 6.471592354503322042, 3.061616997868380183E-16, -2.500000000000001332 ) ) ;
#93285=AXIS2_PLACEMENT_3D ( 'NONE', #26603, #105565, #70846 ) ;
#93341=EDGE_LOOP ( 'NONE', ( #14489, #99842, #36699, #35964, #129190, #17143 ) ) ;
#93357=ORIENTED_EDGE ( 'NONE', *, *, #122099, .T. ) ;
#93367=VERTEX_POINT ( 'NONE', #119200 ) ;
#93414=CARTESIAN_POINT ( 'NONE',  ( 11.15159235450332176, -2.500000000000000000, 3.061616997868384127E-16 ) ) ;
#93431=DIRECTION ( 'NONE',  ( 0.000000000000000000, -1.000000000000000000, 0.000000000000000000 ) ) ;
#93446=CARTESIAN_POINT ( 'NONE',  ( 19.88840764549667384, 3.061616997868380183E-16, -2.500000000000001332 ) ) ;
#93476=DIRECTION ( 'NONE',  ( -1.000000000000000000, -0.000000000000000000, -0.000000000000000000 ) ) ;
#93529=AXIS2_PLACEMENT_3D ( 'NONE', #92132, #71855, #94282 ) ;
#93610=CONICAL_SURFACE ( 'NONE', #114490, 2.500000000000000888, 0.9599310885968822538 ) ;
#93623=DIRECTION ( 'NONE',  ( 0.000000000000000000, -1.000000000000000000, 0.000000000000000000 ) ) ;
#93696=AXIS2_PLACEMENT_3D ( 'NONE', #17399, #5062, #60968 ) ;
#93697=CARTESIAN_POINT ( 'NONE',  ( 20.51159235450331764, 9.902892378096218942E-16, 0.000000000000000000 ) ) ;
#93740=CIRCLE ( 'NONE', #28966, 2.500000000000000888 ) ;
#93757=CARTESIAN_POINT ( 'NONE',  ( 27.22000000000000242, 9.521314400968980422E-16, 0.000000000000000000 ) ) ;
#93766=ORIENTED_EDGE ( 'NONE', *, *, #18616, .F. ) ;
#93824=DIRECTION ( 'NONE',  ( -1.000000000000000000, -0.000000000000000000, -0.000000000000000000 ) ) ;
#93840=VECTOR ( 'NONE', #85600, 1000.000000000000000 ) ;
#93869=DIRECTION ( 'NONE',  ( 0.5735764363510453823, -0.8191520442889923537, 1.003171929053525486E-16 ) ) ;
#93887=DIRECTION ( 'NONE',  ( -1.000000000000000000, -0.000000000000000000, -0.000000000000000000 ) ) ;
#93947=AXIS2_PLACEMENT_3D ( 'NONE', #64364, #53492, #76696 ) ;
#93980=CARTESIAN_POINT ( 'NONE',  ( 19.41999999999999815, 9.521314400968980422E-16, 0.000000000000000000 ) ) ;
#94005=CONICAL_SURFACE ( 'NONE', #19903, 2.055000000000001048, 0.9599310885968758145 ) ;
#94039=VERTEX_POINT ( 'NONE', #68729 ) ;
#94088=FACE_OUTER_BOUND ( 'NONE', #15557, .T. ) ;
#94121=CARTESIAN_POINT ( 'NONE',  ( 7.251592354503322291, 9.902892378096218942E-16, 0.000000000000000000 ) ) ;
#94156=ORIENTED_EDGE ( 'NONE', *, *, #77160, .F. ) ;
#94181=FACE_OUTER_BOUND ( 'NONE', #110321, .T. ) ;
#94195=VERTEX_POINT ( 'NONE', #40485 ) ;
#94203=EDGE_CURVE ( 'NONE', #112837, #67571, #17276, .T. ) ;
#94229=CARTESIAN_POINT ( 'NONE',  ( 13.96000000000000085, -2.055000000000000160, 2.789133085058098087E-16 ) ) ;
#94237=CIRCLE ( 'NONE', #66528, 2.500000000000000888 ) ;
#94282=DIRECTION ( 'NONE',  ( 0.000000000000000000, 1.000000000000000000, 0.000000000000000000 ) ) ;
#94284=CIRCLE ( 'NONE', #3990, 2.500000000000000888 ) ;
#94311=AXIS2_PLACEMENT_3D ( 'NONE', #100131, #11646, #98680 ) ;
#94332=DIRECTION ( 'NONE',  ( -1.000000000000000000, -0.000000000000000000, -0.000000000000000000 ) ) ;
#94339=DIRECTION ( 'NONE',  ( 0.000000000000000000, -1.000000000000000000, 0.000000000000000000 ) ) ;
#94356=ORIENTED_EDGE ( 'NONE', *, *, #49934, .F. ) ;
#94375=CARTESIAN_POINT ( 'NONE',  ( 13.49159235450332162, 9.902892378096218942E-16, 0.000000000000000000 ) ) ;
#94387=ORIENTED_EDGE ( 'NONE', *, *, #49575, .F. ) ;
#94394=EDGE_CURVE ( 'NONE', #85293, #76586, #76175, .T. ) ;
#94408=EDGE_CURVE ( 'NONE', #91029, #86782, #90385, .T. ) ;
#94429=FACE_OUTER_BOUND ( 'NONE', #102254, .T. ) ;
#94461=EDGE_LOOP ( 'NONE', ( #49471, #109503, #108376, #122172, #2843 ) ) ;
#94464=DIRECTION ( 'NONE',  ( -1.000000000000000000, -1.224606353822377258E-16, -0.000000000000000000 ) ) ;
#94487=AXIS2_PLACEMENT_3D ( 'NONE', #101084, #92332, #48152 ) ;
#94491=ORIENTED_EDGE ( 'NONE', *, *, #29107, .F. ) ;
#94515=EDGE_CURVE ( 'NONE', #87542, #60854, #115438, .T. ) ;
#94525=AXIS2_PLACEMENT_3D ( 'NONE', #123199, #79730, #15101 ) ;
#94561=AXIS2_PLACEMENT_3D ( 'NONE', #93253, #46951, #80964 ) ;
#94568=DIRECTION ( 'NONE',  ( 0.000000000000000000, 0.000000000000000000, 1.000000000000000000 ) ) ;
#94604=ADVANCED_FACE ( 'NONE', ( #71506 ), #27503, .T. ) ;
#94614=ORIENTED_EDGE ( 'NONE', *, *, #17787, .F. ) ;
#94652=DIRECTION ( 'NONE',  ( 0.000000000000000000, -1.000000000000000000, 0.000000000000000000 ) ) ;
#94713=ADVANCED_FACE ( 'NONE', ( #104829 ), #125157, .T. ) ;
#94725=AXIS2_PLACEMENT_3D ( 'NONE', #139008, #138290, #38967 ) ;
#94787=CARTESIAN_POINT ( 'NONE',  ( 7.720000000000001528, 9.521314400968980422E-16, 0.000000000000000000 ) ) ;
#94811=DIRECTION ( 'NONE',  ( -0.5735764363510507113, 0.8191520442889885789, 1.003171929053520926E-16 ) ) ;
#94843=CARTESIAN_POINT ( 'NONE',  ( 0.000000000000000000, 0.5999999999999987566, -3.054668707061621191 ) ) ;
#94896=CARTESIAN_POINT ( 'NONE',  ( 11.93159235450332112, 3.061616997868380183E-16, -2.500000000000001332 ) ) ;
#94919=CARTESIAN_POINT ( 'NONE',  ( 27.99999999999999645, 2.055000000000001492, 2.516649172247811554E-16 ) ) ;
#94979=DIRECTION ( 'NONE',  ( 1.000000000000000000, 1.224606353822377258E-16, 0.000000000000000000 ) ) ;
#94986=ORIENTED_EDGE ( 'NONE', *, *, #86127, .T. ) ;
#95047=DIRECTION ( 'NONE',  ( -1.000000000000000000, -1.224606353822377258E-16, -0.000000000000000000 ) ) ;
#95052=CARTESIAN_POINT ( 'NONE',  ( 16.61159235450331906, 9.902892378096218942E-16, 0.000000000000000000 ) ) ;
#95057=DIRECTION ( 'NONE',  ( 0.000000000000000000, -1.000000000000000000, 0.000000000000000000 ) ) ;
#95075=CIRCLE ( 'NONE', #32596, 2.500000000000000888 ) ;
#95124=ORIENTED_EDGE ( 'NONE', *, *, #64442, .F. ) ;
#95140=VECTOR ( 'NONE', #66359, 1000.000000000000000 ) ;
#95203=CARTESIAN_POINT ( 'NONE',  ( 13.49159235450332162, -2.500000000000000000, 3.061616997868384127E-16 ) ) ;
#95206=DIRECTION ( 'NONE',  ( -1.000000000000000000, -1.224606353822377258E-16, -0.000000000000000000 ) ) ;
#95218=EDGE_CURVE ( 'NONE', #39945, #111361, #99288, .T. ) ;
#95243=ORIENTED_EDGE ( 'NONE', *, *, #112227, .F. ) ;
#95286=CARTESIAN_POINT ( 'NONE',  ( 0.000000000000000000, 0.5999999999999987566, 3.054668707061621191 ) ) ;
#95308=FACE_OUTER_BOUND ( 'NONE', #86057, .T. ) ;
#95317=LINE ( 'NONE', #84475, #123250 ) ;
#95335=CARTESIAN_POINT ( 'NONE',  ( 10.37159235450332062, 3.061616997868380183E-16, -2.500000000000001332 ) ) ;
#95376=EDGE_CURVE ( 'NONE', #39592, #103460, #34791, .T. ) ;
#95379=AXIS2_PLACEMENT_3D ( 'NONE', #10600, #42574, #132455 ) ;
#95431=DIRECTION ( 'NONE',  ( 0.000000000000000000, -1.000000000000000000, 0.000000000000000000 ) ) ;
#95457=ORIENTED_EDGE ( 'NONE', *, *, #56656, .F. ) ;
#95458=EDGE_LOOP ( 'NONE', ( #79065, #130401, #114943, #19348, #124762 ) ) ;
#95468=ORIENTED_EDGE ( 'NONE', *, *, #20244, .T. ) ;
#95490=ORIENTED_EDGE ( 'NONE', *, *, #40328, .T. ) ;
#95506=CARTESIAN_POINT ( 'NONE',  ( 11.30840764549667554, 9.139736423841732040E-16, 0.000000000000000000 ) ) ;
#95513=CONICAL_SURFACE ( 'NONE', #7548, 2.500000000000000888, 0.9599310885968822538 ) ;
#95550=CIRCLE ( 'NONE', #137281, 2.500000000000000888 ) ;
#95551=( GEOMETRIC_REPRESENTATION_CONTEXT ( 3 ) GLOBAL_UNCERTAINTY_ASSIGNED_CONTEXT ( ( #89499 ) ) GLOBAL_UNIT_ASSIGNED_CONTEXT ( ( #92601, #125252, #58633 ) ) REPRESENTATION_CONTEXT ( 'NONE', 'WORKASPACE' ) );
#95584=LINE ( 'NONE', #28204, #44373 ) ;
#95586=CIRCLE ( 'NONE', #90962, 2.500000000000000888 ) ;
#95637=DIRECTION ( 'NONE',  ( 0.000000000000000000, -1.000000000000000000, 0.000000000000000000 ) ) ;
#95642=VECTOR ( 'NONE', #117411, 1000.000000000000000 ) ;
#95657=DIRECTION ( 'NONE',  ( -1.000000000000000000, -1.224606353822377258E-16, -0.000000000000000000 ) ) ;
#95665=EDGE_CURVE ( 'NONE', #3604, #105943, #118748, .T. ) ;
#95683=B_SPLINE_CURVE_WITH_KNOTS ( 'NONE', 3,
 ( #64425, #9283, #53562, #97770, #55001, #86908, #131122, #44119, #31806, #33277 ),
 .UNSPECIFIED., .F., .F.,
 ( 4, 2, 2, 2, 4 ),
 ( 0.008003515366661703712, 0.008517983447693482785, 0.009032451528725263593, 0.009546919609757044400, 0.01006138769078882347 ),
 .UNSPECIFIED. ) ;
#95692=DIRECTION ( 'NONE',  ( 0.000000000000000000, -1.000000000000000000, 0.000000000000000000 ) ) ;
#95750=LINE ( 'NONE', #84878, #14306 ) ;
#95787=VERTEX_POINT ( 'NONE', #136056 ) ;
#95790=DIRECTION ( 'NONE',  ( -1.000000000000000000, -1.224606353822377258E-16, -0.000000000000000000 ) ) ;
#95799=CARTESIAN_POINT ( 'NONE',  ( 27.99999999999999645, 9.521314400968980422E-16, 0.000000000000000000 ) ) ;
#95832=EDGE_CURVE ( 'NONE', #78861, #44190, #39337, .T. ) ;
#95841=ORIENTED_EDGE ( 'NONE', *, *, #15957, .T. ) ;
#95854=LINE ( 'NONE', #42217, #34002 ) ;
#95905=VERTEX_POINT ( 'NONE', #49076 ) ;
#95909=EDGE_CURVE ( 'NONE', #138815, #16132, #48340, .T. ) ;
#95931=DIRECTION ( 'NONE',  ( -1.000000000000000000, -1.224606353822377258E-16, -0.000000000000000000 ) ) ;
#95941=DIRECTION ( 'NONE',  ( 0.000000000000000000, -1.000000000000000000, 0.000000000000000000 ) ) ;
#95955=EDGE_CURVE ( 'NONE', #55993, #21453, #41033, .T. ) ;
#95988=ORIENTED_EDGE ( 'NONE', *, *, #91498, .F. ) ;
#95994=CARTESIAN_POINT ( 'NONE',  ( 19.88840764549667384, -3.851859888774471706E-31, 2.500000000000001332 ) ) ;
#96013=CIRCLE ( 'NONE', #114534, 2.500000000000000888 ) ;
#96042=ORIENTED_EDGE ( 'NONE', *, *, #78847, .T. ) ;
#96059=CARTESIAN_POINT ( 'NONE',  ( 27.68840764549667455, 9.139736423841732040E-16, 0.000000000000000000 ) ) ;
#96065=CIRCLE ( 'NONE', #45219, 2.500000000000000888 ) ;
#96075=ORIENTED_EDGE ( 'NONE', *, *, #138957, .T. ) ;
#96085=LINE ( 'NONE', #129433, #7097 ) ;
#96131=ORIENTED_EDGE ( 'NONE', *, *, #43257, .T. ) ;
#96133=DIRECTION ( 'NONE',  ( -0.000000000000000000, 1.000000000000000000, 1.224646799147353207E-16 ) ) ;
#96177=DIRECTION ( 'NONE',  ( 0.000000000000000000, 1.000000000000000000, 0.000000000000000000 ) ) ;
#96185=ORIENTED_EDGE ( 'NONE', *, *, #92613, .T. ) ;
#96188=ORIENTED_EDGE ( 'NONE', *, *, #63254, .F. ) ;
#96195=VECTOR ( 'NONE', #15516, 999.9999999999998863 ) ;
#96228=DIRECTION ( 'NONE',  ( 0.000000000000000000, -1.000000000000000000, 0.000000000000000000 ) ) ;
#96236=CYLINDRICAL_SURFACE ( 'NONE', #79001, 2.500000000000000000 ) ;
#96266=ADVANCED_FACE ( 'NONE', ( #27119 ), #62407, .T. ) ;
#96288=EDGE_LOOP ( 'NONE', ( #130082, #23394, #70600, #103829, #71964 ) ) ;
#96291=CONICAL_SURFACE ( 'NONE', #10614, 2.500000000000000888, 0.9599310885968822538 ) ;
#96317=ORIENTED_EDGE ( 'NONE', *, *, #107411, .F. ) ;
#96330=DIRECTION ( 'NONE',  ( -1.000000000000000000, -0.000000000000000000, -0.000000000000000000 ) ) ;
#96332=CONICAL_SURFACE ( 'NONE', #114869, 2.055000000000001048, 0.9599310885968758145 ) ;
#96350=AXIS2_PLACEMENT_3D ( 'NONE', #91065, #3294, #33821 ) ;
#96397=ORIENTED_EDGE ( 'NONE', *, *, #24034, .T. ) ;
#96400=DIRECTION ( 'NONE',  ( -1.000000000000000000, -1.224606353822377258E-16, -0.000000000000000000 ) ) ;
#96409=ORIENTED_EDGE ( 'NONE', *, *, #118549, .F. ) ;
#96428=FACE_OUTER_BOUND ( 'NONE', #23795, .T. ) ;
#96456=DIRECTION ( 'NONE',  ( 0.000000000000000000, -1.000000000000000000, 0.000000000000000000 ) ) ;
#96470=CYLINDRICAL_SURFACE ( 'NONE', #75738, 2.500000000000000000 ) ;
#96488=DIRECTION ( 'NONE',  ( 0.000000000000000000, -1.000000000000000000, 0.000000000000000000 ) ) ;
#96550=ORIENTED_EDGE ( 'NONE', *, *, #121421, .T. ) ;
#96574=DIRECTION ( 'NONE',  ( 0.000000000000000000, -1.000000000000000000, 0.000000000000000000 ) ) ;
#96579=EDGE_LOOP ( 'NONE', ( #113184, #87430, #53648, #37841, #64306 ) ) ;
#96608=CARTESIAN_POINT ( 'NONE',  ( 8.031592354503320763, -2.500000000000000444, 3.061616997868384620E-16 ) ) ;
#96633=EDGE_LOOP ( 'NONE', ( #127144, #30658, #13613, #100556, #105189, #130849 ) ) ;
#96651=CARTESIAN_POINT ( 'NONE',  ( 17.39159235450332019, 9.902892378096218942E-16, 0.000000000000000000 ) ) ;
#96659=CARTESIAN_POINT ( 'NONE',  ( 27.22000000000000242, -2.055000000000000160, 2.789133085058098087E-16 ) ) ;
#96672=AXIS2_PLACEMENT_3D ( 'NONE', #48895, #112705, #35898 ) ;
#96749=VERTEX_POINT ( 'NONE', #21619 ) ;
#96801=CARTESIAN_POINT ( 'NONE',  ( -25.39999999999996305, 3.061616997868383141E-16, -2.500000000000000000 ) ) ;
#96805=VECTOR ( 'NONE', #21914, 1000.000000000000000 ) ;
#96831=VERTEX_POINT ( 'NONE', #58587 ) ;
#96835=DIRECTION ( 'NONE',  ( 0.000000000000000000, 1.000000000000000000, 0.000000000000000000 ) ) ;
#96841=DIRECTION ( 'NONE',  ( 0.000000000000000000, -1.000000000000000000, 0.000000000000000000 ) ) ;
#96855=DIRECTION ( 'NONE',  ( -1.000000000000000000, -1.224606353822377258E-16, -0.000000000000000000 ) ) ;
#96857=EDGE_CURVE ( 'NONE', #76475, #41073, #46998, .T. ) ;
#96867=ORIENTED_EDGE ( 'NONE', *, *, #61857, .T. ) ;
#96890=ORIENTED_EDGE ( 'NONE', *, *, #126927, .T. ) ;
#96903=DIRECTION ( 'NONE',  ( 0.000000000000000000, -1.000000000000000000, 0.000000000000000000 ) ) ;
#96904=EDGE_LOOP ( 'NONE', ( #121365, #8013, #73945, #97911, #74821, #136315 ) ) ;
#96927=DIRECTION ( 'NONE',  ( 0.5735764363510451602, 0.8191520442889924647, 0.000000000000000000 ) ) ;
#96935=DIRECTION ( 'NONE',  ( -1.000000000000000000, -1.224606353822377258E-16, -0.000000000000000000 ) ) ;
#96988=ORIENTED_EDGE ( 'NONE', *, *, #63591, .T. ) ;
#97008=ORIENTED_EDGE ( 'NONE', *, *, #114929, .T. ) ;
#97010=LINE ( 'NONE', #118053, #131063 ) ;
#97028=ORIENTED_EDGE ( 'NONE', *, *, #36449, .T. ) ;
#97029=CARTESIAN_POINT ( 'NONE',  ( -25.39999999999996305, 3.061616997868383141E-16, -2.500000000000000000 ) ) ;
#97042=ORIENTED_EDGE ( 'NONE', *, *, #104694, .F. ) ;
#97050=DIRECTION ( 'NONE',  ( -1.000000000000000000, -0.000000000000000000, -0.000000000000000000 ) ) ;
#97080=DIRECTION ( 'NONE',  ( -1.000000000000000000, -1.224606353822377258E-16, -0.000000000000000000 ) ) ;
#97096=DIRECTION ( 'NONE',  ( 0.000000000000000000, -1.000000000000000000, 0.000000000000000000 ) ) ;
#97099=FACE_OUTER_BOUND ( 'NONE', #18627, .T. ) ;
#97111=EDGE_LOOP ( 'NONE', ( #30335, #19513, #119574, #68540, #109404 ) ) ;
#97144=VERTEX_POINT ( 'NONE', #9086 ) ;
#97191=AXIS2_PLACEMENT_3D ( 'NONE', #36372, #115298, #103728 ) ;
#97209=CARTESIAN_POINT ( 'NONE',  ( 22.07159235450331991, 9.902892378096218942E-16, 0.000000000000000000 ) ) ;
#97267=DIRECTION ( 'NONE',  ( 0.000000000000000000, -1.000000000000000000, 0.000000000000000000 ) ) ;
#97329=ORIENTED_EDGE ( 'NONE', *, *, #135510, .T. ) ;
#97335=DIRECTION ( 'NONE',  ( 0.000000000000000000, -1.000000000000000000, 0.000000000000000000 ) ) ;
#97336=AXIS2_PLACEMENT_3D ( 'NONE', #19409, #6341, #17269 ) ;
#97342=CARTESIAN_POINT ( 'NONE',  ( 26.75159235450331963, 9.902892378096218942E-16, 0.000000000000000000 ) ) ;
#97363=DIRECTION ( 'NONE',  ( 0.000000000000000000, 1.000000000000000000, 0.000000000000000000 ) ) ;
#97405=CARTESIAN_POINT ( 'NONE',  ( 0.8691243128804486684, 0.5999999999999987566, 4.444585127983390116 ) ) ;
#97411=CIRCLE ( 'NONE', #134501, 2.055000000000001048 ) ;
#97426=DIRECTION ( 'NONE',  ( 0.000000000000000000, 0.000000000000000000, 1.000000000000000000 ) ) ;
#97427=CIRCLE ( 'NONE', #49150, 3.113037248396092416 ) ;
#97442=CARTESIAN_POINT ( 'NONE',  ( 15.83159235450332147, 9.902892378096218942E-16, 0.000000000000000000 ) ) ;
#97451=EDGE_LOOP ( 'NONE', ( #27368, #42447, #42746, #56727, #102176 ) ) ;
#97463=EDGE_CURVE ( 'NONE', #61706, #32667, #108809, .T. ) ;
#97483=EDGE_CURVE ( 'NONE', #44918, #57148, #106528, .T. ) ;
#97511=CIRCLE ( 'NONE', #35056, 2.500000000000000888 ) ;
#97518=ORIENTED_EDGE ( 'NONE', *, *, #55538, .T. ) ;
#97527=AXIS2_PLACEMENT_3D ( 'NONE', #30650, #10981, #43647 ) ;
#97600=VERTEX_POINT ( 'NONE', #120545 ) ;
#97617=CARTESIAN_POINT ( 'NONE',  ( 27.53159235450332076, -7.703719777548943412E-31, 2.500000000000001332 ) ) ;
#97682=VERTEX_POINT ( 'NONE', #112565 ) ;
#97693=DIRECTION ( 'NONE',  ( -1.000000000000000000, -0.000000000000000000, -0.000000000000000000 ) ) ;
#97697=AXIS2_PLACEMENT_3D ( 'NONE', #56731, #100891, #32813 ) ;
#97703=FACE_OUTER_BOUND ( 'NONE', #40530, .T. ) ;
#97710=ORIENTED_EDGE ( 'NONE', *, *, #107183, .T. ) ;
#97752=DIRECTION ( 'NONE',  ( 0.000000000000000000, -1.000000000000000000, 0.000000000000000000 ) ) ;
#97770=CARTESIAN_POINT ( 'NONE',  ( 0.1419055191998411514, 0.5999999999999987566, -3.724211676661871806 ) ) ;
#97788=EDGE_LOOP ( 'NONE', ( #24564, #127582, #31170, #113944, #21225 ) ) ;
#97868=DIRECTION ( 'NONE',  ( 0.000000000000000000, -1.000000000000000000, 0.000000000000000000 ) ) ;
#97872=ORIENTED_EDGE ( 'NONE', *, *, #94408, .T. ) ;
#97883=CARTESIAN_POINT ( 'NONE',  ( 10.37159235450332062, -2.500000000000000000, 3.061616997868384127E-16 ) ) ;
#97911=ORIENTED_EDGE ( 'NONE', *, *, #122059, .F. ) ;
#97932=DIRECTION ( 'NONE',  ( -1.000000000000000000, -0.000000000000000000, -0.000000000000000000 ) ) ;
#97960=ORIENTED_EDGE ( 'NONE', *, *, #81111, .F. ) ;
#97991=ORIENTED_EDGE ( 'NONE', *, *, #41950, .T. ) ;
#98020=VERTEX_POINT ( 'NONE', #63751 ) ;
#98026=DIRECTION ( 'NONE',  ( -1.000000000000000000, -1.224606353822377258E-16, -0.000000000000000000 ) ) ;
#98050=DIRECTION ( 'NONE',  ( -1.000000000000000000, -1.224606353822377258E-16, -0.000000000000000000 ) ) ;
#98153=AXIS2_PLACEMENT_3D ( 'NONE', #108661, #118120, #131172 ) ;
#98163=CARTESIAN_POINT ( 'NONE',  ( 15.98840764549667703, -3.851859888774471706E-31, 2.500000000000001332 ) ) ;
#98196=CONICAL_SURFACE ( 'NONE', #126036, 2.500000000000000888, 0.9599310885968822538 ) ;
#98216=CARTESIAN_POINT ( 'NONE',  ( -25.39999999999996305, 0.000000000000000000, 0.000000000000000000 ) ) ;
#98223=FACE_OUTER_BOUND ( 'NONE', #13720, .T. ) ;
#98248=DIRECTION ( 'NONE',  ( 0.000000000000000000, 0.000000000000000000, 1.000000000000000000 ) ) ;
#98256=DIRECTION ( 'NONE',  ( -0.5735764363510507113, 0.8191520442889885789, 1.003171929053520926E-16 ) ) ;
#98341=CARTESIAN_POINT ( 'NONE',  ( 13.64840764549667540, -3.851859888774471706E-31, 2.500000000000001332 ) ) ;
#98342=CARTESIAN_POINT ( 'NONE',  ( 1.031246673762481025, -0.6000000000000000888, 4.508537709115516989 ) ) ;
#98349=EDGE_CURVE ( 'NONE', #26004, #34476, #92599, .T. ) ;
#98351=CIRCLE ( 'NONE', #63604, 2.500000000000000888 ) ;
#98356=ORIENTED_EDGE ( 'NONE', *, *, #83244, .T. ) ;
#98357=DIRECTION ( 'NONE',  ( -1.000000000000000000, -0.000000000000000000, -0.000000000000000000 ) ) ;
#98397=VERTEX_POINT ( 'NONE', #95994 ) ;
#98445=ORIENTED_EDGE ( 'NONE', *, *, #3106, .F. ) ;
#98479=DIRECTION ( 'NONE',  ( -0.5735764363510503783, -0.8191520442889886899, 0.000000000000000000 ) ) ;
#98537=FACE_OUTER_BOUND ( 'NONE', #64750, .T. ) ;
#98552=CARTESIAN_POINT ( 'NONE',  ( 16.61159235450331906, 2.500000000000001332, 0.000000000000000000 ) ) ;
#98567=ORIENTED_EDGE ( 'NONE', *, *, #60483, .T. ) ;
#98568=DIRECTION ( 'NONE',  ( 0.000000000000000000, -1.000000000000000000, 0.000000000000000000 ) ) ;
#98604=CONICAL_SURFACE ( 'NONE', #63956, 2.500000000000000888, 0.9599310885968822538 ) ;
#98616=DIRECTION ( 'NONE',  ( 0.5735764363510451602, 0.8191520442889924647, 0.000000000000000000 ) ) ;
#98654=ORIENTED_EDGE ( 'NONE', *, *, #116627, .F. ) ;
#98671=DIRECTION ( 'NONE',  ( 0.000000000000000000, -1.000000000000000000, 0.000000000000000000 ) ) ;
#98673=EDGE_CURVE ( 'NONE', #100764, #50175, #60450, .T. ) ;
#98676=DIRECTION ( 'NONE',  ( -0.5735764363510503783, -0.8191520442889886899, 0.000000000000000000 ) ) ;
#98680=DIRECTION ( 'NONE',  ( 0.000000000000000000, 0.000000000000000000, 1.000000000000000000 ) ) ;
#98763=DIRECTION ( 'NONE',  ( 0.000000000000000000, -1.000000000000000000, 0.000000000000000000 ) ) ;
#98802=EDGE_CURVE ( 'NONE', #91029, #64292, #32740, .T. ) ;
#98812=CARTESIAN_POINT ( 'NONE',  ( 1.199999999999999956, 5.612226965700972570E-16, -4.582731094065999322 ) ) ;
#98873=EDGE_LOOP ( 'NONE', ( #8698, #2770, #27945, #20168, #14678 ) ) ;
#98874=CARTESIAN_POINT ( 'NONE',  ( 4.288407645496676857, -2.499999999999999556, 0.000000000000000000 ) ) ;
#98884=DIRECTION ( 'NONE',  ( 0.000000000000000000, -1.000000000000000000, 0.000000000000000000 ) ) ;
#98908=DIRECTION ( 'NONE',  ( 0.000000000000000000, 0.000000000000000000, 1.000000000000000000 ) ) ;
#98935=CARTESIAN_POINT ( 'NONE',  ( -25.39999999999996305, 3.061616997868383141E-16, -2.500000000000000000 ) ) ;
#99001=DIRECTION ( 'NONE',  ( -1.000000000000000000, -1.224606353822377258E-16, -0.000000000000000000 ) ) ;
#99003=CIRCLE ( 'NONE', #52652, 2.500000000000000888 ) ;
#99028=ORIENTED_EDGE ( 'NONE', *, *, #2727, .F. ) ;
#99070=LINE ( 'NONE', #108507, #76439 ) ;
#99145=ORIENTED_EDGE ( 'NONE', *, *, #94515, .F. ) ;
#99211=CIRCLE ( 'NONE', #36734, 2.500000000000000888 ) ;
#99234=VERTEX_POINT ( 'NONE', #31834 ) ;
#99237=ADVANCED_FACE ( 'NONE', ( #121674 ), #44409, .T. ) ;
#99288=LINE ( 'NONE', #143534, #23038 ) ;
#99297=DIRECTION ( 'NONE',  ( -1.000000000000000000, -1.224606353822377258E-16, -0.000000000000000000 ) ) ;
#99382=SURFACE_STYLE_USAGE ( .BOTH. , #88563 ) ;
#99383=ORIENTED_EDGE ( 'NONE', *, *, #38108, .T. ) ;
#99389=ORIENTED_EDGE ( 'NONE', *, *, #119947, .T. ) ;
#99395=DIRECTION ( 'NONE',  ( 0.000000000000000000, -1.000000000000000000, 0.000000000000000000 ) ) ;
#99397=CARTESIAN_POINT ( 'NONE',  ( 20.97999999999999687, 2.055000000000001492, 2.516649172247811554E-16 ) ) ;
#99403=ORIENTED_EDGE ( 'NONE', *, *, #115652, .T. ) ;
#99427=EDGE_CURVE ( 'NONE', #139966, #31468, #62167, .T. ) ;
#99490=CARTESIAN_POINT ( 'NONE',  ( -25.39999999999996305, 0.000000000000000000, 0.000000000000000000 ) ) ;
#99509=EDGE_CURVE ( 'NONE', #138069, #19604, #23667, .T. ) ;
#99572=CIRCLE ( 'NONE', #55631, 2.500000000000000888 ) ;
#99576=DIRECTION ( 'NONE',  ( -1.000000000000000000, -1.224606353822377258E-16, -0.000000000000000000 ) ) ;
#99607=VERTEX_POINT ( 'NONE', #43274 ) ;
#99661=CIRCLE ( 'NONE', #53413, 2.500000000000000888 ) ;
#99689=CONICAL_SURFACE ( 'NONE', #90494, 2.500000000000000888, 0.9599310885968822538 ) ;
#99712=CARTESIAN_POINT ( 'NONE',  ( 14.27159235450332098, -2.500000000000000000, 3.061616997868384127E-16 ) ) ;
#99726=VERTEX_POINT ( 'NONE', #13450 ) ;
#99732=ORIENTED_EDGE ( 'NONE', *, *, #136880, .F. ) ;
#99740=ORIENTED_EDGE ( 'NONE', *, *, #31562, .T. ) ;
#99753=VERTEX_POINT ( 'NONE', #112101 ) ;
#99794=LINE ( 'NONE', #28505, #89210 ) ;
#99807=AXIS2_PLACEMENT_3D ( 'NONE', #114512, #57323, #36957 ) ;
#99822=AXIS2_PLACEMENT_3D ( 'NONE', #83016, #28648, #104755 ) ;
#99830=CARTESIAN_POINT ( 'NONE',  ( -8.534745106696862769E-17, 0.000000000000000000, 0.000000000000000000 ) ) ;
#99832=VECTOR ( 'NONE', #115045, 1000.000000000000000 ) ;
#99839=ORIENTED_EDGE ( 'NONE', *, *, #14346, .F. ) ;
#99842=ORIENTED_EDGE ( 'NONE', *, *, #21282, .T. ) ;
#99863=DIRECTION ( 'NONE',  ( -1.000000000000000000, -1.224606353822377258E-16, -0.000000000000000000 ) ) ;
#99875=EDGE_CURVE ( 'NONE', #108597, #4396, #95317, .T. ) ;
#99889=ORIENTED_EDGE ( 'NONE', *, *, #65939, .F. ) ;
#99893=DIRECTION ( 'NONE',  ( 0.5735764363510451602, 0.8191520442889924647, 0.000000000000000000 ) ) ;
#99952=ORIENTED_EDGE ( 'NONE', *, *, #39080, .F. ) ;
#99957=DIRECTION ( 'NONE',  ( 0.000000000000000000, -1.000000000000000000, 0.000000000000000000 ) ) ;
#99997=VERTEX_POINT ( 'NONE', #110455 ) ;
#100020=VERTEX_POINT ( 'NONE', #98874 ) ;
#100060=AXIS2_PLACEMENT_3D ( 'NONE', #24681, #80520, #58077 ) ;
#100064=CARTESIAN_POINT ( 'NONE',  ( 26.75159235450331963, -3.851859888774471706E-31, 2.500000000000001332 ) ) ;
#100085=ADVANCED_FACE ( 'NONE', ( #41652 ), #102452, .T. ) ;
#100102=FACE_OUTER_BOUND ( 'NONE', #66300, .T. ) ;
#100131=CARTESIAN_POINT ( 'NONE',  ( -25.39999999999996305, 0.000000000000000000, 0.000000000000000000 ) ) ;
#100156=FACE_OUTER_BOUND ( 'NONE', #67452, .T. ) ;
#100202=CARTESIAN_POINT ( 'NONE',  ( 7.251592354503322291, -5.777789833161707559E-31, 2.500000000000001332 ) ) ;
#100207=DIRECTION ( 'NONE',  ( -0.000000000000000000, 0.000000000000000000, 1.000000000000000000 ) ) ;
#100221=CIRCLE ( 'NONE', #40032, 2.500000000000000888 ) ;
#100264=DIRECTION ( 'NONE',  ( -1.000000000000000000, -1.224606353822377258E-16, -0.000000000000000000 ) ) ;
#100293=CIRCLE ( 'NONE', #58640, 2.500000000000000888 ) ;
#100312=CARTESIAN_POINT ( 'NONE',  ( -25.39999999999996305, 3.061616997868383141E-16, -2.500000000000000000 ) ) ;
#100330=DIRECTION ( 'NONE',  ( -0.5735764363510507113, 0.8191520442889885789, 1.003171929053520926E-16 ) ) ;
#100351=FACE_OUTER_BOUND ( 'NONE', #97451, .T. ) ;
#100362=LINE ( 'NONE', #133013, #29641 ) ;
#100393=FACE_OUTER_BOUND ( 'NONE', #140372, .T. ) ;
#100418=DIRECTION ( 'NONE',  ( -1.000000000000000000, -0.000000000000000000, -0.000000000000000000 ) ) ;
#100440=ADVANCED_FACE ( 'NONE', ( #22375 ), #30833, .T. ) ;
#100505=CONICAL_SURFACE ( 'NONE', #125965, 2.500000000000000888, 0.9599310885968822538 ) ;
#100532=LINE ( 'NONE', #91098, #133775 ) ;
#100556=ORIENTED_EDGE ( 'NONE', *, *, #115652, .F. ) ;
#100571=ORIENTED_EDGE ( 'NONE', *, *, #25779, .T. ) ;
#100577=AXIS2_PLACEMENT_3D ( 'NONE', #75408, #131206, #31894 ) ;
#100586=CIRCLE ( 'NONE', #56646, 2.055000000000001048 ) ;
#100602=EDGE_LOOP ( 'NONE', ( #140163, #56196, #60951, #68556, #39563 ) ) ;
#100618=DIRECTION ( 'NONE',  ( -1.000000000000000000, -0.000000000000000000, -0.000000000000000000 ) ) ;
#100642=ORIENTED_EDGE ( 'NONE', *, *, #27887, .T. ) ;
#100692=CIRCLE ( 'NONE', #82193, 2.500000000000000888 ) ;
#100693=EDGE_CURVE ( 'NONE', #58993, #124257, #51629, .T. ) ;
#100717=CARTESIAN_POINT ( 'NONE',  ( 23.63159235450331863, 9.902892378096218942E-16, 0.000000000000000000 ) ) ;
#100733=VERTEX_POINT ( 'NONE', #111370 ) ;
#100739=ORIENTED_EDGE ( 'NONE', *, *, #104858, .F. ) ;
#100756=DIRECTION ( 'NONE',  ( -1.000000000000000000, -0.000000000000000000, -0.000000000000000000 ) ) ;
#100764=VERTEX_POINT ( 'NONE', #78066 ) ;
#100775=DIRECTION ( 'NONE',  ( 0.000000000000000000, 0.000000000000000000, 1.000000000000000000 ) ) ;
#100785=DIRECTION ( 'NONE',  ( -1.000000000000000000, -1.224606353822377258E-16, -0.000000000000000000 ) ) ;
#100842=EDGE_CURVE ( 'NONE', #7890, #92905, #47604, .T. ) ;
#100891=DIRECTION ( 'NONE',  ( 1.000000000000000000, 1.224606353822377258E-16, 0.000000000000000000 ) ) ;
#100938=CARTESIAN_POINT ( 'NONE',  ( 13.64840764549667540, 9.139736423841732040E-16, 0.000000000000000000 ) ) ;
#100975=DIRECTION ( 'NONE',  ( -1.000000000000000000, -1.224606353822377258E-16, -0.000000000000000000 ) ) ;
#101000=LINE ( 'NONE', #69116, #11101 ) ;
#101027=ORIENTED_EDGE ( 'NONE', *, *, #118629, .T. ) ;
#101054=CARTESIAN_POINT ( 'NONE',  ( 15.98840764549667703, 9.139736423841732040E-16, 0.000000000000000000 ) ) ;
#101081=UNCERTAINTY_MEASURE_WITH_UNIT (LENGTH_MEASURE( 1.000000000000000082E-05 ), #15718, 'distance_accuracy_value', 'NONE');
#101082=DIRECTION ( 'NONE',  ( -1.000000000000000000, -1.224606353822377258E-16, -0.000000000000000000 ) ) ;
#101084=CARTESIAN_POINT ( 'NONE',  ( 6.471592354503322042, 9.902892378096218942E-16, 0.000000000000000000 ) ) ;
#101106=EDGE_CURVE ( 'NONE', #96749, #64832, #42536, .T. ) ;
#101107=DIRECTION ( 'NONE',  ( -1.000000000000000000, -1.224606353822377258E-16, -0.000000000000000000 ) ) ;
#101140=CARTESIAN_POINT ( 'NONE',  ( 22.22840764549667725, -2.499999999999996003, 0.000000000000000000 ) ) ;
#101182=VECTOR ( 'NONE', #122333, 999.9999999999998863 ) ;
#101259=CARTESIAN_POINT ( 'NONE',  ( 24.41159235450331977, 9.902892378096218942E-16, 0.000000000000000000 ) ) ;
#101271=ORIENTED_EDGE ( 'NONE', *, *, #82055, .T. ) ;
#101299=ORIENTED_EDGE ( 'NONE', *, *, #141152, .T. ) ;
#101341=ORIENTED_EDGE ( 'NONE', *, *, #46718, .F. ) ;
#101345=DIRECTION ( 'NONE',  ( 0.000000000000000000, -1.000000000000000000, 0.000000000000000000 ) ) ;
#101385=CARTESIAN_POINT ( 'NONE',  ( 10.83999999999999986, 9.521314400968980422E-16, 0.000000000000000000 ) ) ;
#101416=FACE_OUTER_BOUND ( 'NONE', #38977, .T. ) ;
#101427=EDGE_CURVE ( 'NONE', #119455, #103076, #54136, .T. ) ;
#101439=ORIENTED_EDGE ( 'NONE', *, *, #132076, .F. ) ;
#101536=DIRECTION ( 'NONE',  ( -1.000000000000000000, -1.224606353822377258E-16, -0.000000000000000000 ) ) ;
#101547=DIRECTION ( 'NONE',  ( -1.000000000000000000, -1.224606353822377258E-16, -0.000000000000000000 ) ) ;
#101549=CARTESIAN_POINT ( 'NONE',  ( 25.97159235450331849, -2.500000000000000000, 3.061616997868384127E-16 ) ) ;
#101555=FACE_OUTER_BOUND ( 'NONE', #66724, .T. ) ;
#101556=ORIENTED_EDGE ( 'NONE', *, *, #34724, .T. ) ;
#101557=ORIENTED_EDGE ( 'NONE', *, *, #49934, .T. ) ;
#101559=ORIENTED_EDGE ( 'NONE', *, *, #138957, .F. ) ;
#101562=AXIS2_PLACEMENT_3D ( 'NONE', #8481, #110662, #52734 ) ;
#101593=ADVANCED_FACE ( 'NONE', ( #119749 ), #3160, .T. ) ;
#101595=DIRECTION ( 'NONE',  ( 0.000000000000000000, -1.000000000000000000, 0.000000000000000000 ) ) ;
#101620=CARTESIAN_POINT ( 'NONE',  ( 23.78840764549667597, 9.139736423841732040E-16, 0.000000000000000000 ) ) ;
#101669=ORIENTED_EDGE ( 'NONE', *, *, #91935, .T. ) ;
#101695=CARTESIAN_POINT ( 'NONE',  ( 7.251592354503322291, 9.902892378096218942E-16, 0.000000000000000000 ) ) ;
#101759=VERTEX_POINT ( 'NONE', #1534 ) ;
#101812=VERTEX_POINT ( 'NONE', #134976 ) ;
#101830=CIRCLE ( 'NONE', #111008, 2.055000000000001048 ) ;
#101868=DIRECTION ( 'NONE',  ( 0.000000000000000000, 1.000000000000000000, 0.000000000000000000 ) ) ;
#101944=ADVANCED_FACE ( 'NONE', ( #130168 ), #87372, .T. ) ;
#101953=CIRCLE ( 'NONE', #41828, 2.500000000000000888 ) ;
#101974=ADVANCED_FACE ( 'NONE', ( #100393 ), #14552, .T. ) ;
#101975=CARTESIAN_POINT ( 'NONE',  ( 27.53159235450332076, 9.902892378096218942E-16, 0.000000000000000000 ) ) ;
#101983=CARTESIAN_POINT ( 'NONE',  ( 17.07999999999999829, 9.521314400968980422E-16, 0.000000000000000000 ) ) ;
#101988=CIRCLE ( 'NONE', #127776, 2.500000000000000888 ) ;
#102001=AXIS2_PLACEMENT_3D ( 'NONE', #28922, #126107, #38375 ) ;
#102005=CARTESIAN_POINT ( 'NONE',  ( 15.98840764549667703, 9.139736423841732040E-16, 0.000000000000000000 ) ) ;
#102034=LINE ( 'NONE', #143387, #802 ) ;
#102049=CARTESIAN_POINT ( 'NONE',  ( -25.39999999999996305, 0.000000000000000000, 0.000000000000000000 ) ) ;
#102059=EDGE_CURVE ( 'NONE', #3378, #36518, #665, .T. ) ;
#102103=DIRECTION ( 'NONE',  ( -1.000000000000000000, -1.224606353822377258E-16, -0.000000000000000000 ) ) ;
#102111=ORIENTED_EDGE ( 'NONE', *, *, #130697, .T. ) ;
#102119=DIRECTION ( 'NONE',  ( 0.000000000000000000, -1.000000000000000000, 0.000000000000000000 ) ) ;
#102128=CARTESIAN_POINT ( 'NONE',  ( 15.83159235450332147, 9.902892378096218942E-16, 0.000000000000000000 ) ) ;
#102144=CIRCLE ( 'NONE', #139203, 2.500000000000000888 ) ;
#102176=ORIENTED_EDGE ( 'NONE', *, *, #126600, .T. ) ;
#102179=ORIENTED_EDGE ( 'NONE', *, *, #61124, .T. ) ;
#102188=DIRECTION ( 'NONE',  ( 0.000000000000000000, -1.000000000000000000, 0.000000000000000000 ) ) ;
#102198=CONICAL_SURFACE ( 'NONE', #132330, 2.055000000000001048, 0.9599310885968758145 ) ;
#102206=AXIS2_PLACEMENT_3D ( 'NONE', #84450, #64827, #108271 ) ;
#102212=CARTESIAN_POINT ( 'NONE',  ( 11.30840764549667554, 2.500000000000000888, 3.061616997868383141E-16 ) ) ;
#102230=LINE ( 'NONE', #113068, #68427 ) ;
#102231=DIRECTION ( 'NONE',  ( 0.000000000000000000, -1.000000000000000000, 0.000000000000000000 ) ) ;
#102254=EDGE_LOOP ( 'NONE', ( #41685, #123398, #618, #129227, #83625 ) ) ;
#102260=ADVANCED_FACE ( 'NONE', ( #103914 ), #118652, .T. ) ;
#102265=CARTESIAN_POINT ( 'NONE',  ( 15.05159235450332034, 9.902892378096218942E-16, 0.000000000000000000 ) ) ;
#102393=DIRECTION ( 'NONE',  ( -1.000000000000000000, -0.000000000000000000, -0.000000000000000000 ) ) ;
#102444=CARTESIAN_POINT ( 'NONE',  ( 1.199999999999999956, 0.5999999999999987566, 4.749999999999999112 ) ) ;
#102446=ADVANCED_FACE ( 'NONE', ( #29232 ), #42280, .T. ) ;
#102452=CONICAL_SURFACE ( 'NONE', #577, 2.055000000000001048, 0.9599310885968758145 ) ;
#102525=DIRECTION ( 'NONE',  ( -1.000000000000000000, -1.224606353822377258E-16, -0.000000000000000000 ) ) ;
#102551=ORIENTED_EDGE ( 'NONE', *, *, #143300, .F. ) ;
#102584=LINE ( 'NONE', #114146, #306 ) ;
#102706=FACE_OUTER_BOUND ( 'NONE', #52614, .T. ) ;
#102714=LINE ( 'NONE', #2654, #76173 ) ;
#102716=EDGE_LOOP ( 'NONE', ( #114845, #70435, #3752, #55761, #45839, #19727 ) ) ;
#102722=CARTESIAN_POINT ( 'NONE',  ( 26.90840764549667696, 9.139736423841732040E-16, 0.000000000000000000 ) ) ;
#102768=ORIENTED_EDGE ( 'NONE', *, *, #75675, .T. ) ;
#102792=VERTEX_POINT ( 'NONE', #8685 ) ;
#102810=CARTESIAN_POINT ( 'NONE',  ( 4.911592354503321545, 9.902892378096218942E-16, 0.000000000000000000 ) ) ;
#102857=DIRECTION ( 'NONE',  ( -0.5735764363510503783, -0.8191520442889886899, 0.000000000000000000 ) ) ;
#102875=ORIENTED_EDGE ( 'NONE', *, *, #44003, .T. ) ;
#102881=ORIENTED_EDGE ( 'NONE', *, *, #107582, .F. ) ;
#102911=CIRCLE ( 'NONE', #93696, 2.500000000000000888 ) ;
#102933=DIRECTION ( 'NONE',  ( -1.000000000000000000, -1.224606353822377258E-16, -0.000000000000000000 ) ) ;
#102950=ORIENTED_EDGE ( 'NONE', *, *, #110056, .F. ) ;
#103040=AXIS2_PLACEMENT_3D ( 'NONE', #63154, #9405, #131963 ) ;
#103065=DIRECTION ( 'NONE',  ( 0.000000000000000000, -1.000000000000000000, 0.000000000000000000 ) ) ;
#103070=CARTESIAN_POINT ( 'NONE',  ( -25.39999999999996305, 3.061616997868383141E-16, -2.500000000000000000 ) ) ;
#103076=VERTEX_POINT ( 'NONE', #93446 ) ;
#103081=VERTEX_POINT ( 'NONE', #81896 ) ;
#103096=ADVANCED_FACE ( 'NONE', ( #4216 ), #113035, .T. ) ;
#103110=DIRECTION ( 'NONE',  ( 1.000000000000000000, 1.224606353822377258E-16, 0.000000000000000000 ) ) ;
#103135=DIRECTION ( 'NONE',  ( 0.000000000000000000, -1.000000000000000000, 0.000000000000000000 ) ) ;
#103148=CARTESIAN_POINT ( 'NONE',  ( -25.39999999999996305, 0.000000000000000000, 0.000000000000000000 ) ) ;
#103175=ORIENTED_EDGE ( 'NONE', *, *, #71181, .T. ) ;
#103223=DIRECTION ( 'NONE',  ( 0.000000000000000000, -1.000000000000000000, 0.000000000000000000 ) ) ;
#103245=EDGE_CURVE ( 'NONE', #40200, #52853, #40244, .T. ) ;
#103346=EDGE_CURVE ( 'NONE', #137915, #72729, #14848, .T. ) ;
#103374=PLANE ( 'NONE',  #47705 ) ;
#103415=CARTESIAN_POINT ( 'NONE',  ( 10.37159235450332062, 9.902892378096218942E-16, 0.000000000000000000 ) ) ;
#103419=CYLINDRICAL_SURFACE ( 'NONE', #18875, 2.500000000000000000 ) ;
#103442=CIRCLE ( 'NONE', #73377, 2.055000000000001048 ) ;
#103460=VERTEX_POINT ( 'NONE', #35354 ) ;
#103469=CARTESIAN_POINT ( 'NONE',  ( 21.29159235450332233, 9.902892378096218942E-16, 0.000000000000000000 ) ) ;
#103551=DIRECTION ( 'NONE',  ( 0.000000000000000000, -1.000000000000000000, 0.000000000000000000 ) ) ;
#103562=VERTEX_POINT ( 'NONE', #75635 ) ;
#103567=CARTESIAN_POINT ( 'NONE',  ( 23.32000000000000028, 9.521314400968980422E-16, 0.000000000000000000 ) ) ;
#103574=CYLINDRICAL_SURFACE ( 'NONE', #20799, 2.500000000000000000 ) ;
#103577=AXIS2_PLACEMENT_3D ( 'NONE', #122456, #45665, #44226 ) ;
#103597=ORIENTED_EDGE ( 'NONE', *, *, #77744, .T. ) ;
#103623=CIRCLE ( 'NONE', #10992, 2.500000000000000888 ) ;
#103631=VERTEX_POINT ( 'NONE', #41553 ) ;
#103653=CARTESIAN_POINT ( 'NONE',  ( 25.19159235450331735, -3.851859888774471706E-31, 2.500000000000001332 ) ) ;
#103693=CARTESIAN_POINT ( 'NONE',  ( 9.279999999999999361, -2.055000000000000160, 0.000000000000000000 ) ) ;
#103724=DIRECTION ( 'NONE',  ( -1.000000000000000000, -0.000000000000000000, -0.000000000000000000 ) ) ;
#103728=DIRECTION ( 'NONE',  ( 0.000000000000000000, -1.000000000000000000, 0.000000000000000000 ) ) ;
#103731=CARTESIAN_POINT ( 'NONE',  ( 5.068407645496677105, 9.139736423841732040E-16, 0.000000000000000000 ) ) ;
#103735=CARTESIAN_POINT ( 'NONE',  ( 15.20840764549667767, -3.851859888774471706E-31, 2.500000000000001332 ) ) ;
#103763=VECTOR ( 'NONE', #26735, 1000.000000000000114 ) ;
#103779=EDGE_LOOP ( 'NONE', ( #79138, #23105, #41915, #57939, #4095 ) ) ;
#103784=LINE ( 'NONE', #25526, #129336 ) ;
#103800=ORIENTED_EDGE ( 'NONE', *, *, #94203, .T. ) ;
#103808=DIRECTION ( 'NONE',  ( 0.000000000000000000, 0.000000000000000000, 1.000000000000000000 ) ) ;
#103829=ORIENTED_EDGE ( 'NONE', *, *, #70615, .T. ) ;
#103849=FACE_OUTER_BOUND ( 'NONE', #87819, .T. ) ;
#103860=EDGE_CURVE ( 'NONE', #43087, #115095, #3728, .T. ) ;
#103862=AXIS2_PLACEMENT_3D ( 'NONE', #143463, #134040, #23847 ) ;
#103892=DIRECTION ( 'NONE',  ( -1.000000000000000000, -0.000000000000000000, -0.000000000000000000 ) ) ;
#103914=FACE_OUTER_BOUND ( 'NONE', #108325, .T. ) ;
#103951=CONICAL_SURFACE ( 'NONE', #25321, 2.055000000000001048, 0.9599310885968758145 ) ;
#103999=DIRECTION ( 'NONE',  ( -1.000000000000000000, -0.000000000000000000, -0.000000000000000000 ) ) ;
#104057=ORIENTED_EDGE ( 'NONE', *, *, #124729, .T. ) ;
#104075=DIRECTION ( 'NONE',  ( 0.000000000000000000, -1.000000000000000000, 0.000000000000000000 ) ) ;
#104082=CIRCLE ( 'NONE', #122626, 2.500000000000000888 ) ;
#104085=CARTESIAN_POINT ( 'NONE',  ( 21.29159235450332233, -2.500000000000000444, 3.061616997868384620E-16 ) ) ;
#104091=EDGE_CURVE ( 'NONE', #118058, #105436, #26547, .T. ) ;
#104096=VERTEX_POINT ( 'NONE', #2133 ) ;
#104129=CONICAL_SURFACE ( 'NONE', #132019, 2.055000000000001048, 0.9599310885968758145 ) ;
#104132=DIRECTION ( 'NONE',  ( 0.5735764363510453823, -0.8191520442889923537, 1.003171929053525486E-16 ) ) ;
#104222=AXIS2_PLACEMENT_3D ( 'NONE', #39754, #117956, #107109 ) ;
#104260=AXIS2_PLACEMENT_3D ( 'NONE', #12397, #90705, #1500 ) ;
#104312=EDGE_CURVE ( 'NONE', #50175, #29061, #81923, .T. ) ;
#104336=AXIS2_PLACEMENT_3D ( 'NONE', #89401, #46667, #135086 ) ;
#104348=VECTOR ( 'NONE', #15590, 1000.000000000000114 ) ;
#104377=LINE ( 'NONE', #5037, #142851 ) ;
#104389=DIRECTION ( 'NONE',  ( -1.000000000000000000, -0.000000000000000000, -0.000000000000000000 ) ) ;
#104451=CARTESIAN_POINT ( 'NONE',  ( 12.08840764549667668, -3.851859888774471706E-31, 2.500000000000001332 ) ) ;
#104455=VECTOR ( 'NONE', #131833, 1000.000000000000000 ) ;
#104465=ORIENTED_EDGE ( 'NONE', *, *, #88718, .T. ) ;
#104492=CYLINDRICAL_SURFACE ( 'NONE', #52492, 2.500000000000000000 ) ;
#104498=CARTESIAN_POINT ( 'NONE',  ( 15.52000000000000135, 9.521314400968980422E-16, 0.000000000000000000 ) ) ;
#104512=DIRECTION ( 'NONE',  ( 0.000000000000000000, -1.000000000000000000, 0.000000000000000000 ) ) ;
#104539=ORIENTED_EDGE ( 'NONE', *, *, #73746, .F. ) ;
#104576=ORIENTED_EDGE ( 'NONE', *, *, #17475, .T. ) ;
#104583=VERTEX_POINT ( 'NONE', #131096 ) ;
#104618=CIRCLE ( 'NONE', #88506, 2.055000000000001048 ) ;
#104622=DIRECTION ( 'NONE',  ( 0.000000000000000000, 1.000000000000000000, 0.000000000000000000 ) ) ;
#104642=LINE ( 'NONE', #48859, #142086 ) ;
#104668=ADVANCED_FACE ( 'NONE', ( #21621 ), #128491, .T. ) ;
#104694=EDGE_CURVE ( 'NONE', #93111, #44264, #14302, .T. ) ;
#104729=ORIENTED_EDGE ( 'NONE', *, *, #133107, .F. ) ;
#104755=DIRECTION ( 'NONE',  ( 0.000000000000000000, -1.000000000000000000, 0.000000000000000000 ) ) ;
#104794=DIRECTION ( 'NONE',  ( -1.000000000000000000, -0.000000000000000000, -0.000000000000000000 ) ) ;
#104826=DIRECTION ( 'NONE',  ( 0.000000000000000000, -1.000000000000000000, 0.000000000000000000 ) ) ;
#104829=FACE_OUTER_BOUND ( 'NONE', #63460, .T. ) ;
#104857=DIRECTION ( 'NONE',  ( -1.000000000000000000, -1.224606353822377258E-16, -0.000000000000000000 ) ) ;
#104858=EDGE_CURVE ( 'NONE', #77143, #113805, #61431, .T. ) ;
#104873=VECTOR ( 'NONE', #72409, 1000.000000000000114 ) ;
#104878=EDGE_CURVE ( 'NONE', #61060, #34133, #96065, .T. ) ;
#104881=DIRECTION ( 'NONE',  ( -1.000000000000000000, -1.224606353822377258E-16, -0.000000000000000000 ) ) ;
#104890=ORIENTED_EDGE ( 'NONE', *, *, #62200, .T. ) ;
#104959=ORIENTED_EDGE ( 'NONE', *, *, #136444, .T. ) ;
#104963=ORIENTED_EDGE ( 'NONE', *, *, #52012, .F. ) ;
#104965=PRODUCT_DEFINITION_FORMATION_WITH_SPECIFIED_SOURCE ( 'ANY', '', #142759, .NOT_KNOWN. ) ;
#105003=FACE_OUTER_BOUND ( 'NONE', #113847, .T. ) ;
#105005=DIRECTION ( 'NONE',  ( 0.000000000000000000, -1.000000000000000000, 0.000000000000000000 ) ) ;
#105029=FACE_OUTER_BOUND ( 'NONE', #23676, .T. ) ;
#105037=ORIENTED_EDGE ( 'NONE', *, *, #136284, .F. ) ;
#105046=EDGE_CURVE ( 'NONE', #1660, #139966, #89258, .T. ) ;
#105077=LINE ( 'NONE', #41239, #56148 ) ;
#105087=ADVANCED_FACE ( 'NONE', ( #122162 ), #22832, .T. ) ;
#105098=CARTESIAN_POINT ( 'NONE',  ( 18.95159235450331892, 2.500000000000001332, 0.000000000000000000 ) ) ;
#105128=DIRECTION ( 'NONE',  ( 0.000000000000000000, 0.000000000000000000, 1.000000000000000000 ) ) ;
#105151=DIRECTION ( 'NONE',  ( 0.000000000000000000, 1.000000000000000000, 0.000000000000000000 ) ) ;
#105158=FACE_OUTER_BOUND ( 'NONE', #109572, .T. ) ;
#105169=VECTOR ( 'NONE', #44355, 1000.000000000000114 ) ;
#105189=ORIENTED_EDGE ( 'NONE', *, *, #113518, .F. ) ;
#105229=AXIS2_PLACEMENT_3D ( 'NONE', #15257, #48646, #137080 ) ;
#105250=LINE ( 'NONE', #5901, #43357 ) ;
#105342=EDGE_CURVE ( 'NONE', #118163, #43549, #38348, .T. ) ;
#105376=ADVANCED_FACE ( 'NONE', ( #41590 ), #84613, .T. ) ;
#105382=DIRECTION ( 'NONE',  ( -1.000000000000000000, -1.224606353822377258E-16, -0.000000000000000000 ) ) ;
#105428=ORIENTED_EDGE ( 'NONE', *, *, #142033, .T. ) ;
#105431=DIRECTION ( 'NONE',  ( 0.000000000000000000, -1.000000000000000000, 0.000000000000000000 ) ) ;
#105436=VERTEX_POINT ( 'NONE', #46467 ) ;
#105443=ORIENTED_EDGE ( 'NONE', *, *, #78802, .F. ) ;
#105461=FACE_OUTER_BOUND ( 'NONE', #24054, .T. ) ;
#105469=VERTEX_POINT ( 'NONE', #4266 ) ;
#105474=ORIENTED_EDGE ( 'NONE', *, *, #55099, .T. ) ;
#105483=DIRECTION ( 'NONE',  ( -0.5735764363510503783, -0.8191520442889886899, 0.000000000000000000 ) ) ;
#105488=ORIENTED_EDGE ( 'NONE', *, *, #50014, .T. ) ;
#105506=ORIENTED_EDGE ( 'NONE', *, *, #120577, .T. ) ;
#105518=ORIENTED_EDGE ( 'NONE', *, *, #41735, .T. ) ;
#105522=CARTESIAN_POINT ( 'NONE',  ( 6.471592354503322042, 2.500000000000001332, 0.000000000000000000 ) ) ;
#105565=DIRECTION ( 'NONE',  ( -1.000000000000000000, -1.224606353822377258E-16, -0.000000000000000000 ) ) ;
#105566=DIRECTION ( 'NONE',  ( -1.000000000000000000, -0.000000000000000000, -0.000000000000000000 ) ) ;
#105568=CARTESIAN_POINT ( 'NONE',  ( 24.41159235450331977, 9.902892378096218942E-16, 0.000000000000000000 ) ) ;
#105584=AXIS2_PLACEMENT_3D ( 'NONE', #130427, #10738, #64435 ) ;
#105593=VECTOR ( 'NONE', #32116, 1000.000000000000000 ) ;
#105638=EDGE_CURVE ( 'NONE', #29342, #43549, #97010, .T. ) ;
#105641=CIRCLE ( 'NONE', #31685, 2.500000000000000000 ) ;
#105651=DIRECTION ( 'NONE',  ( 0.000000000000000000, -1.000000000000000000, 0.000000000000000000 ) ) ;
#105659=CONICAL_SURFACE ( 'NONE', #124215, 2.055000000000001048, 0.9599310885968758145 ) ;
#105670=CIRCLE ( 'NONE', #124131, 2.500000000000000888 ) ;
#105678=ORIENTED_EDGE ( 'NONE', *, *, #138411, .T. ) ;
#105705=CARTESIAN_POINT ( 'NONE',  ( 5.848407645496676466, 9.139736423841732040E-16, 0.000000000000000000 ) ) ;
#105725=ADVANCED_FACE ( 'NONE', ( #28718 ), #103374, .T. ) ;
#105745=EDGE_LOOP ( 'NONE', ( #47821, #5742, #81312, #40842, #95243, #78691 ) ) ;
#105808=DIRECTION ( 'NONE',  ( -1.000000000000000000, -1.224606353822377258E-16, -0.000000000000000000 ) ) ;
#105853=AXIS2_PLACEMENT_3D ( 'NONE', #102049, #47015, #113623 ) ;
#105906=DIRECTION ( 'NONE',  ( -1.000000000000000000, -1.224606353822377258E-16, -0.000000000000000000 ) ) ;
#105915=AXIS2_PLACEMENT_3D ( 'NONE', #12212, #136143, #33992 ) ;
#105943=VERTEX_POINT ( 'NONE', #6459 ) ;
#105983=EDGE_CURVE ( 'NONE', #139966, #1660, #31513, .T. ) ;
#106005=EDGE_CURVE ( 'NONE', #21906, #99997, #105670, .T. ) ;
#106030=EDGE_CURVE ( 'NONE', #23774, #121207, #45514, .T. ) ;
#106049=FACE_OUTER_BOUND ( 'NONE', #81545, .T. ) ;
#106090=EDGE_CURVE ( 'NONE', #1673, #128813, #26498, .T. ) ;
#106130=DIRECTION ( 'NONE',  ( -1.000000000000000000, -0.000000000000000000, -0.000000000000000000 ) ) ;
#106148=DIRECTION ( 'NONE',  ( 1.000000000000000000, 0.000000000000000000, 0.000000000000000000 ) ) ;
#106180=EDGE_CURVE ( 'NONE', #51758, #9966, #8390, .T. ) ;
#106213=CARTESIAN_POINT ( 'NONE',  ( 10.06000000000000050, -2.055000000000000160, 2.789133085058098087E-16 ) ) ;
#106215=VERTEX_POINT ( 'NONE', #21332 ) ;
#106249=AXIS2_PLACEMENT_3D ( 'NONE', #78956, #11486, #12931 ) ;
#106302=ORIENTED_EDGE ( 'NONE', *, *, #59709, .F. ) ;
#106330=CARTESIAN_POINT ( 'NONE',  ( 19.73159235450332005, 2.500000000000001776, 0.000000000000000000 ) ) ;
#106345=ORIENTED_EDGE ( 'NONE', *, *, #66744, .T. ) ;
#106382=CYLINDRICAL_SURFACE ( 'NONE', #131610, 2.500000000000000000 ) ;
#106395=AXIS2_PLACEMENT_3D ( 'NONE', #55404, #75722, #9722 ) ;
#106451=VERTEX_POINT ( 'NONE', #78573 ) ;
#106456=CIRCLE ( 'NONE', #115761, 2.500000000000000888 ) ;
#106507=ORIENTED_EDGE ( 'NONE', *, *, #89673, .T. ) ;
#106522=DIRECTION ( 'NONE',  ( 0.000000000000000000, -1.000000000000000000, 0.000000000000000000 ) ) ;
#106528=CIRCLE ( 'NONE', #127364, 2.500000000000000888 ) ;
#106549=ORIENTED_EDGE ( 'NONE', *, *, #61035, .T. ) ;
#106613=FACE_OUTER_BOUND ( 'NONE', #100602, .T. ) ;
#106658=CARTESIAN_POINT ( 'NONE',  ( 23.63159235450331863, 2.500000000000001332, 0.000000000000000000 ) ) ;
#106663=EDGE_CURVE ( 'NONE', #79589, #87542, #95854, .T. ) ;
#106690=ORIENTED_EDGE ( 'NONE', *, *, #91204, .T. ) ;
#106721=VERTEX_POINT ( 'NONE', #30625 ) ;
#106737=CIRCLE ( 'NONE', #99822, 2.055000000000001048 ) ;
#106738=EDGE_CURVE ( 'NONE', #92199, #22742, #8479, .T. ) ;
#106746=CARTESIAN_POINT ( 'NONE',  ( 20.51159235450331764, -2.500000000000000000, 3.061616997868384127E-16 ) ) ;
#106750=ORIENTED_EDGE ( 'NONE', *, *, #6039, .F. ) ;
#106754=AXIS2_PLACEMENT_3D ( 'NONE', #140549, #107897, #74613 ) ;
#106819=VECTOR ( 'NONE', #96927, 1000.000000000000000 ) ;
#106854=DIRECTION ( 'NONE',  ( 0.000000000000000000, -1.000000000000000000, 0.000000000000000000 ) ) ;
#106866=CARTESIAN_POINT ( 'NONE',  ( 0.2261952378971223976, 0.5999999999999987566, 3.877637771780739318 ) ) ;
#106912=CARTESIAN_POINT ( 'NONE',  ( 21.29159235450332233, -2.500000000000000000, 3.061616997868384127E-16 ) ) ;
#106927=FACE_OUTER_BOUND ( 'NONE', #112462, .T. ) ;
#106929=CIRCLE ( 'NONE', #14433, 2.500000000000000888 ) ;
#106945=ORIENTED_EDGE ( 'NONE', *, *, #104878, .T. ) ;
#106993=CARTESIAN_POINT ( 'NONE',  ( 5.380000000000000782, -2.055000000000000160, 2.789133085058098087E-16 ) ) ;
#107059=SURFACE_STYLE_USAGE ( .BOTH. , #16454 ) ;
#107080=FACE_OUTER_BOUND ( 'NONE', #58851, .T. ) ;
#107109=DIRECTION ( 'NONE',  ( 0.000000000000000000, 0.000000000000000000, 1.000000000000000000 ) ) ;
#107112=AXIS2_PLACEMENT_3D ( 'NONE', #1435, #81926, #102231 ) ;
#107121=EDGE_LOOP ( 'NONE', ( #50011, #35623, #48668, #1724, #55787 ) ) ;
#107122=CARTESIAN_POINT ( 'NONE',  ( 27.53159235450332076, 2.500000000000001776, 0.000000000000000000 ) ) ;
#107123=FACE_OUTER_BOUND ( 'NONE', #71677, .T. ) ;
#107148=ADVANCED_FACE ( 'NONE', ( #98537 ), #22829, .T. ) ;
#107183=EDGE_CURVE ( 'NONE', #47923, #123374, #45975, .T. ) ;
#107237=CARTESIAN_POINT ( 'NONE',  ( 14.27159235450332098, 2.500000000000001332, 0.000000000000000000 ) ) ;
#107248=CARTESIAN_POINT ( 'NONE',  ( 10.83999999999999986, -2.055000000000000160, 2.789133085058098087E-16 ) ) ;
#107280=ADVANCED_FACE ( 'NONE', ( #125299 ), #61407, .T. ) ;
#107283=CARTESIAN_POINT ( 'NONE',  ( 0.000000000000000000, -0.5999999999999993117, -4.750000000000000000 ) ) ;
#107297=DIRECTION ( 'NONE',  ( -1.000000000000000000, -1.224606353822377258E-16, -0.000000000000000000 ) ) ;
#107315=EDGE_CURVE ( 'NONE', #108329, #96831, #114627, .T. ) ;
#107321=CIRCLE ( 'NONE', #44889, 2.500000000000000888 ) ;
#107340=FACE_OUTER_BOUND ( 'NONE', #126299, .T. ) ;
#107354=EDGE_LOOP ( 'NONE', ( #15264, #18093, #51143, #110969, #5390 ) ) ;
#107379=DIRECTION ( 'NONE',  ( -1.000000000000000000, -1.224606353822377258E-16, -0.000000000000000000 ) ) ;
#107381=CARTESIAN_POINT ( 'NONE',  ( 6.628407645496676714, 9.139736423841732040E-16, 0.000000000000000000 ) ) ;
#107400=DIRECTION ( 'NONE',  ( 0.000000000000000000, 0.000000000000000000, 1.000000000000000000 ) ) ;
#107411=EDGE_CURVE ( 'NONE', #118031, #15339, #109975, .T. ) ;
#107420=CARTESIAN_POINT ( 'NONE',  ( 18.63999999999999702, 9.521314400968980422E-16, 0.000000000000000000 ) ) ;
#107582=EDGE_CURVE ( 'NONE', #44190, #99753, #99794, .T. ) ;
#107587=CARTESIAN_POINT ( 'NONE',  ( 0.02842916987967500017, 0.5999999999999986455, 3.398229573760036093 ) ) ;
#107598=AXIS2_PLACEMENT_3D ( 'NONE', #64584, #53727, #96456 ) ;
#107601=AXIS2_PLACEMENT_3D ( 'NONE', #95506, #19384, #52024 ) ;
#107606=CIRCLE ( 'NONE', #26590, 2.500000000000000888 ) ;
#107616=ORIENTED_EDGE ( 'NONE', *, *, #14849, .T. ) ;
#107630=ADVANCED_FACE ( 'NONE', ( #50964 ), #39384, .T. ) ;
#107640=EDGE_LOOP ( 'NONE', ( #79940, #103800, #21910, #6317, #58746 ) ) ;
#107650=CYLINDRICAL_SURFACE ( 'NONE', #7745, 2.500000000000000000 ) ;
#107671=LINE ( 'NONE', #61376, #69568 ) ;
#107690=ORIENTED_EDGE ( 'NONE', *, *, #42208, .F. ) ;
#107700=AXIS2_PLACEMENT_3D ( 'NONE', #89891, #34824, #47178 ) ;
#107725=VERTEX_POINT ( 'NONE', #130575 ) ;
#107733=ORIENTED_EDGE ( 'NONE', *, *, #38683, .F. ) ;
#107804=ORIENTED_EDGE ( 'NONE', *, *, #31398, .F. ) ;
#107811=CARTESIAN_POINT ( 'NONE',  ( 1.369266385878517678, 0.000000000000000000, 0.000000000000000000 ) ) ;
#107853=CIRCLE ( 'NONE', #17535, 2.500000000000000888 ) ;
#107893=CARTESIAN_POINT ( 'NONE',  ( 22.85159235450332105, 9.902892378096218942E-16, 0.000000000000000000 ) ) ;
#107897=DIRECTION ( 'NONE',  ( -1.000000000000000000, -1.224606353822377258E-16, -0.000000000000000000 ) ) ;
#107903=EDGE_CURVE ( 'NONE', #47888, #65959, #86923, .T. ) ;
#107913=ADVANCED_FACE ( 'NONE', ( #92741 ), #5718, .T. ) ;
#107946=CARTESIAN_POINT ( 'NONE',  ( 4.600000000000001421, 9.521314400968980422E-16, 0.000000000000000000 ) ) ;
#107968=EDGE_LOOP ( 'NONE', ( #82525, #102875, #143077, #97028, #59134 ) ) ;
#108005=ORIENTED_EDGE ( 'NONE', *, *, #23196, .F. ) ;
#108046=CARTESIAN_POINT ( 'NONE',  ( 15.20840764549667767, 9.139736423841732040E-16, 0.000000000000000000 ) ) ;
#108049=DIRECTION ( 'NONE',  ( 0.000000000000000000, -1.000000000000000000, 0.000000000000000000 ) ) ;
#108067=DIRECTION ( 'NONE',  ( -1.000000000000000000, -1.224606353822377258E-16, -0.000000000000000000 ) ) ;
#108087=AXIS2_PLACEMENT_3D ( 'NONE', #133941, #105566, #28761 ) ;
#108124=CARTESIAN_POINT ( 'NONE',  ( 10.06000000000000050, 9.521314400968980422E-16, 0.000000000000000000 ) ) ;
#108159=EDGE_CURVE ( 'NONE', #28445, #52993, #12685, .T. ) ;
#108196=ORIENTED_EDGE ( 'NONE', *, *, #20731, .F. ) ;
#108208=VECTOR ( 'NONE', #105483, 1000.000000000000114 ) ;
#108213=CARTESIAN_POINT ( 'NONE',  ( 22.22840764549667725, 9.139736423841732040E-16, 0.000000000000000000 ) ) ;
#108271=DIRECTION ( 'NONE',  ( 0.000000000000000000, -1.000000000000000000, 0.000000000000000000 ) ) ;
#108276=CONICAL_SURFACE ( 'NONE', #78323, 2.500000000000000888, 0.9599310885968822538 ) ;
#108286=ORIENTED_EDGE ( 'NONE', *, *, #12785, .T. ) ;
#108321=ORIENTED_EDGE ( 'NONE', *, *, #122099, .F. ) ;
#108323=VECTOR ( 'NONE', #141014, 1000.000000000000000 ) ;
#108325=EDGE_LOOP ( 'NONE', ( #41117, #11373, #31531, #7883, #86176 ) ) ;
#108329=VERTEX_POINT ( 'NONE', #38045 ) ;
#108376=ORIENTED_EDGE ( 'NONE', *, *, #107903, .T. ) ;
#108379=AXIS2_PLACEMENT_3D ( 'NONE', #109587, #33493, #19717 ) ;
#108418=VERTEX_POINT ( 'NONE', #98812 ) ;
#108422=ADVANCED_FACE ( 'NONE', ( #30741 ), #96291, .T. ) ;
#108423=DIRECTION ( 'NONE',  ( 0.000000000000000000, 1.000000000000000000, 0.000000000000000000 ) ) ;
#108442=CARTESIAN_POINT ( 'NONE',  ( 18.63999999999999702, 9.521314400968980422E-16, 0.000000000000000000 ) ) ;
#108448=VERTEX_POINT ( 'NONE', #88690 ) ;
#108468=DIRECTION ( 'NONE',  ( -1.000000000000000000, -1.224606353822377258E-16, -0.000000000000000000 ) ) ;
#108507=CARTESIAN_POINT ( 'NONE',  ( 10.83999999999999986, -2.055000000000000160, 0.000000000000000000 ) ) ;
#108511=CIRCLE ( 'NONE', #138691, 2.500000000000000888 ) ;
#108522=CIRCLE ( 'NONE', #83123, 2.500000000000000888 ) ;
#108528=EDGE_CURVE ( 'NONE', #101812, #13435, #37145, .T. ) ;
#108569=AXIS2_PLACEMENT_3D ( 'NONE', #32209, #139574, #40257 ) ;
#108597=VERTEX_POINT ( 'NONE', #68383 ) ;
#108606=CARTESIAN_POINT ( 'NONE',  ( 27.68840764549667455, -3.851859888774471706E-31, 2.500000000000001332 ) ) ;
#108661=CARTESIAN_POINT ( 'NONE',  ( 13.49159235450332162, 9.902892378096218942E-16, 0.000000000000000000 ) ) ;
#108672=CIRCLE ( 'NONE', #136539, 2.500000000000000888 ) ;
#108687=EDGE_LOOP ( 'NONE', ( #12114, #64559, #682, #6670 ) ) ;
#108694=DIRECTION ( 'NONE',  ( -1.000000000000000000, -1.224606353822377258E-16, -0.000000000000000000 ) ) ;
#108737=CARTESIAN_POINT ( 'NONE',  ( 20.97999999999999687, 9.521314400968980422E-16, 0.000000000000000000 ) ) ;
#108760=CARTESIAN_POINT ( 'NONE',  ( 0.4427966827908959013, -0.5999999999999994227, -4.147834322102035287 ) ) ;
#108809=CIRCLE ( 'NONE', #25534, 4.582731094065999322 ) ;
#108820=ORIENTED_EDGE ( 'NONE', *, *, #60358, .F. ) ;
#108822=CIRCLE ( 'NONE', #44, 2.500000000000000888 ) ;
#108825=EDGE_CURVE ( 'NONE', #7326, #6269, #3768, .T. ) ;
#108876=CARTESIAN_POINT ( 'NONE',  ( 19.73159235450332005, 9.902892378096218942E-16, 0.000000000000000000 ) ) ;
#108878=CIRCLE ( 'NONE', #4744, 2.500000000000000888 ) ;
#108901=DIRECTION ( 'NONE',  ( -1.000000000000000000, -1.224606353822377258E-16, -0.000000000000000000 ) ) ;
#108930=DIRECTION ( 'NONE',  ( 0.000000000000000000, 0.000000000000000000, 1.000000000000000000 ) ) ;
#108979=ORIENTED_EDGE ( 'NONE', *, *, #112227, .T. ) ;
#109075=CARTESIAN_POINT ( 'NONE',  ( 15.20840764549667767, 9.139736423841732040E-16, 0.000000000000000000 ) ) ;
#109086=CARTESIAN_POINT ( 'NONE',  ( 8.811592354503320124, 9.902892378096218942E-16, 0.000000000000000000 ) ) ;
#109091=DIRECTION ( 'NONE',  ( -1.000000000000000000, -1.224606353822377258E-16, -0.000000000000000000 ) ) ;
#109094=VERTEX_POINT ( 'NONE', #94896 ) ;
#109123=ORIENTED_EDGE ( 'NONE', *, *, #141152, .F. ) ;
#109127=EDGE_LOOP ( 'NONE', ( #80938, #128487, #6485, #26600, #4993 ) ) ;
#109150=CIRCLE ( 'NONE', #106754, 2.500000000000000888 ) ;
#109156=VERTEX_POINT ( 'NONE', #126134 ) ;
#109188=CIRCLE ( 'NONE', #18832, 2.055000000000001048 ) ;
#109226=CARTESIAN_POINT ( 'NONE',  ( 22.07159235450331991, 9.902892378096218942E-16, 0.000000000000000000 ) ) ;
#109229=EDGE_CURVE ( 'NONE', #80743, #87397, #68658, .T. ) ;
#109233=ORIENTED_EDGE ( 'NONE', *, *, #32972, .T. ) ;
#109274=CIRCLE ( 'NONE', #39876, 2.500000000000000888 ) ;
#109279=CARTESIAN_POINT ( 'NONE',  ( 5.380000000000000782, 2.055000000000001492, 0.000000000000000000 ) ) ;
#109310=CARTESIAN_POINT ( 'NONE',  ( 18.63999999999999702, 2.055000000000001492, 0.000000000000000000 ) ) ;
#109314=AXIS2_PLACEMENT_3D ( 'NONE', #41312, #22398, #33354 ) ;
#109323=VERTEX_POINT ( 'NONE', #34812 ) ;
#109331=DIRECTION ( 'NONE',  ( -1.000000000000000000, -1.224606353822377258E-16, -0.000000000000000000 ) ) ;
#109404=ORIENTED_EDGE ( 'NONE', *, *, #116627, .T. ) ;
#109494=ORIENTED_EDGE ( 'NONE', *, *, #12283, .T. ) ;
#109503=ORIENTED_EDGE ( 'NONE', *, *, #1429, .T. ) ;
#109567=ADVANCED_FACE ( 'NONE', ( #45538 ), #89714, .T. ) ;
#109572=EDGE_LOOP ( 'NONE', ( #41373, #53033, #89051, #18982, #15255 ) ) ;
#109587=CARTESIAN_POINT ( 'NONE',  ( 6.471592354503322042, 9.902892378096218942E-16, 0.000000000000000000 ) ) ;
#109602=DIRECTION ( 'NONE',  ( -1.000000000000000000, -1.224606353822377258E-16, -0.000000000000000000 ) ) ;
#109681=DIRECTION ( 'NONE',  ( 0.000000000000000000, -1.000000000000000000, 0.000000000000000000 ) ) ;
#109693=VERTEX_POINT ( 'NONE', #37500 ) ;
#109771=AXIS2_PLACEMENT_3D ( 'NONE', #79921, #13867, #21913 ) ;
#109784=CARTESIAN_POINT ( 'NONE',  ( 15.98840764549667703, -2.500000000000000888, 0.000000000000000000 ) ) ;
#109800=EDGE_LOOP ( 'NONE', ( #121315, #9328, #116235, #138966, #84176 ) ) ;
#109809=EDGE_CURVE ( 'NONE', #79885, #102792, #89589, .T. ) ;
#109816=CARTESIAN_POINT ( 'NONE',  ( -25.39999999999996305, 3.061616997868383141E-16, -2.500000000000000000 ) ) ;
#109822=DIRECTION ( 'NONE',  ( -1.000000000000000000, -1.224606353822377258E-16, -0.000000000000000000 ) ) ;
#109823=ORIENTED_EDGE ( 'NONE', *, *, #59351, .F. ) ;
#109831=VECTOR ( 'NONE', #62887, 1000.000000000000114 ) ;
#109841=LINE ( 'NONE', #110529, #95140 ) ;
#109850=VECTOR ( 'NONE', #14004, 1000.000000000000000 ) ;
#109866=FACE_OUTER_BOUND ( 'NONE', #57539, .T. ) ;
#109868=CONICAL_SURFACE ( 'NONE', #12679, 2.055000000000001048, 0.9599310885968758145 ) ;
#109877=CARTESIAN_POINT ( 'NONE',  ( 15.05159235450332034, -3.851859888774471706E-31, 2.500000000000001332 ) ) ;
#109950=EDGE_CURVE ( 'NONE', #16237, #39945, #38791, .T. ) ;
#109957=ORIENTED_EDGE ( 'NONE', *, *, #69236, .F. ) ;
#109972=CIRCLE ( 'NONE', #66043, 2.055000000000001048 ) ;
#109975=CIRCLE ( 'NONE', #107601, 2.500000000000000888 ) ;
#109979=CARTESIAN_POINT ( 'NONE',  ( 24.41159235450331977, 2.500000000000001776, 0.000000000000000000 ) ) ;
#109987=ADVANCED_FACE ( 'NONE', ( #74048 ), #96470, .T. ) ;
#110004=ORIENTED_EDGE ( 'NONE', *, *, #104091, .T. ) ;
#110031=ADVANCED_FACE ( 'NONE', ( #29113 ), #142892, .T. ) ;
#110038=CARTESIAN_POINT ( 'NONE',  ( -25.39999999999996305, 3.061616997868383141E-16, -2.500000000000000000 ) ) ;
#110056=EDGE_CURVE ( 'NONE', #36671, #94039, #39289, .T. ) ;
#110059=VERTEX_POINT ( 'NONE', #85613 ) ;
#110060=ORIENTED_EDGE ( 'NONE', *, *, #55104, .F. ) ;
#110064=CYLINDRICAL_SURFACE ( 'NONE', #105584, 2.500000000000000000 ) ;
#110071=EDGE_CURVE ( 'NONE', #92828, #82762, #73467, .T. ) ;
#110095=ORIENTED_EDGE ( 'NONE', *, *, #133318, .F. ) ;
#110130=VERTEX_POINT ( 'NONE', #20351 ) ;
#110140=FACE_OUTER_BOUND ( 'NONE', #5028, .T. ) ;
#110144=FACE_OUTER_BOUND ( 'NONE', #94461, .T. ) ;
#110196=CARTESIAN_POINT ( 'NONE',  ( 8.811592354503320124, 9.902892378096218942E-16, 0.000000000000000000 ) ) ;
#110206=CARTESIAN_POINT ( 'NONE',  ( 18.95159235450331892, 9.902892378096218942E-16, 0.000000000000000000 ) ) ;
#110245=VECTOR ( 'NONE', #120048, 999.9999999999998863 ) ;
#110319=CARTESIAN_POINT ( 'NONE',  ( -25.39999999999996305, 0.000000000000000000, 0.000000000000000000 ) ) ;
#110321=EDGE_LOOP ( 'NONE', ( #125563, #37630, #42998, #26285, #102551 ) ) ;
#110325=VERTEX_POINT ( 'NONE', #3586 ) ;
#110393=DIRECTION ( 'NONE',  ( 1.000000000000000000, 1.224606353822377258E-16, 0.000000000000000000 ) ) ;
#110398=DIRECTION ( 'NONE',  ( 0.000000000000000000, -1.000000000000000000, 0.000000000000000000 ) ) ;
#110455=CARTESIAN_POINT ( 'NONE',  ( 8.031592354503320763, -3.851859888774471706E-31, 2.500000000000001332 ) ) ;
#110475=LINE ( 'NONE', #53248, #44156 ) ;
#110492=CARTESIAN_POINT ( 'NONE',  ( 11.62000000000000099, 2.055000000000001492, 2.516649172247811554E-16 ) ) ;
#110511=DIRECTION ( 'NONE',  ( 0.000000000000000000, -1.000000000000000000, 0.000000000000000000 ) ) ;
#110512=CIRCLE ( 'NONE', #59658, 2.500000000000000888 ) ;
#110522=EDGE_LOOP ( 'NONE', ( #32010, #96988, #42292, #33448, #131198, #4140 ) ) ;
#110525=VERTEX_POINT ( 'NONE', #141255 ) ;
#110529=CARTESIAN_POINT ( 'NONE',  ( -25.39999999999996305, 0.000000000000000000, 2.500000000000000000 ) ) ;
#110552=DIRECTION ( 'NONE',  ( -1.000000000000000000, -0.000000000000000000, -0.000000000000000000 ) ) ;
#110570=CIRCLE ( 'NONE', #71200, 2.055000000000001048 ) ;
#110576=ADVANCED_FACE ( 'NONE', ( #33955 ), #38473, .T. ) ;
#110599=CARTESIAN_POINT ( 'NONE',  ( 24.87999999999999901, -2.055000000000000160, 2.789133085058098087E-16 ) ) ;
#110614=ORIENTED_EDGE ( 'NONE', *, *, #29899, .T. ) ;
#110662=DIRECTION ( 'NONE',  ( 1.000000000000000000, 1.224606353822377258E-16, 0.000000000000000000 ) ) ;
#110693=VERTEX_POINT ( 'NONE', #112225 ) ;
#110702=DIRECTION ( 'NONE',  ( -0.5735764363510503783, -0.8191520442889886899, 0.000000000000000000 ) ) ;
#110703=DIRECTION ( 'NONE',  ( 0.000000000000000000, -1.000000000000000000, 0.000000000000000000 ) ) ;
#110707=VECTOR ( 'NONE', #8287, 999.9999999999998863 ) ;
#110720=ORIENTED_EDGE ( 'NONE', *, *, #56680, .T. ) ;
#110732=LINE ( 'NONE', #31087, #63293 ) ;
#110744=DIRECTION ( 'NONE',  ( 0.000000000000000000, -1.000000000000000000, 0.000000000000000000 ) ) ;
#110760=AXIS2_PLACEMENT_3D ( 'NONE', #108442, #96855, #121491 ) ;
#110803=FACE_OUTER_BOUND ( 'NONE', #95458, .T. ) ;
#110810=DIRECTION ( 'NONE',  ( 1.000000000000000000, 1.224606353822377258E-16, 0.000000000000000000 ) ) ;
#110813=CARTESIAN_POINT ( 'NONE',  ( 25.19159235450331735, 9.902892378096218942E-16, 0.000000000000000000 ) ) ;
#110910=DIRECTION ( 'NONE',  ( 0.000000000000000000, 1.000000000000000000, 0.000000000000000000 ) ) ;
#110923=ADVANCED_FACE ( 'NONE', ( #7709 ), #10801, .T. ) ;
#110933=ORIENTED_EDGE ( 'NONE', *, *, #74113, .T. ) ;
#110968=CARTESIAN_POINT ( 'NONE',  ( 4.911592354503321545, 2.500000000000001776, 0.000000000000000000 ) ) ;
#110969=ORIENTED_EDGE ( 'NONE', *, *, #116123, .T. ) ;
#110972=PRESENTATION_STYLE_ASSIGNMENT (( #99382 ) ) ;
#110980=ORIENTED_EDGE ( 'NONE', *, *, #86127, .F. ) ;
#110985=ADVANCED_FACE ( 'NONE', ( #30186 ), #80304, .T. ) ;
#111008=AXIS2_PLACEMENT_3D ( 'NONE', #13208, #133602, #21960 ) ;
#111052=DIRECTION ( 'NONE',  ( 0.5735764363510453823, -0.8191520442889923537, 1.003171929053525486E-16 ) ) ;
#111060=DIRECTION ( 'NONE',  ( -1.000000000000000000, -1.224606353822377258E-16, -0.000000000000000000 ) ) ;
#111077=DIRECTION ( 'NONE',  ( 0.000000000000000000, -1.000000000000000000, 0.000000000000000000 ) ) ;
#111097=EDGE_CURVE ( 'NONE', #5504, #35419, #90273, .T. ) ;
#111119=CIRCLE ( 'NONE', #67170, 2.500000000000000888 ) ;
#111120=DIRECTION ( 'NONE',  ( 0.000000000000000000, -1.000000000000000000, 0.000000000000000000 ) ) ;
#111133=ORIENTED_EDGE ( 'NONE', *, *, #78011, .T. ) ;
#111154=DIRECTION ( 'NONE',  ( 0.000000000000000000, -1.000000000000000000, 0.000000000000000000 ) ) ;
#111189=ORIENTED_EDGE ( 'NONE', *, *, #114486, .F. ) ;
#111219=FACE_OUTER_BOUND ( 'NONE', #107640, .T. ) ;
#111234=CARTESIAN_POINT ( 'NONE',  ( 7.251592354503322291, 9.902892378096218942E-16, 0.000000000000000000 ) ) ;
#111244=VECTOR ( 'NONE', #117425, 1000.000000000000000 ) ;
#111259=CARTESIAN_POINT ( 'NONE',  ( -25.39999999999996305, 0.000000000000000000, 0.000000000000000000 ) ) ;
#111302=CARTESIAN_POINT ( 'NONE',  ( 8.500000000000000000, -2.055000000000000160, 2.789133085058098087E-16 ) ) ;
#111306=VECTOR ( 'NONE', #124282, 999.9999999999998863 ) ;
#111339=AXIS2_PLACEMENT_3D ( 'NONE', #135679, #25459, #81311 ) ;
#111346=CARTESIAN_POINT ( 'NONE',  ( 8.188407645496676324, 3.061616997868380183E-16, -2.500000000000001332 ) ) ;
#111358=ORIENTED_EDGE ( 'NONE', *, *, #29107, .T. ) ;
#111361=VERTEX_POINT ( 'NONE', #64808 ) ;
#111370=CARTESIAN_POINT ( 'NONE',  ( 1.199999999999999956, -0.5999999999999993117, -4.543283425070392845 ) ) ;
#111377=CIRCLE ( 'NONE', #48912, 2.500000000000000888 ) ;
#111460=CARTESIAN_POINT ( 'NONE',  ( -25.39999999999996305, 0.000000000000000000, 0.000000000000000000 ) ) ;
#111486=ORIENTED_EDGE ( 'NONE', *, *, #91474, .F. ) ;
#111502=FACE_OUTER_BOUND ( 'NONE', #81945, .T. ) ;
#111540=EDGE_CURVE ( 'NONE', #110325, #11989, #124357, .T. ) ;
#111542=ORIENTED_EDGE ( 'NONE', *, *, #27395, .T. ) ;
#111559=LINE ( 'NONE', #125302, #31833 ) ;
#111564=ORIENTED_EDGE ( 'NONE', *, *, #19754, .T. ) ;
#111600=EDGE_CURVE ( 'NONE', #56418, #76475, #131294, .T. ) ;
#111702=VECTOR ( 'NONE', #104794, 1000.000000000000000 ) ;
#111716=CYLINDRICAL_SURFACE ( 'NONE', #94311, 2.500000000000000000 ) ;
#111732=FACE_OUTER_BOUND ( 'NONE', #56548, .T. ) ;
#111754=ORIENTED_EDGE ( 'NONE', *, *, #10040, .T. ) ;
#111909=DIRECTION ( 'NONE',  ( 0.000000000000000000, -1.000000000000000000, 0.000000000000000000 ) ) ;
#111930=DIRECTION ( 'NONE',  ( 1.000000000000000000, 1.224606353822377258E-16, 0.000000000000000000 ) ) ;
#111960=ORIENTED_EDGE ( 'NONE', *, *, #60446, .F. ) ;
#111961=CIRCLE ( 'NONE', #68015, 2.500000000000000888 ) ;
#111970=VECTOR ( 'NONE', #61356, 1000.000000000000000 ) ;
#111999=VERTEX_POINT ( 'NONE', #98341 ) ;
#112025=CIRCLE ( 'NONE', #24053, 2.500000000000000000 ) ;
#112034=DIRECTION ( 'NONE',  ( 1.000000000000000000, 1.224606353822377258E-16, 0.000000000000000000 ) ) ;
#112040=CARTESIAN_POINT ( 'NONE',  ( 18.63999999999999702, 9.521314400968980422E-16, 0.000000000000000000 ) ) ;
#112083=ORIENTED_EDGE ( 'NONE', *, *, #15862, .T. ) ;
#112101=CARTESIAN_POINT ( 'NONE',  ( 23.00840764549667483, 2.500000000000003553, 3.061616997868386099E-16 ) ) ;
#112184=AXIS2_PLACEMENT_3D ( 'NONE', #47044, #112243, #33292 ) ;
#112187=LINE ( 'NONE', #32477, #116219 ) ;
#112208=CARTESIAN_POINT ( 'NONE',  ( -25.39999999999996305, 3.061616997868383141E-16, -2.500000000000000000 ) ) ;
#112225=CARTESIAN_POINT ( 'NONE',  ( 18.32840764549667512, -2.499999999999996003, 0.000000000000000000 ) ) ;
#112227=EDGE_CURVE ( 'NONE', #95905, #51588, #13289, .T. ) ;
#112230=CIRCLE ( 'NONE', #49736, 2.055000000000001048 ) ;
#112243=DIRECTION ( 'NONE',  ( -1.000000000000000000, -0.000000000000000000, -0.000000000000000000 ) ) ;
#112249=CIRCLE ( 'NONE', #49763, 2.500000000000000888 ) ;
#112250=CARTESIAN_POINT ( 'NONE',  ( 6.628407645496676714, 2.500000000000003553, 3.061616997868386099E-16 ) ) ;
#112261=CARTESIAN_POINT ( 'NONE',  ( 8.968407645496675684, -2.499999999999998224, 0.000000000000000000 ) ) ;
#112275=VERTEX_POINT ( 'NONE', #17710 ) ;
#112279=DIRECTION ( 'NONE',  ( -1.000000000000000000, -1.224606353822377258E-16, -0.000000000000000000 ) ) ;
#112289=EDGE_CURVE ( 'NONE', #117339, #121372, #64337, .T. ) ;
#112338=ORIENTED_EDGE ( 'NONE', *, *, #105638, .T. ) ;
#112405=CARTESIAN_POINT ( 'NONE',  ( 25.19159235450331735, -2.500000000000000444, 3.061616997868384620E-16 ) ) ;
#112444=DIRECTION ( 'NONE',  ( 0.000000000000000000, 1.000000000000000000, 0.000000000000000000 ) ) ;
#112446=DIRECTION ( 'NONE',  ( 0.000000000000000000, -1.000000000000000000, 0.000000000000000000 ) ) ;
#112462=EDGE_LOOP ( 'NONE', ( #85982, #61669, #77204, #12890, #4372, #93766 ) ) ;
#112478=ORIENTED_EDGE ( 'NONE', *, *, #55104, .T. ) ;
#112485=EDGE_CURVE ( 'NONE', #786, #71528, #101000, .T. ) ;
#112488=ORIENTED_EDGE ( 'NONE', *, *, #95665, .F. ) ;
#112505=ORIENTED_EDGE ( 'NONE', *, *, #95376, .T. ) ;
#112514=ORIENTED_EDGE ( 'NONE', *, *, #58532, .F. ) ;
#112543=FACE_OUTER_BOUND ( 'NONE', #139237, .T. ) ;
#112565=CARTESIAN_POINT ( 'NONE',  ( 12.40000000000000213, 2.055000000000001492, 0.000000000000000000 ) ) ;
#112573=ADVANCED_FACE ( 'NONE', ( #77840 ), #135786, .T. ) ;
#112579=ORIENTED_EDGE ( 'NONE', *, *, #99875, .T. ) ;
#112580=CARTESIAN_POINT ( 'NONE',  ( 11.93159235450332112, 9.902892378096218942E-16, 0.000000000000000000 ) ) ;
#112649=CARTESIAN_POINT ( 'NONE',  ( 1.199999999999999956, -0.5999999999999993117, -4.750000000000000000 ) ) ;
#112705=DIRECTION ( 'NONE',  ( -1.000000000000000000, -1.224606353822377258E-16, -0.000000000000000000 ) ) ;
#112775=ADVANCED_FACE ( 'NONE', ( #67135 ), #8902, .T. ) ;
#112837=VERTEX_POINT ( 'NONE', #110599 ) ;
#112843=DIRECTION ( 'NONE',  ( -0.5735764363510507113, 0.8191520442889885789, 1.003171929053520926E-16 ) ) ;
#112856=AXIS2_PLACEMENT_3D ( 'NONE', #2554, #46862, #91049 ) ;
#112933=LINE ( 'NONE', #13599, #73234 ) ;
#112948=DIRECTION ( 'NONE',  ( 0.000000000000000000, -1.000000000000000000, 0.000000000000000000 ) ) ;
#112982=DIRECTION ( 'NONE',  ( 0.000000000000000000, -1.000000000000000000, 0.000000000000000000 ) ) ;
#113010=CIRCLE ( 'NONE', #94487, 2.500000000000000888 ) ;
#113027=CARTESIAN_POINT ( 'NONE',  ( 25.97159235450331849, 3.061616997868380183E-16, -2.500000000000001332 ) ) ;
#113035=CYLINDRICAL_SURFACE ( 'NONE', #23972, 2.500000000000000000 ) ;
#113068=CARTESIAN_POINT ( 'NONE',  ( -25.39999999999996305, 0.000000000000000000, 2.500000000000000000 ) ) ;
#113110=VECTOR ( 'NONE', #16943, 999.9999999999998863 ) ;
#113128=VERTEX_POINT ( 'NONE', #130634 ) ;
#113131=ORIENTED_EDGE ( 'NONE', *, *, #8587, .T. ) ;
#113184=ORIENTED_EDGE ( 'NONE', *, *, #120577, .F. ) ;
#113224=CARTESIAN_POINT ( 'NONE',  ( -25.39999999999996305, 0.000000000000000000, 0.000000000000000000 ) ) ;
#113278=DIRECTION ( 'NONE',  ( 0.000000000000000000, -1.000000000000000000, 0.000000000000000000 ) ) ;
#113284=ORIENTED_EDGE ( 'NONE', *, *, #84478, .T. ) ;
#113348=DIRECTION ( 'NONE',  ( 0.000000000000000000, 0.000000000000000000, 1.000000000000000000 ) ) ;
#113417=VECTOR ( 'NONE', #102393, 1000.000000000000000 ) ;
#113452=CIRCLE ( 'NONE', #46348, 2.055000000000001048 ) ;
#113498=CIRCLE ( 'NONE', #97336, 2.500000000000000888 ) ;
#113504=CIRCLE ( 'NONE', #51033, 2.055000000000001048 ) ;
#113514=ORIENTED_EDGE ( 'NONE', *, *, #92157, .F. ) ;
#113518=EDGE_CURVE ( 'NONE', #98020, #136003, #87716, .T. ) ;
#113525=CONICAL_SURFACE ( 'NONE', #34913, 2.500000000000000888, 0.9599310885968822538 ) ;
#113538=VERTEX_POINT ( 'NONE', #112261 ) ;
#113559=AXIS2_PLACEMENT_3D ( 'NONE', #39042, #29578, #49941 ) ;
#113577=DIRECTION ( 'NONE',  ( 0.000000000000000000, -1.000000000000000000, 0.000000000000000000 ) ) ;
#113589=ORIENTED_EDGE ( 'NONE', *, *, #128913, .T. ) ;
#113611=EDGE_LOOP ( 'NONE', ( #41472, #95468, #12753, #69062 ) ) ;
#113613=DIRECTION ( 'NONE',  ( 0.000000000000000000, 0.000000000000000000, 1.000000000000000000 ) ) ;
#113617=ORIENTED_EDGE ( 'NONE', *, *, #59372, .T. ) ;
#113623=DIRECTION ( 'NONE',  ( 0.000000000000000000, 0.000000000000000000, 1.000000000000000000 ) ) ;
#113637=DIRECTION ( 'NONE',  ( 0.000000000000000000, -1.000000000000000000, 0.000000000000000000 ) ) ;
#113640=ORIENTED_EDGE ( 'NONE', *, *, #77160, .T. ) ;
#113645=CIRCLE ( 'NONE', #16342, 2.500000000000000888 ) ;
#113719=CARTESIAN_POINT ( 'NONE',  ( 9.748407645496676821, -2.499999999999998224, 0.000000000000000000 ) ) ;
#113725=VERTEX_POINT ( 'NONE', #2006 ) ;
#113766=DIRECTION ( 'NONE',  ( 0.000000000000000000, -1.000000000000000000, 0.000000000000000000 ) ) ;
#113805=VERTEX_POINT ( 'NONE', #38264 ) ;
#113814=EDGE_CURVE ( 'NONE', #109323, #96749, #14363, .T. ) ;
#113827=DIRECTION ( 'NONE',  ( -1.000000000000000000, -1.224606353822377258E-16, -0.000000000000000000 ) ) ;
#113847=EDGE_LOOP ( 'NONE', ( #128454, #115237, #142208, #123095, #82216 ) ) ;
#113872=ADVANCED_FACE ( 'NONE', ( #18612 ), #130284, .F. ) ;
#113932=CARTESIAN_POINT ( 'NONE',  ( -25.39999999999996305, 0.000000000000000000, 2.500000000000000000 ) ) ;
#113944=ORIENTED_EDGE ( 'NONE', *, *, #139180, .T. ) ;
#113946=EDGE_CURVE ( 'NONE', #132528, #86782, #124869, .T. ) ;
#113950=CARTESIAN_POINT ( 'NONE',  ( 5.068407645496677105, 9.139736423841732040E-16, 0.000000000000000000 ) ) ;
#113988=EDGE_LOOP ( 'NONE', ( #69161, #102111, #36635, #123282, #139061, #117645 ) ) ;
#113993=AXIS2_PLACEMENT_3D ( 'NONE', #27833, #105382, #25687 ) ;
#114027=DIRECTION ( 'NONE',  ( -1.000000000000000000, -1.224606353822377258E-16, -0.000000000000000000 ) ) ;
#114072=VECTOR ( 'NONE', #122746, 1000.000000000000000 ) ;
#114073=VERTEX_POINT ( 'NONE', #97617 ) ;
#114079=VERTEX_POINT ( 'NONE', #141879 ) ;
#114087=CIRCLE ( 'NONE', #93285, 2.055000000000001048 ) ;
#114146=CARTESIAN_POINT ( 'NONE',  ( 17.85999999999999943, -2.055000000000000160, 0.000000000000000000 ) ) ;
#114170=CARTESIAN_POINT ( 'NONE',  ( 19.10840764549667270, -2.500000000000000888, 0.000000000000000000 ) ) ;
#114234=ADVANCED_FACE ( 'NONE', ( #105461 ), #6126, .T. ) ;
#114237=ORIENTED_EDGE ( 'NONE', *, *, #55127, .T. ) ;
#114251=EDGE_LOOP ( 'NONE', ( #76940, #106345, #31262, #55714, #105037 ) ) ;
#114298=COLOUR_RGB ( '', 0.09019608, 0.27058824, 0.51372549) ;
#114405=EDGE_CURVE ( 'NONE', #94039, #81745, #30057, .T. ) ;
#114428=ORIENTED_EDGE ( 'NONE', *, *, #139762, .F. ) ;
#114486=EDGE_CURVE ( 'NONE', #54110, #125050, #2299, .T. ) ;
#114490=AXIS2_PLACEMENT_3D ( 'NONE', #143113, #111930, #12587 ) ;
#114512=CARTESIAN_POINT ( 'NONE',  ( -25.39999999999996305, 0.000000000000000000, 0.000000000000000000 ) ) ;
#114534=AXIS2_PLACEMENT_3D ( 'NONE', #1314, #70222, #12909 ) ;
#114547=EDGE_CURVE ( 'NONE', #138330, #47703, #68446, .T. ) ;
#114552=DIRECTION ( 'NONE',  ( -1.000000000000000000, -1.224606353822377258E-16, -0.000000000000000000 ) ) ;
#114595=DIRECTION ( 'NONE',  ( 0.000000000000000000, -1.000000000000000000, 0.000000000000000000 ) ) ;
#114601=CARTESIAN_POINT ( 'NONE',  ( 20.19999999999999929, 9.521314400968980422E-16, 0.000000000000000000 ) ) ;
#114627=CIRCLE ( 'NONE', #133192, 2.500000000000000888 ) ;
#114651=CARTESIAN_POINT ( 'NONE',  ( 8.811592354503320124, 9.902892378096218942E-16, 0.000000000000000000 ) ) ;
#114766=FACE_OUTER_BOUND ( 'NONE', #34361, .T. ) ;
#114769=DIRECTION ( 'NONE',  ( -1.000000000000000000, -1.224606353822377258E-16, -0.000000000000000000 ) ) ;
#114836=ORIENTED_EDGE ( 'NONE', *, *, #44948, .F. ) ;
#114845=ORIENTED_EDGE ( 'NONE', *, *, #125134, .F. ) ;
#114869=AXIS2_PLACEMENT_3D ( 'NONE', #103567, #70302, #59408 ) ;
#114882=CIRCLE ( 'NONE', #117175, 2.500000000000000888 ) ;
#114900=AXIS2_PLACEMENT_3D ( 'NONE', #27321, #71572, #115732 ) ;
#114906=VECTOR ( 'NONE', #112843, 1000.000000000000000 ) ;
#114918=DIRECTION ( 'NONE',  ( -1.000000000000000000, -1.224606353822377258E-16, -0.000000000000000000 ) ) ;
#114925=ORIENTED_EDGE ( 'NONE', *, *, #116184, .F. ) ;
#114929=EDGE_CURVE ( 'NONE', #6269, #7326, #134401, .T. ) ;
#114943=ORIENTED_EDGE ( 'NONE', *, *, #20091, .T. ) ;
#114958=ORIENTED_EDGE ( 'NONE', *, *, #24623, .T. ) ;
#114980=VECTOR ( 'NONE', #35239, 1000.000000000000000 ) ;
#115012=CARTESIAN_POINT ( 'NONE',  ( -25.39999999999996305, 0.000000000000000000, 0.000000000000000000 ) ) ;
#115014=VERTEX_POINT ( 'NONE', #83961 ) ;
#115045=DIRECTION ( 'NONE',  ( -0.5735764363510507113, 0.8191520442889885789, 1.003171929053520926E-16 ) ) ;
#115087=CARTESIAN_POINT ( 'NONE',  ( 11.93159235450332112, -2.500000000000000444, 3.061616997868384620E-16 ) ) ;
#115095=VERTEX_POINT ( 'NONE', #130308 ) ;
#115126=CARTESIAN_POINT ( 'NONE',  ( 7.408407645496676963, -2.499999999999999556, 0.000000000000000000 ) ) ;
#115162=ORIENTED_EDGE ( 'NONE', *, *, #10344, .F. ) ;
#115170=FACE_OUTER_BOUND ( 'NONE', #97788, .T. ) ;
#115208=CIRCLE ( 'NONE', #105915, 2.500000000000000888 ) ;
#115213=ORIENTED_EDGE ( 'NONE', *, *, #140376, .F. ) ;
#115214=VERTEX_POINT ( 'NONE', #133166 ) ;
#115228=ORIENTED_EDGE ( 'NONE', *, *, #85241, .F. ) ;
#115237=ORIENTED_EDGE ( 'NONE', *, *, #95218, .T. ) ;
#115277=EDGE_CURVE ( 'NONE', #79589, #24205, #58496, .T. ) ;
#115287=DIRECTION ( 'NONE',  ( -1.000000000000000000, -1.224606353822377258E-16, -0.000000000000000000 ) ) ;
#115298=DIRECTION ( 'NONE',  ( -1.000000000000000000, -1.224606353822377258E-16, -0.000000000000000000 ) ) ;
#115318=VECTOR ( 'NONE', #17614, 1000.000000000000000 ) ;
#115330=ORIENTED_EDGE ( 'NONE', *, *, #90738, .T. ) ;
#115362=ORIENTED_EDGE ( 'NONE', *, *, #34512, .T. ) ;
#115388=ORIENTED_EDGE ( 'NONE', *, *, #4273, .F. ) ;
#115438=CIRCLE ( 'NONE', #18273, 2.500000000000000888 ) ;
#115462=FACE_OUTER_BOUND ( 'NONE', #79561, .T. ) ;
#115473=CYLINDRICAL_SURFACE ( 'NONE', #141836, 2.500000000000000000 ) ;
#115481=EDGE_CURVE ( 'NONE', #118031, #11132, #110475, .T. ) ;
#115486=DIRECTION ( 'NONE',  ( 0.000000000000000000, 1.000000000000000000, 0.000000000000000000 ) ) ;
#115499=CIRCLE ( 'NONE', #136338, 2.055000000000001048 ) ;
#115568=ORIENTED_EDGE ( 'NONE', *, *, #75675, .F. ) ;
#115576=CARTESIAN_POINT ( 'NONE',  ( 2.999999999999999112, 0.000000000000000000, 0.000000000000000000 ) ) ;
#115611=EDGE_CURVE ( 'NONE', #68485, #91029, #97411, .T. ) ;
#115652=EDGE_CURVE ( 'NONE', #136003, #64283, #134608, .T. ) ;
#115657=EDGE_LOOP ( 'NONE', ( #136757, #138675, #110933, #8570, #115362 ) ) ;
#115681=ORIENTED_EDGE ( 'NONE', *, *, #132277, .T. ) ;
#115682=DIRECTION ( 'NONE',  ( 0.000000000000000000, -1.000000000000000000, 0.000000000000000000 ) ) ;
#115732=DIRECTION ( 'NONE',  ( 0.000000000000000000, -1.000000000000000000, 0.000000000000000000 ) ) ;
#115754=AXIS2_PLACEMENT_3D ( 'NONE', #64595, #75481, #41403 ) ;
#115758=ORIENTED_EDGE ( 'NONE', *, *, #62200, .F. ) ;
#115761=AXIS2_PLACEMENT_3D ( 'NONE', #13185, #124831, #48012 ) ;
#115828=VERTEX_POINT ( 'NONE', #73437 ) ;
#115871=CARTESIAN_POINT ( 'NONE',  ( 20.51159235450331764, 2.500000000000001776, 0.000000000000000000 ) ) ;
#115881=ORIENTED_EDGE ( 'NONE', *, *, #44872, .T. ) ;
#115892=CARTESIAN_POINT ( 'NONE',  ( 15.05159235450332034, 3.061616997868380183E-16, -2.500000000000001332 ) ) ;
#115909=EDGE_CURVE ( 'NONE', #71117, #112837, #139165, .T. ) ;
#115928=DIRECTION ( 'NONE',  ( 0.000000000000000000, -1.000000000000000000, 0.000000000000000000 ) ) ;
#115967=CARTESIAN_POINT ( 'NONE',  ( 1.369266385878517678, 0.000000000000000000, -4.607329295533711289 ) ) ;
#115992=VECTOR ( 'NONE', #65048, 1000.000000000000114 ) ;
#116010=EDGE_LOOP ( 'NONE', ( #138175, #39744, #69678, #118470, #14725 ) ) ;
#116032=ORIENTED_EDGE ( 'NONE', *, *, #132967, .T. ) ;
#116046=VERTEX_POINT ( 'NONE', #119746 ) ;
#116048=EDGE_LOOP ( 'NONE', ( #93019, #106750, #39309, #57051, #102179 ) ) ;
#116051=AXIS2_PLACEMENT_3D ( 'NONE', #45374, #66389, #33773 ) ;
#116067=DIRECTION ( 'NONE',  ( -1.000000000000000000, -1.224606353822377258E-16, -0.000000000000000000 ) ) ;
#116123=EDGE_CURVE ( 'NONE', #106215, #79257, #62796, .T. ) ;
#116129=ORIENTED_EDGE ( 'NONE', *, *, #70450, .F. ) ;
#116141=DIRECTION ( 'NONE',  ( 0.000000000000000000, -1.000000000000000000, 0.000000000000000000 ) ) ;
#116158=CIRCLE ( 'NONE', #120804, 2.500000000000000888 ) ;
#116184=EDGE_CURVE ( 'NONE', #79885, #114073, #135663, .T. ) ;
#116198=EDGE_LOOP ( 'NONE', ( #11575, #59793, #96397, #125336, #25525 ) ) ;
#116219=VECTOR ( 'NONE', #110702, 1000.000000000000114 ) ;
#116221=CARTESIAN_POINT ( 'NONE',  ( 23.32000000000000028, 9.521314400968980422E-16, 0.000000000000000000 ) ) ;
#116235=ORIENTED_EDGE ( 'NONE', *, *, #17418, .T. ) ;
#116271=ORIENTED_EDGE ( 'NONE', *, *, #23773, .F. ) ;
#116298=DIRECTION ( 'NONE',  ( 0.000000000000000000, -1.000000000000000000, 0.000000000000000000 ) ) ;
#116306=CARTESIAN_POINT ( 'NONE',  ( 20.51159235450331764, 9.902892378096218942E-16, 0.000000000000000000 ) ) ;
#116343=ORIENTED_EDGE ( 'NONE', *, *, #77073, .F. ) ;
#116353=CIRCLE ( 'NONE', #76966, 2.500000000000000888 ) ;
#116356=ORIENTED_EDGE ( 'NONE', *, *, #122510, .T. ) ;
#116360=DIRECTION ( 'NONE',  ( 0.000000000000000000, -1.000000000000000000, 0.000000000000000000 ) ) ;
#116365=CIRCLE ( 'NONE', #53888, 2.500000000000000888 ) ;
#116417=CARTESIAN_POINT ( 'NONE',  ( 15.52000000000000135, 9.521314400968980422E-16, 0.000000000000000000 ) ) ;
#116520=ORIENTED_EDGE ( 'NONE', *, *, #111540, .F. ) ;
#116575=STYLED_ITEM ( 'NONE', ( #110972 ), #42351 ) ;
#116586=LINE ( 'NONE', #32267, #128434 ) ;
#116596=ORIENTED_EDGE ( 'NONE', *, *, #118571, .T. ) ;
#116610=ORIENTED_EDGE ( 'NONE', *, *, #55680, .F. ) ;
#116625=CARTESIAN_POINT ( 'NONE',  ( -25.39999999999996305, 0.000000000000000000, 0.000000000000000000 ) ) ;
#116627=EDGE_CURVE ( 'NONE', #22742, #50481, #108878, .T. ) ;
#116692=AXIS2_PLACEMENT_3D ( 'NONE', #37620, #70965, #25285 ) ;
#116694=CIRCLE ( 'NONE', #77319, 2.500000000000000888 ) ;
#116702=DIRECTION ( 'NONE',  ( -1.000000000000000000, -1.224606353822377258E-16, -0.000000000000000000 ) ) ;
#116725=CIRCLE ( 'NONE', #40391, 2.055000000000001048 ) ;
#116727=CARTESIAN_POINT ( 'NONE',  ( 6.628407645496676714, 3.061616997868380183E-16, -2.500000000000001332 ) ) ;
#116801=DIRECTION ( 'NONE',  ( 0.000000000000000000, 0.000000000000000000, 1.000000000000000000 ) ) ;
#116879=ADVANCED_FACE ( 'NONE', ( #28823 ), #32550, .T. ) ;
#116903=DIRECTION ( 'NONE',  ( 0.000000000000000000, -1.000000000000000000, 0.000000000000000000 ) ) ;
#116982=AXIS2_PLACEMENT_3D ( 'NONE', #90257, #3242, #125034 ) ;
#116991=CARTESIAN_POINT ( 'NONE',  ( 8.031592354503320763, 9.902892378096218942E-16, 0.000000000000000000 ) ) ;
#117002=VERTEX_POINT ( 'NONE', #31676 ) ;
#117018=AXIS2_PLACEMENT_3D ( 'NONE', #38384, #93476, #138408 ) ;
#117031=CARTESIAN_POINT ( 'NONE',  ( 20.19999999999999929, -2.055000000000000160, 2.789133085058098087E-16 ) ) ;
#117047=ADVANCED_FACE ( 'NONE', ( #86778 ), #7142, .T. ) ;
#117061=CARTESIAN_POINT ( 'NONE',  ( 26.43999999999999773, -2.055000000000000160, 2.789133085058098087E-16 ) ) ;
#117087=ORIENTED_EDGE ( 'NONE', *, *, #120529, .F. ) ;
#117102=EDGE_CURVE ( 'NONE', #115214, #118985, #53438, .T. ) ;
#117147=B_SPLINE_CURVE_WITH_KNOTS ( 'NONE', 3,
 ( #19159, #31474, #97405, #75001, #62680, #106866, #63420, #107587, #20565, #95286 ),
 .UNSPECIFIED., .F., .F.,
 ( 4, 2, 2, 2, 4 ),
 ( 0.005493704601871781008, 0.006008885122700058715, 0.006524065643528337288, 0.007039246164356615862, 0.007554426685184895303 ),
 .UNSPECIFIED. ) ;
#117152=ORIENTED_EDGE ( 'NONE', *, *, #35026, .T. ) ;
#117175=AXIS2_PLACEMENT_3D ( 'NONE', #47038, #135433, #101345 ) ;
#117192=FACE_OUTER_BOUND ( 'NONE', #78772, .T. ) ;
#117193=CARTESIAN_POINT ( 'NONE',  ( -25.39999999999996305, 0.000000000000000000, 0.000000000000000000 ) ) ;
#117245=DIRECTION ( 'NONE',  ( 0.000000000000000000, -1.000000000000000000, 0.000000000000000000 ) ) ;
#117262=AXIS2_PLACEMENT_3D ( 'NONE', #3948, #15548, #27898 ) ;
#117302=AXIS2_PLACEMENT_3D ( 'NONE', #87235, #131459, #54618 ) ;
#117339=VERTEX_POINT ( 'NONE', #4688 ) ;
#117360=CIRCLE ( 'NONE', #27043, 2.500000000000000888 ) ;
#117411=DIRECTION ( 'NONE',  ( -1.000000000000000000, -0.000000000000000000, -0.000000000000000000 ) ) ;
#117425=DIRECTION ( 'NONE',  ( 0.000000000000000000, -9.130123557772670799E-17, 1.000000000000000000 ) ) ;
#117461=DIRECTION ( 'NONE',  ( -0.5735764363510503783, -0.8191520442889886899, 0.000000000000000000 ) ) ;
#117466=VERTEX_POINT ( 'NONE', #119899 ) ;
#117478=CARTESIAN_POINT ( 'NONE',  ( 14.74000000000000021, 9.521314400968980422E-16, 0.000000000000000000 ) ) ;
#117506=AXIS2_PLACEMENT_3D ( 'NONE', #41275, #31840, #132620 ) ;
#117582=AXIS2_PLACEMENT_3D ( 'NONE', #128695, #54026, #51870 ) ;
#117597=DIRECTION ( 'NONE',  ( 0.000000000000000000, -1.000000000000000000, 0.000000000000000000 ) ) ;
#117599=DIRECTION ( 'NONE',  ( -0.5735764363510507113, 0.8191520442889885789, 1.003171929053520926E-16 ) ) ;
#117645=ORIENTED_EDGE ( 'NONE', *, *, #120706, .F. ) ;
#117655=FACE_OUTER_BOUND ( 'NONE', #113988, .T. ) ;
#117669=ORIENTED_EDGE ( 'NONE', *, *, #57102, .F. ) ;
#117691=CIRCLE ( 'NONE', #41343, 2.500000000000000888 ) ;
#117716=LINE ( 'NONE', #16258, #44410 ) ;
#117742=AXIS2_PLACEMENT_3D ( 'NONE', #14048, #68482, #36534 ) ;
#117805=ORIENTED_EDGE ( 'NONE', *, *, #39503, .T. ) ;
#117807=DIRECTION ( 'NONE',  ( -1.000000000000000000, -0.000000000000000000, -0.000000000000000000 ) ) ;
#117846=CARTESIAN_POINT ( 'NONE',  ( 19.73159235450332005, 2.500000000000001332, 0.000000000000000000 ) ) ;
#117908=ADVANCED_FACE ( 'NONE', ( #94429 ), #125375, .T. ) ;
#117915=CARTESIAN_POINT ( 'NONE',  ( 1.199999999999999956, 0.5999999999999987566, 4.749999999999999112 ) ) ;
#117936=DIRECTION ( 'NONE',  ( -1.000000000000000000, -1.224606353822377258E-16, -0.000000000000000000 ) ) ;
#117956=DIRECTION ( 'NONE',  ( -1.000000000000000000, -0.000000000000000000, -0.000000000000000000 ) ) ;
#118018=FACE_OUTER_BOUND ( 'NONE', #16492, .T. ) ;
#118021=ORIENTED_EDGE ( 'NONE', *, *, #60643, .T. ) ;
#118031=VERTEX_POINT ( 'NONE', #36846 ) ;
#118053=CARTESIAN_POINT ( 'NONE',  ( -25.39999999999996305, 0.000000000000000000, 2.500000000000000000 ) ) ;
#118058=VERTEX_POINT ( 'NONE', #91942 ) ;
#118120=DIRECTION ( 'NONE',  ( -1.000000000000000000, -1.224606353822377258E-16, -0.000000000000000000 ) ) ;
#118121=ORIENTED_EDGE ( 'NONE', *, *, #67503, .T. ) ;
#118163=VERTEX_POINT ( 'NONE', #115087 ) ;
#118188=DIRECTION ( 'NONE',  ( -0.5735764363510507113, 0.8191520442889885789, 1.003171929053520926E-16 ) ) ;
#118211=DIRECTION ( 'NONE',  ( 1.000000000000000000, 1.224606353822377258E-16, 0.000000000000000000 ) ) ;
#118222=DIRECTION ( 'NONE',  ( 0.000000000000000000, -1.000000000000000000, 0.000000000000000000 ) ) ;
#118248=AXIS2_PLACEMENT_3D ( 'NONE', #66878, #32101, #132146 ) ;
#118259=DIRECTION ( 'NONE',  ( -1.000000000000000000, -0.000000000000000000, -0.000000000000000000 ) ) ;
#118280=DIRECTION ( 'NONE',  ( 0.000000000000000000, -1.000000000000000000, 0.000000000000000000 ) ) ;
#118292=AXIS2_PLACEMENT_3D ( 'NONE', #73331, #105906, #51578 ) ;
#118293=CARTESIAN_POINT ( 'NONE',  ( 19.73159235450332005, -3.851859888774471706E-31, 2.500000000000001332 ) ) ;
#118317=DIRECTION ( 'NONE',  ( -1.000000000000000000, -1.224606353822377258E-16, -0.000000000000000000 ) ) ;
#118322=ORIENTED_EDGE ( 'NONE', *, *, #22985, .T. ) ;
#118349=CARTESIAN_POINT ( 'NONE',  ( 25.34840764549667469, -2.499999999999996003, 0.000000000000000000 ) ) ;
#118350=CYLINDRICAL_SURFACE ( 'NONE', #39611, 2.500000000000000000 ) ;
#118372=VECTOR ( 'NONE', #137894, 1000.000000000000000 ) ;
#118374=CIRCLE ( 'NONE', #55915, 2.500000000000000888 ) ;
#118404=ORIENTED_EDGE ( 'NONE', *, *, #103860, .F. ) ;
#118411=VECTOR ( 'NONE', #10645, 1000.000000000000000 ) ;
#118436=CONICAL_SURFACE ( 'NONE', #37333, 2.500000000000000888, 0.9599310885968822538 ) ;
#118461=CIRCLE ( 'NONE', #56003, 2.500000000000000888 ) ;
#118468=DIRECTION ( 'NONE',  ( 0.000000000000000000, -1.000000000000000000, 0.000000000000000000 ) ) ;
#118470=ORIENTED_EDGE ( 'NONE', *, *, #15403, .F. ) ;
#118482=EDGE_CURVE ( 'NONE', #60854, #3234, #118628, .T. ) ;
#118549=EDGE_CURVE ( 'NONE', #82762, #92828, #58466, .T. ) ;
#118571=EDGE_CURVE ( 'NONE', #141686, #77389, #83050, .T. ) ;
#118628=CIRCLE ( 'NONE', #76965, 2.500000000000000888 ) ;
#118629=EDGE_CURVE ( 'NONE', #31572, #95905, #140976, .T. ) ;
#118644=CARTESIAN_POINT ( 'NONE',  ( 22.85159235450332105, -3.851859888774471706E-31, 2.500000000000001332 ) ) ;
#118651=ADVANCED_FACE ( 'NONE', ( #106927 ), #51145, .T. ) ;
#118652=CONICAL_SURFACE ( 'NONE', #137201, 2.055000000000001048, 0.9599310885968758145 ) ;
#118660=LINE ( 'NONE', #41820, #110245 ) ;
#118683=EDGE_CURVE ( 'NONE', #76159, #54903, #85172, .T. ) ;
#118716=AXIS2_PLACEMENT_3D ( 'NONE', #48671, #103724, #68319 ) ;
#118748=LINE ( 'NONE', #143360, #71732 ) ;
#118755=DIRECTION ( 'NONE',  ( -1.000000000000000000, -1.224606353822377258E-16, -0.000000000000000000 ) ) ;
#118778=CARTESIAN_POINT ( 'NONE',  ( -25.39999999999996305, 0.000000000000000000, 0.000000000000000000 ) ) ;
#118832=AXIS2_PLACEMENT_3D ( 'NONE', #48837, #40122, #104622 ) ;
#118862=DIRECTION ( 'NONE',  ( -1.000000000000000000, -1.224606353822377258E-16, -0.000000000000000000 ) ) ;
#118867=ORIENTED_EDGE ( 'NONE', *, *, #51367, .F. ) ;
#118873=DIRECTION ( 'NONE',  ( 0.5735764363510451602, 0.8191520442889924647, 0.000000000000000000 ) ) ;
#118910=AXIS2_PLACEMENT_3D ( 'NONE', #56468, #55716, #88345 ) ;
#118985=VERTEX_POINT ( 'NONE', #135834 ) ;
#118993=AXIS2_PLACEMENT_3D ( 'NONE', #7222, #52876, #50768 ) ;
#119001=VERTEX_POINT ( 'NONE', #58330 ) ;
#119056=CIRCLE ( 'NONE', #8207, 2.500000000000000888 ) ;
#119073=ORIENTED_EDGE ( 'NONE', *, *, #45056, .F. ) ;
#119078=EDGE_CURVE ( 'NONE', #109323, #81745, #140136, .T. ) ;
#119116=DIRECTION ( 'NONE',  ( -1.000000000000000000, -1.224606353822377258E-16, -0.000000000000000000 ) ) ;
#119121=CARTESIAN_POINT ( 'NONE',  ( 0.000000000000000000, 0.000000000000000000, 0.000000000000000000 ) ) ;
#119138=CARTESIAN_POINT ( 'NONE',  ( 7.251592354503322291, 9.902892378096218942E-16, 0.000000000000000000 ) ) ;
#119141=LINE ( 'NONE', #75660, #9899 ) ;
#119187=VECTOR ( 'NONE', #7431, 999.9999999999998863 ) ;
#119192=AXIS2_PLACEMENT_3D ( 'NONE', #25221, #91908, #47055 ) ;
#119200=CARTESIAN_POINT ( 'NONE',  ( 26.75159235450331963, 2.500000000000001332, 0.000000000000000000 ) ) ;
#119215=CARTESIAN_POINT ( 'NONE',  ( 13.18000000000000149, 9.521314400968980422E-16, 0.000000000000000000 ) ) ;
#119241=EDGE_LOOP ( 'NONE', ( #31234, #73395, #60110, #75565, #143550 ) ) ;
#119257=DIRECTION ( 'NONE',  ( -1.000000000000000000, -0.000000000000000000, -0.000000000000000000 ) ) ;
#119290=AXIS2_PLACEMENT_3D ( 'NONE', #4703, #84492, #17077 ) ;
#119318=ORIENTED_EDGE ( 'NONE', *, *, #14346, .T. ) ;
#119327=CARTESIAN_POINT ( 'NONE',  ( 12.86840764549667604, 9.139736423841732040E-16, 0.000000000000000000 ) ) ;
#119331=CARTESIAN_POINT ( 'NONE',  ( 5.691592354503320905, 9.902892378096218942E-16, 0.000000000000000000 ) ) ;
#119351=VERTEX_POINT ( 'NONE', #69724 ) ;
#119361=DIRECTION ( 'NONE',  ( 0.000000000000000000, -1.000000000000000000, 0.000000000000000000 ) ) ;
#119364=DIRECTION ( 'NONE',  ( 0.000000000000000000, 1.000000000000000000, 0.000000000000000000 ) ) ;
#119367=EDGE_CURVE ( 'NONE', #82762, #135296, #5103, .T. ) ;
#119411=CARTESIAN_POINT ( 'NONE',  ( 26.90840764549667696, -2.500000000000000888, 0.000000000000000000 ) ) ;
#119420=FACE_OUTER_BOUND ( 'NONE', #52419, .T. ) ;
#119455=VERTEX_POINT ( 'NONE', #15978 ) ;
#119488=LINE ( 'NONE', #120191, #129928 ) ;
#119527=CARTESIAN_POINT ( 'NONE',  ( 23.63159235450331863, -2.500000000000000444, 3.061616997868384620E-16 ) ) ;
#119567=ORIENTED_EDGE ( 'NONE', *, *, #136655, .F. ) ;
#119568=AXIS2_PLACEMENT_3D ( 'NONE', #119331, #7718, #20741 ) ;
#119574=ORIENTED_EDGE ( 'NONE', *, *, #48314, .T. ) ;
#119613=CARTESIAN_POINT ( 'NONE',  ( 25.19159235450331735, 2.500000000000001332, 0.000000000000000000 ) ) ;
#119614=DIRECTION ( 'NONE',  ( -1.000000000000000000, -1.224606353822377258E-16, -0.000000000000000000 ) ) ;
#119662=CARTESIAN_POINT ( 'NONE',  ( 25.65999999999999659, 9.521314400968980422E-16, 0.000000000000000000 ) ) ;
#119746=CARTESIAN_POINT ( 'NONE',  ( 7.720000000000001528, -2.055000000000000160, 2.789133085058098087E-16 ) ) ;
#119749=FACE_OUTER_BOUND ( 'NONE', #135480, .T. ) ;
#119763=DIRECTION ( 'NONE',  ( -1.000000000000000000, -0.000000000000000000, -0.000000000000000000 ) ) ;
#119844=CARTESIAN_POINT ( 'NONE',  ( 24.09999999999999787, -2.055000000000000160, 2.789133085058098087E-16 ) ) ;
#119859=CARTESIAN_POINT ( 'NONE',  ( 11.93159235450332112, 2.500000000000001776, 0.000000000000000000 ) ) ;
#119899=CARTESIAN_POINT ( 'NONE',  ( 12.86840764549667604, -2.500000000000000888, 0.000000000000000000 ) ) ;
#119916=AXIS2_PLACEMENT_3D ( 'NONE', #119215, #19896, #98884 ) ;
#119947=EDGE_CURVE ( 'NONE', #31644, #117339, #116586, .T. ) ;
#119959=PLANE ( 'NONE',  #127456 ) ;
#119965=CONICAL_SURFACE ( 'NONE', #34321, 2.055000000000001048, 0.9599310885968758145 ) ;
#119975=ORIENTED_EDGE ( 'NONE', *, *, #6709, .T. ) ;
#119999=DIRECTION ( 'NONE',  ( 0.000000000000000000, 1.000000000000000000, 0.000000000000000000 ) ) ;
#120004=EDGE_CURVE ( 'NONE', #36659, #143251, #65650, .T. ) ;
#120048=DIRECTION ( 'NONE',  ( 0.5735764363510453823, -0.8191520442889923537, 1.003171929053525486E-16 ) ) ;
#120158=DIRECTION ( 'NONE',  ( 0.000000000000000000, -1.000000000000000000, 0.000000000000000000 ) ) ;
#120178=DIRECTION ( 'NONE',  ( -1.000000000000000000, -1.224606353822377258E-16, -0.000000000000000000 ) ) ;
#120191=CARTESIAN_POINT ( 'NONE',  ( 10.06000000000000050, -2.055000000000000160, 0.000000000000000000 ) ) ;
#120264=DIRECTION ( 'NONE',  ( 0.000000000000000000, -1.000000000000000000, 0.000000000000000000 ) ) ;
#120266=ADVANCED_FACE ( 'NONE', ( #74036 ), #52041, .T. ) ;
#120300=AXIS2_PLACEMENT_3D ( 'NONE', #133922, #133232, #23729 ) ;
#120309=CARTESIAN_POINT ( 'NONE',  ( 18.95159235450331892, -2.500000000000000444, 3.061616997868384620E-16 ) ) ;
#120313=DIRECTION ( 'NONE',  ( 0.000000000000000000, -1.000000000000000000, 0.000000000000000000 ) ) ;
#120349=EDGE_LOOP ( 'NONE', ( #88389, #52664, #140106, #48231, #1045 ) ) ;
#120354=DIRECTION ( 'NONE',  ( -0.5735764363510503783, -0.8191520442889886899, 0.000000000000000000 ) ) ;
#120358=LINE ( 'NONE', #11604, #88398 ) ;
#120364=CIRCLE ( 'NONE', #48590, 2.500000000000000888 ) ;
#120395=VECTOR ( 'NONE', #98616, 1000.000000000000000 ) ;
#120406=ORIENTED_EDGE ( 'NONE', *, *, #81725, .F. ) ;
#120420=ADVANCED_FACE ( 'NONE', ( #129117 ), #26583, .T. ) ;
#120453=EDGE_LOOP ( 'NONE', ( #7714, #30136, #39486, #43699, #121812, #134312 ) ) ;
#120458=ORIENTED_EDGE ( 'NONE', *, *, #81870, .T. ) ;
#120485=EDGE_CURVE ( 'NONE', #9148, #48488, #93740, .T. ) ;
#120529=EDGE_CURVE ( 'NONE', #43087, #29352, #109972, .T. ) ;
#120545=CARTESIAN_POINT ( 'NONE',  ( 12.08840764549667668, 3.061616997868380183E-16, -2.500000000000001332 ) ) ;
#120577=EDGE_CURVE ( 'NONE', #54899, #101759, #52272, .T. ) ;
#120646=CARTESIAN_POINT ( 'NONE',  ( 13.18000000000000149, 2.055000000000001492, 2.516649172247811554E-16 ) ) ;
#120706=EDGE_CURVE ( 'NONE', #4422, #96831, #102230, .T. ) ;
#120717=EDGE_CURVE ( 'NONE', #24671, #103081, #86920, .T. ) ;
#120804=AXIS2_PLACEMENT_3D ( 'NONE', #76590, #65735, #121482 ) ;
#120838=CARTESIAN_POINT ( 'NONE',  ( 6.940000000000001279, 2.055000000000001492, 0.000000000000000000 ) ) ;
#120893=AXIS2_PLACEMENT_3D ( 'NONE', #139820, #60850, #105005 ) ;
#120965=ORIENTED_EDGE ( 'NONE', *, *, #105638, .F. ) ;
#120975=EDGE_LOOP ( 'NONE', ( #74322, #132373, #72499, #130815, #55885 ) ) ;
#120977=ADVANCED_FACE ( 'NONE', ( #30349 ), #74592, .T. ) ;
#121005=EDGE_LOOP ( 'NONE', ( #13418, #30788, #25371, #111133, #74683, #3593 ) ) ;
#121024=VERTEX_POINT ( 'NONE', #78881 ) ;
#121045=CIRCLE ( 'NONE', #77111, 2.500000000000000888 ) ;
#121095=FACE_OUTER_BOUND ( 'NONE', #91739, .T. ) ;
#121108=CARTESIAN_POINT ( 'NONE',  ( 23.00840764549667483, 3.061616997868380183E-16, -2.500000000000001332 ) ) ;
#121110=CIRCLE ( 'NONE', #98153, 2.500000000000000888 ) ;
#121158=ORIENTED_EDGE ( 'NONE', *, *, #87721, .F. ) ;
#121185=CONICAL_SURFACE ( 'NONE', #58761, 2.500000000000000888, 0.9599310885968822538 ) ;
#121207=VERTEX_POINT ( 'NONE', #125941 ) ;
#121224=AXIS2_PLACEMENT_3D ( 'NONE', #42659, #31758, #110703 ) ;
#121238=EDGE_CURVE ( 'NONE', #27726, #115014, #63851, .T. ) ;
#121240=ORIENTED_EDGE ( 'NONE', *, *, #5595, .T. ) ;
#121284=ORIENTED_EDGE ( 'NONE', *, *, #77140, .T. ) ;
#121297=FACE_OUTER_BOUND ( 'NONE', #107354, .T. ) ;
#121315=ORIENTED_EDGE ( 'NONE', *, *, #94203, .F. ) ;
#121329=ORIENTED_EDGE ( 'NONE', *, *, #108159, .T. ) ;
#121354=EDGE_CURVE ( 'NONE', #123367, #108418, #47730, .T. ) ;
#121358=AXIS2_PLACEMENT_3D ( 'NONE', #47079, #35459, #102119 ) ;
#121365=ORIENTED_EDGE ( 'NONE', *, *, #27330, .T. ) ;
#121372=VERTEX_POINT ( 'NONE', #86722 ) ;
#121379=DIRECTION ( 'NONE',  ( -0.5735764363510507113, 0.8191520442889885789, 1.003171929053520926E-16 ) ) ;
#121392=EDGE_CURVE ( 'NONE', #92828, #109156, #135236, .T. ) ;
#121409=CIRCLE ( 'NONE', #58980, 2.055000000000001048 ) ;
#121421=EDGE_CURVE ( 'NONE', #99607, #80827, #122905, .T. ) ;
#121482=DIRECTION ( 'NONE',  ( 0.000000000000000000, -1.000000000000000000, 0.000000000000000000 ) ) ;
#121491=DIRECTION ( 'NONE',  ( 0.000000000000000000, -1.000000000000000000, 0.000000000000000000 ) ) ;
#121520=ORIENTED_EDGE ( 'NONE', *, *, #13862, .T. ) ;
#121521=EDGE_CURVE ( 'NONE', #138330, #110525, #75433, .T. ) ;
#121546=ORIENTED_EDGE ( 'NONE', *, *, #105046, .T. ) ;
#121556=EDGE_CURVE ( 'NONE', #91883, #56418, #135653, .T. ) ;
#121659=FACE_OUTER_BOUND ( 'NONE', #87251, .T. ) ;
#121674=FACE_OUTER_BOUND ( 'NONE', #10330, .T. ) ;
#121683=APPLICATION_CONTEXT ( 'automotive_design' ) ;
#121758=AXIS2_PLACEMENT_3D ( 'NONE', #82433, #32336, #95431 ) ;
#121812=ORIENTED_EDGE ( 'NONE', *, *, #7277, .F. ) ;
#121817=EDGE_LOOP ( 'NONE', ( #84743, #133994, #121284, #92130, #122341 ) ) ;
#121820=ORIENTED_EDGE ( 'NONE', *, *, #137058, .T. ) ;
#121850=FILL_AREA_STYLE ('',( #10940 ) ) ;
#121917=CARTESIAN_POINT ( 'NONE',  ( 25.97159235450331849, 9.902892378096218942E-16, 0.000000000000000000 ) ) ;
#121952=DIRECTION ( 'NONE',  ( 0.000000000000000000, -1.000000000000000000, 0.000000000000000000 ) ) ;
#121959=LINE ( 'NONE', #141607, #61963 ) ;
#122035=AXIS2_PLACEMENT_3D ( 'NONE', #126324, #14712, #16095 ) ;
#122043=CARTESIAN_POINT ( 'NONE',  ( 23.78840764549667597, 3.061616997868385113E-16, -2.500000000000001332 ) ) ;
#122059=EDGE_CURVE ( 'NONE', #104096, #81350, #26989, .T. ) ;
#122099=EDGE_CURVE ( 'NONE', #28445, #97682, #43253, .T. ) ;
#122133=EDGE_LOOP ( 'NONE', ( #33013, #30156, #116596, #86795, #107804, #114836 ) ) ;
#122155=CARTESIAN_POINT ( 'NONE',  ( -25.39999999999996305, 0.000000000000000000, 2.500000000000000000 ) ) ;
#122162=FACE_OUTER_BOUND ( 'NONE', #54964, .T. ) ;
#122163=ORIENTED_EDGE ( 'NONE', *, *, #92064, .T. ) ;
#122172=ORIENTED_EDGE ( 'NONE', *, *, #45056, .T. ) ;
#122180=DIRECTION ( 'NONE',  ( -1.000000000000000000, -0.000000000000000000, -0.000000000000000000 ) ) ;
#122216=B_SPLINE_CURVE_WITH_KNOTS ( 'NONE', 3,
 ( #32366, #7729, #141860, #43255, #9121, #86756, #51983, #18594, #98342, #76610 ),
 .UNSPECIFIED., .F., .F.,
 ( 4, 2, 2, 2, 4 ),
 ( 0.001941010781631071457, 0.002456031491763875727, 0.002971052201896679998, 0.003486072912029485136, 0.004001093622162290274 ),
 .UNSPECIFIED. ) ;
#122260=AXIS2_PLACEMENT_3D ( 'NONE', #59342, #14373, #68783 ) ;
#122272=CARTESIAN_POINT ( 'NONE',  ( 1.199999999999999956, 0.000000000000000000, 0.000000000000000000 ) ) ;
#122280=EDGE_LOOP ( 'NONE', ( #76771, #108005, #92277, #135956, #65833 ) ) ;
#122283=AXIS2_PLACEMENT_3D ( 'NONE', #20312, #99297, #41362 ) ;
#122321=DIRECTION ( 'NONE',  ( 0.000000000000000000, 0.000000000000000000, 1.000000000000000000 ) ) ;
#122333=DIRECTION ( 'NONE',  ( 0.5735764363510453823, -0.8191520442889923537, 1.003171929053525486E-16 ) ) ;
#122341=ORIENTED_EDGE ( 'NONE', *, *, #66799, .F. ) ;
#122345=CARTESIAN_POINT ( 'NONE',  ( 13.64840764549667540, 2.500000000000003553, 3.061616997868386099E-16 ) ) ;
#122426=ORIENTED_EDGE ( 'NONE', *, *, #41483, .F. ) ;
#122456=CARTESIAN_POINT ( 'NONE',  ( 14.42840764549667476, 9.139736423841732040E-16, 0.000000000000000000 ) ) ;
#122465=LINE ( 'NONE', #97883, #30898 ) ;
#122476=DIRECTION ( 'NONE',  ( -1.000000000000000000, -0.000000000000000000, -0.000000000000000000 ) ) ;
#122510=EDGE_CURVE ( 'NONE', #29342, #95787, #89486, .T. ) ;
#122511=EDGE_CURVE ( 'NONE', #31472, #95905, #40959, .T. ) ;
#122520=CARTESIAN_POINT ( 'NONE',  ( 10.52840764549667618, 9.139736423841732040E-16, 0.000000000000000000 ) ) ;
#122545=DIRECTION ( 'NONE',  ( 0.000000000000000000, 1.000000000000000000, 0.000000000000000000 ) ) ;
#122583=AXIS2_PLACEMENT_3D ( 'NONE', #41511, #42262, #96574 ) ;
#122590=CIRCLE ( 'NONE', #50793, 2.500000000000000888 ) ;
#122626=AXIS2_PLACEMENT_3D ( 'NONE', #131867, #53597, #87637 ) ;
#122706=CARTESIAN_POINT ( 'NONE',  ( 11.93159235450332112, 9.902892378096218942E-16, 0.000000000000000000 ) ) ;
#122746=DIRECTION ( 'NONE',  ( -1.000000000000000000, -0.000000000000000000, -0.000000000000000000 ) ) ;
#122759=DIRECTION ( 'NONE',  ( -1.000000000000000000, -1.224606353822377258E-16, -0.000000000000000000 ) ) ;
#122771=VECTOR ( 'NONE', #80579, 1000.000000000000000 ) ;
#122776=DIRECTION ( 'NONE',  ( 1.000000000000000000, 1.224606353822377258E-16, 0.000000000000000000 ) ) ;
#122783=CIRCLE ( 'NONE', #4649, 2.055000000000001048 ) ;
#122784=CIRCLE ( 'NONE', #58055, 2.500000000000000888 ) ;
#122803=DIRECTION ( 'NONE',  ( 1.000000000000000000, 1.224606353822377258E-16, 0.000000000000000000 ) ) ;
#122849=DIRECTION ( 'NONE',  ( -1.000000000000000000, -1.224606353822377258E-16, -0.000000000000000000 ) ) ;
#122859=CARTESIAN_POINT ( 'NONE',  ( 22.22840764549667725, 9.139736423841732040E-16, 0.000000000000000000 ) ) ;
#122870=DIRECTION ( 'NONE',  ( 0.000000000000000000, -1.000000000000000000, 0.000000000000000000 ) ) ;
#122888=DIRECTION ( 'NONE',  ( -1.000000000000000000, -1.224606353822377258E-16, -0.000000000000000000 ) ) ;
#122897=FACE_OUTER_BOUND ( 'NONE', #26677, .T. ) ;
#122898=EDGE_CURVE ( 'NONE', #61706, #20496, #117147, .T. ) ;
#122904=DIRECTION ( 'NONE',  ( 0.000000000000000000, -1.000000000000000000, 0.000000000000000000 ) ) ;
#122905=LINE ( 'NONE', #12692, #49986 ) ;
#122911=VERTEX_POINT ( 'NONE', #142386 ) ;
#123057=EDGE_CURVE ( 'NONE', #8957, #13435, #94237, .T. ) ;
#123095=ORIENTED_EDGE ( 'NONE', *, *, #3903, .F. ) ;
#123101=CARTESIAN_POINT ( 'NONE',  ( 21.29159235450332233, 2.500000000000001332, 0.000000000000000000 ) ) ;
#123121=TOROIDAL_SURFACE ( 'NONE', #9657, 3.113037248396092416, 1.500000000000000000 ) ;
#123126=CARTESIAN_POINT ( 'NONE',  ( -25.39999999999996305, 3.061616997868383141E-16, -2.500000000000000000 ) ) ;
#123174=DIRECTION ( 'NONE',  ( 0.000000000000000000, -1.000000000000000000, 0.000000000000000000 ) ) ;
#123177=ORIENTED_EDGE ( 'NONE', *, *, #37492, .T. ) ;
#123191=CIRCLE ( 'NONE', #74552, 2.055000000000001048 ) ;
#123199=CARTESIAN_POINT ( 'NONE',  ( -25.39999999999996305, 0.000000000000000000, 0.000000000000000000 ) ) ;
#123231=EDGE_CURVE ( 'NONE', #64995, #51758, #124465, .T. ) ;
#123246=CARTESIAN_POINT ( 'NONE',  ( 23.78840764549667597, 0.000000000000000000, 2.500000000000001332 ) ) ;
#123250=VECTOR ( 'NONE', #127222, 1000.000000000000114 ) ;
#123261=CIRCLE ( 'NONE', #56111, 2.500000000000000888 ) ;
#123268=DIRECTION ( 'NONE',  ( -1.000000000000000000, -1.224606353822377258E-16, -0.000000000000000000 ) ) ;
#123282=ORIENTED_EDGE ( 'NONE', *, *, #38117, .F. ) ;
#123293=ORIENTED_EDGE ( 'NONE', *, *, #109950, .F. ) ;
#123335=ORIENTED_EDGE ( 'NONE', *, *, #20847, .T. ) ;
#123367=VERTEX_POINT ( 'NONE', #115967 ) ;
#123374=VERTEX_POINT ( 'NONE', #50038 ) ;
#123380=CONICAL_SURFACE ( 'NONE', #63270, 2.055000000000001048, 0.9599310885968758145 ) ;
#123381=ORIENTED_EDGE ( 'NONE', *, *, #37843, .F. ) ;
#123395=EDGE_CURVE ( 'NONE', #31572, #87975, #110570, .T. ) ;
#123398=ORIENTED_EDGE ( 'NONE', *, *, #31558, .T. ) ;
#123440=ADVANCED_FACE ( 'NONE', ( #64468 ), #61986, .T. ) ;
#123444=CARTESIAN_POINT ( 'NONE',  ( -25.39999999999996305, 0.000000000000000000, 2.500000000000000000 ) ) ;
#123519=ORIENTED_EDGE ( 'NONE', *, *, #54539, .F. ) ;
#123549=EDGE_CURVE ( 'NONE', #3030, #93111, #115208, .T. ) ;
#123563=LINE ( 'NONE', #112649, #33457 ) ;
#123569=DIRECTION ( 'NONE',  ( -1.000000000000000000, -0.000000000000000000, -0.000000000000000000 ) ) ;
#123573=DIRECTION ( 'NONE',  ( -1.000000000000000000, -1.224606353822377258E-16, -0.000000000000000000 ) ) ;
#123578=DIRECTION ( 'NONE',  ( -0.5735764363510507113, 0.8191520442889885789, 1.003171929053520926E-16 ) ) ;
#123607=AXIS2_PLACEMENT_3D ( 'NONE', #34387, #123573, #58336 ) ;
#123629=EDGE_CURVE ( 'NONE', #71528, #24671, #57336, .T. ) ;
#123636=CARTESIAN_POINT ( 'NONE',  ( 25.34840764549667469, 9.139736423841732040E-16, 0.000000000000000000 ) ) ;
#123659=DIRECTION ( 'NONE',  ( -1.000000000000000000, -0.000000000000000000, -0.000000000000000000 ) ) ;
#123738=AXIS2_PLACEMENT_3D ( 'NONE', #141523, #118317, #6666 ) ;
#123756=AXIS2_PLACEMENT_3D ( 'NONE', #122272, #90378, #78096 ) ;
#123759=DIRECTION ( 'NONE',  ( 0.000000000000000000, -1.000000000000000000, 0.000000000000000000 ) ) ;
#123780=VECTOR ( 'NONE', #34216, 1000.000000000000000 ) ;
#123809=DIRECTION ( 'NONE',  ( -1.000000000000000000, -0.000000000000000000, -0.000000000000000000 ) ) ;
#123843=DIRECTION ( 'NONE',  ( -1.000000000000000000, -1.224606353822377258E-16, -0.000000000000000000 ) ) ;
#123852=LINE ( 'NONE', #48403, #31750 ) ;
#123859=CARTESIAN_POINT ( 'NONE',  ( 10.83999999999999986, 9.521314400968980422E-16, 0.000000000000000000 ) ) ;
#123903=ADVANCED_FACE ( 'NONE', ( #107080 ), #108276, .T. ) ;
#123929=EDGE_CURVE ( 'NONE', #142002, #104583, #82882, .T. ) ;
#123956=ORIENTED_EDGE ( 'NONE', *, *, #35984, .F. ) ;
#123978=LINE ( 'NONE', #26785, #35303 ) ;
#123985=ADVANCED_FACE ( 'NONE', ( #103849 ), #58299, .T. ) ;
#124023=DIRECTION ( 'NONE',  ( 0.000000000000000000, -1.000000000000000000, 0.000000000000000000 ) ) ;
#124027=ORIENTED_EDGE ( 'NONE', *, *, #134623, .T. ) ;
#124050=ORIENTED_EDGE ( 'NONE', *, *, #142895, .F. ) ;
#124088=ORIENTED_EDGE ( 'NONE', *, *, #121556, .T. ) ;
#124091=ORIENTED_EDGE ( 'NONE', *, *, #46016, .F. ) ;
#124131=AXIS2_PLACEMENT_3D ( 'NONE', #46883, #70049, #12035 ) ;
#124134=ORIENTED_EDGE ( 'NONE', *, *, #43374, .F. ) ;
#124142=CARTESIAN_POINT ( 'NONE',  ( 10.83999999999999986, 9.521314400968980422E-16, 0.000000000000000000 ) ) ;
#124145=CONICAL_SURFACE ( 'NONE', #45429, 2.055000000000001048, 0.9599310885968758145 ) ;
#124175=DIRECTION ( 'NONE',  ( 0.000000000000000000, -1.000000000000000000, 0.000000000000000000 ) ) ;
#124192=ORIENTED_EDGE ( 'NONE', *, *, #98673, .F. ) ;
#124194=ORIENTED_EDGE ( 'NONE', *, *, #115277, .F. ) ;
#124215=AXIS2_PLACEMENT_3D ( 'NONE', #35885, #90967, #133745 ) ;
#124221=ORIENTED_EDGE ( 'NONE', *, *, #85086, .T. ) ;
#124226=VECTOR ( 'NONE', #48243, 1000.000000000000000 ) ;
#124257=VERTEX_POINT ( 'NONE', #42219 ) ;
#124282=DIRECTION ( 'NONE',  ( 0.5735764363510453823, -0.8191520442889923537, 1.003171929053525486E-16 ) ) ;
#124295=AXIS2_PLACEMENT_3D ( 'NONE', #130670, #141530, #77706 ) ;
#124330=EDGE_CURVE ( 'NONE', #101812, #140709, #65408, .T. ) ;
#124332=ADVANCED_FACE ( 'NONE', ( #100156 ), #131617, .T. ) ;
#124333=EDGE_LOOP ( 'NONE', ( #11346, #25870, #92778, #63450, #77049, #1306 ) ) ;
#124357=CIRCLE ( 'NONE', #17840, 2.500000000000000888 ) ;
#124404=ORIENTED_EDGE ( 'NONE', *, *, #139180, .F. ) ;
#124411=ORIENTED_EDGE ( 'NONE', *, *, #105342, .T. ) ;
#124428=CIRCLE ( 'NONE', #122035, 2.500000000000000888 ) ;
#124434=DIRECTION ( 'NONE',  ( 0.000000000000000000, -1.000000000000000000, 0.000000000000000000 ) ) ;
#124464=ORIENTED_EDGE ( 'NONE', *, *, #89231, .F. ) ;
#124465=CIRCLE ( 'NONE', #52730, 2.500000000000000888 ) ;
#124484=CARTESIAN_POINT ( 'NONE',  ( 23.78840764549667597, 2.499999999999998224, 3.061616997868380183E-16 ) ) ;
#124504=ORIENTED_EDGE ( 'NONE', *, *, #100842, .F. ) ;
#124568=VERTEX_POINT ( 'NONE', #116727 ) ;
#124585=ORIENTED_EDGE ( 'NONE', *, *, #82055, .F. ) ;
#124621=VERTEX_POINT ( 'NONE', #43454 ) ;
#124688=DIRECTION ( 'NONE',  ( 0.000000000000000000, -1.000000000000000000, 0.000000000000000000 ) ) ;
#124705=EDGE_CURVE ( 'NONE', #139177, #67571, #32052, .T. ) ;
#124716=LINE ( 'NONE', #90685, #37552 ) ;
#124727=CARTESIAN_POINT ( 'NONE',  ( -25.39999999999996305, 3.061616997868383141E-16, -2.500000000000000000 ) ) ;
#124729=EDGE_CURVE ( 'NONE', #98397, #119455, #20540, .T. ) ;
#124742=FACE_OUTER_BOUND ( 'NONE', #14966, .T. ) ;
#124749=EDGE_LOOP ( 'NONE', ( #11006, #67735, #5820, #101271, #27386, #129394 ) ) ;
#124751=ORIENTED_EDGE ( 'NONE', *, *, #31045, .F. ) ;
#124759=ORIENTED_EDGE ( 'NONE', *, *, #38108, .F. ) ;
#124762=ORIENTED_EDGE ( 'NONE', *, *, #63591, .F. ) ;
#124799=EDGE_CURVE ( 'NONE', #27842, #17414, #87423, .T. ) ;
#124804=ORIENTED_EDGE ( 'NONE', *, *, #39157, .T. ) ;
#124821=VERTEX_POINT ( 'NONE', #57938 ) ;
#124831=DIRECTION ( 'NONE',  ( -1.000000000000000000, -1.224606353822377258E-16, -0.000000000000000000 ) ) ;
#124832=CARTESIAN_POINT ( 'NONE',  ( 7.408407645496676963, 3.061616997868381169E-16, -2.500000000000001332 ) ) ;
#124869=CIRCLE ( 'NONE', #94725, 2.500000000000000888 ) ;
#124875=EDGE_CURVE ( 'NONE', #135574, #52853, #111559, .T. ) ;
#124904=DIRECTION ( 'NONE',  ( 0.000000000000000000, 0.000000000000000000, 1.000000000000000000 ) ) ;
#124915=DIRECTION ( 'NONE',  ( -1.000000000000000000, -0.000000000000000000, -0.000000000000000000 ) ) ;
#124989=VECTOR ( 'NONE', #136080, 1000.000000000000000 ) ;
#125030=CARTESIAN_POINT ( 'NONE',  ( 12.71159235450332048, -2.500000000000000000, 3.061616997868384127E-16 ) ) ;
#125034=DIRECTION ( 'NONE',  ( 0.000000000000000000, 0.000000000000000000, 1.000000000000000000 ) ) ;
#125050=VERTEX_POINT ( 'NONE', #21535 ) ;
#125060=AXIS2_PLACEMENT_3D ( 'NONE', #55271, #34229, #850 ) ;
#125098=ORIENTED_EDGE ( 'NONE', *, *, #85241, .T. ) ;
#125104=AXIS2_PLACEMENT_3D ( 'NONE', #131512, #88735, #964 ) ;
#125115=DIRECTION ( 'NONE',  ( -1.000000000000000000, -1.224606353822377258E-16, -0.000000000000000000 ) ) ;
#125117=CARTESIAN_POINT ( 'NONE',  ( -25.39999999999996305, 0.000000000000000000, 0.000000000000000000 ) ) ;
#125134=EDGE_CURVE ( 'NONE', #70009, #104583, #100532, .T. ) ;
#125146=DIRECTION ( 'NONE',  ( -1.000000000000000000, -1.224606353822377258E-16, -0.000000000000000000 ) ) ;
#125157=CYLINDRICAL_SURFACE ( 'NONE', #8940, 2.500000000000000000 ) ;
#125173=ORIENTED_EDGE ( 'NONE', *, *, #92777, .T. ) ;
#125226=ORIENTED_EDGE ( 'NONE', *, *, #18379, .F. ) ;
#125252=( NAMED_UNIT ( * ) PLANE_ANGLE_UNIT ( ) SI_UNIT ( $, .RADIAN. ) );
#125260=CIRCLE ( 'NONE', #213, 2.500000000000000888 ) ;
#125299=FACE_OUTER_BOUND ( 'NONE', #76316, .T. ) ;
#125302=CARTESIAN_POINT ( 'NONE',  ( -25.39999999999996305, 0.000000000000000000, 2.500000000000000000 ) ) ;
#125336=ORIENTED_EDGE ( 'NONE', *, *, #12283, .F. ) ;
#125370=DIRECTION ( 'NONE',  ( -1.000000000000000000, -1.224606353822377258E-16, -0.000000000000000000 ) ) ;
#125375=CONICAL_SURFACE ( 'NONE', #81420, 2.055000000000001048, 0.9599310885968758145 ) ;
#125421=CARTESIAN_POINT ( 'NONE',  ( 5.691592354503320905, 9.902892378096218942E-16, 0.000000000000000000 ) ) ;
#125443=ORIENTED_EDGE ( 'NONE', *, *, #58747, .T. ) ;
#125446=AXIS2_PLACEMENT_3D ( 'NONE', #140141, #53088, #130701 ) ;
#125451=ORIENTED_EDGE ( 'NONE', *, *, #137906, .T. ) ;
#125468=DIRECTION ( 'NONE',  ( 0.000000000000000000, 0.000000000000000000, 1.000000000000000000 ) ) ;
#125469=CONICAL_SURFACE ( 'NONE', #67657, 2.500000000000000888, 0.9599310885968822538 ) ;
#125471=EDGE_CURVE ( 'NONE', #71989, #56823, #31945, .T. ) ;
#125488=DIRECTION ( 'NONE',  ( 0.000000000000000000, -1.000000000000000000, 0.000000000000000000 ) ) ;
#125540=ORIENTED_EDGE ( 'NONE', *, *, #138411, .F. ) ;
#125542=CARTESIAN_POINT ( 'NONE',  ( 4.288407645496676857, 9.139736423841732040E-16, 0.000000000000000000 ) ) ;
#125562=DIRECTION ( 'NONE',  ( -1.000000000000000000, -0.000000000000000000, -0.000000000000000000 ) ) ;
#125563=ORIENTED_EDGE ( 'NONE', *, *, #118683, .F. ) ;
#125565=LINE ( 'NONE', #123444, #113417 ) ;
#125586=ORIENTED_EDGE ( 'NONE', *, *, #118629, .F. ) ;
#125600=EDGE_CURVE ( 'NONE', #106721, #56418, #100362, .T. ) ;
#125608=EDGE_LOOP ( 'NONE', ( #59751, #21156, #28647, #94356, #141007 ) ) ;
#125631=ADVANCED_FACE ( 'NONE', ( #66314 ), #48191, .T. ) ;
#125655=CARTESIAN_POINT ( 'NONE',  ( -25.39999999999996305, 0.000000000000000000, 0.000000000000000000 ) ) ;
#125661=LINE ( 'NONE', #80735, #109850 ) ;
#125700=DIRECTION ( 'NONE',  ( 0.000000000000000000, -1.000000000000000000, 0.000000000000000000 ) ) ;
#125705=CARTESIAN_POINT ( 'NONE',  ( 8.968407645496675684, 9.139736423841732040E-16, 0.000000000000000000 ) ) ;
#125713=AXIS2_PLACEMENT_3D ( 'NONE', #75091, #119257, #98248 ) ;
#125733=CARTESIAN_POINT ( 'NONE',  ( -25.39999999999996305, 0.000000000000000000, 0.000000000000000000 ) ) ;
#125870=ADVANCED_FACE ( 'NONE', ( #101416 ), #119965, .T. ) ;
#125883=DIRECTION ( 'NONE',  ( 0.000000000000000000, -1.000000000000000000, 0.000000000000000000 ) ) ;
#125906=EDGE_LOOP ( 'NONE', ( #18974, #141964, #71801, #50075, #134507 ) ) ;
#125926=CIRCLE ( 'NONE', #19417, 2.500000000000000888 ) ;
#125941=CARTESIAN_POINT ( 'NONE',  ( 18.17159235450331778, -2.500000000000000444, 3.061616997868384620E-16 ) ) ;
#125952=ADVANCED_FACE ( 'NONE', ( #78991 ), #14415, .T. ) ;
#125965=AXIS2_PLACEMENT_3D ( 'NONE', #10822, #32626, #76857 ) ;
#125979=EDGE_CURVE ( 'NONE', #121207, #105943, #4233, .T. ) ;
#126013=AXIS2_PLACEMENT_3D ( 'NONE', #21597, #99863, #64382 ) ;
#126036=AXIS2_PLACEMENT_3D ( 'NONE', #63124, #94979, #142106 ) ;
#126068=CARTESIAN_POINT ( 'NONE',  ( 12.40000000000000213, -2.055000000000000160, 0.000000000000000000 ) ) ;
#126085=CARTESIAN_POINT ( 'NONE',  ( 15.83159235450332147, 2.500000000000001332, 0.000000000000000000 ) ) ;
#126107=DIRECTION ( 'NONE',  ( -1.000000000000000000, -1.224606353822377258E-16, -0.000000000000000000 ) ) ;
#126115=CARTESIAN_POINT ( 'NONE',  ( 9.591592354503321260, 9.902892378096218942E-16, 0.000000000000000000 ) ) ;
#126134=CARTESIAN_POINT ( 'NONE',  ( 14.27159235450332098, -2.500000000000000444, 3.061616997868384620E-16 ) ) ;
#126143=CIRCLE ( 'NONE', #119290, 2.500000000000000888 ) ;
#126153=ORIENTED_EDGE ( 'NONE', *, *, #84953, .T. ) ;
#126156=ADVANCED_FACE ( 'NONE', ( #54219 ), #13592, .T. ) ;
#126179=CARTESIAN_POINT ( 'NONE',  ( -25.39999999999996305, 0.000000000000000000, 0.000000000000000000 ) ) ;
#126198=FACE_OUTER_BOUND ( 'NONE', #132356, .T. ) ;
#126199=ORIENTED_EDGE ( 'NONE', *, *, #113946, .F. ) ;
#126279=ORIENTED_EDGE ( 'NONE', *, *, #2727, .T. ) ;
#126299=EDGE_LOOP ( 'NONE', ( #55388, #1948, #4304, #19817, #130663 ) ) ;
#126310=CARTESIAN_POINT ( 'NONE',  ( 23.78840764549667597, 9.139736423841732040E-16, 0.000000000000000000 ) ) ;
#126324=CARTESIAN_POINT ( 'NONE',  ( 25.19159235450331735, 9.902892378096218942E-16, 0.000000000000000000 ) ) ;
#126383=CARTESIAN_POINT ( 'NONE',  ( 20.66840764549667497, 9.139736423841732040E-16, 0.000000000000000000 ) ) ;
#126424=DIRECTION ( 'NONE',  ( -1.000000000000000000, -1.224606353822377258E-16, -0.000000000000000000 ) ) ;
#126489=ORIENTED_EDGE ( 'NONE', *, *, #87092, .F. ) ;
#126566=DIRECTION ( 'NONE',  ( -1.000000000000000000, -0.000000000000000000, -0.000000000000000000 ) ) ;
#126600=EDGE_CURVE ( 'NONE', #115014, #1998, #143276, .T. ) ;
#126651=CYLINDRICAL_SURFACE ( 'NONE', #92438, 2.500000000000000000 ) ;
#126670=CARTESIAN_POINT ( 'NONE',  ( 22.07159235450331991, 2.500000000000001332, 0.000000000000000000 ) ) ;
#126695=CARTESIAN_POINT ( 'NONE',  ( 25.65999999999999659, 9.521314400968980422E-16, 0.000000000000000000 ) ) ;
#126707=DIRECTION ( 'NONE',  ( 0.000000000000000000, -1.000000000000000000, 0.000000000000000000 ) ) ;
#126737=ORIENTED_EDGE ( 'NONE', *, *, #126855, .T. ) ;
#126762=DIRECTION ( 'NONE',  ( 0.000000000000000000, -1.000000000000000000, 0.000000000000000000 ) ) ;
#126788=CARTESIAN_POINT ( 'NONE',  ( -25.39999999999996305, 0.000000000000000000, 0.000000000000000000 ) ) ;
#126829=ORIENTED_EDGE ( 'NONE', *, *, #27514, .T. ) ;
#126855=EDGE_CURVE ( 'NONE', #5733, #122911, #15462, .T. ) ;
#126869=ORIENTED_EDGE ( 'NONE', *, *, #74982, .T. ) ;
#126918=DIRECTION ( 'NONE',  ( -0.5735764363510507113, 0.8191520442889885789, 1.003171929053520926E-16 ) ) ;
#126927=EDGE_CURVE ( 'NONE', #127775, #138069, #34523, .T. ) ;
#127046=EDGE_CURVE ( 'NONE', #129380, #21344, #27563, .T. ) ;
#127058=DIRECTION ( 'NONE',  ( 0.000000000000000000, -1.000000000000000000, 0.000000000000000000 ) ) ;
#127072=CIRCLE ( 'NONE', #106249, 2.500000000000000888 ) ;
#127096=DIRECTION ( 'NONE',  ( 0.000000000000000000, -1.000000000000000000, 0.000000000000000000 ) ) ;
#127106=DIRECTION ( 'NONE',  ( 0.000000000000000000, 1.000000000000000000, 0.000000000000000000 ) ) ;
#127144=ORIENTED_EDGE ( 'NONE', *, *, #16379, .T. ) ;
#127150=CIRCLE ( 'NONE', #2108, 2.500000000000000888 ) ;
#127152=CARTESIAN_POINT ( 'NONE',  ( 22.85159235450332105, 3.061616997868380183E-16, -2.500000000000001332 ) ) ;
#127162=AXIS2_PLACEMENT_3D ( 'NONE', #122859, #130909, #54076 ) ;
#127222=DIRECTION ( 'NONE',  ( -0.5735764363510503783, -0.8191520442889886899, 0.000000000000000000 ) ) ;
#127262=AXIS2_PLACEMENT_3D ( 'NONE', #13899, #24097, #48707 ) ;
#127292=DIRECTION ( 'NONE',  ( 0.000000000000000000, -1.000000000000000000, 0.000000000000000000 ) ) ;
#127364=AXIS2_PLACEMENT_3D ( 'NONE', #48924, #27859, #116298 ) ;
#127408=ORIENTED_EDGE ( 'NONE', *, *, #121521, .F. ) ;
#127421=AXIS2_PLACEMENT_3D ( 'NONE', #132070, #14376, #65401 ) ;
#127456=AXIS2_PLACEMENT_3D ( 'NONE', #10504, #20672, #9038 ) ;
#127463=CARTESIAN_POINT ( 'NONE',  ( 8.968407645496675684, 9.139736423841732040E-16, 0.000000000000000000 ) ) ;
#127471=CARTESIAN_POINT ( 'NONE',  ( 18.95159235450331892, 2.500000000000001776, 0.000000000000000000 ) ) ;
#127501=EDGE_CURVE ( 'NONE', #19604, #21453, #2182, .T. ) ;
#127523=AXIS2_PLACEMENT_3D ( 'NONE', #19797, #140172, #131436 ) ;
#127536=AXIS2_PLACEMENT_3D ( 'NONE', #10127, #54389, #97096 ) ;
#127544=CARTESIAN_POINT ( 'NONE',  ( 16.30000000000000071, 9.521314400968980422E-16, 0.000000000000000000 ) ) ;
#127555=ORIENTED_EDGE ( 'NONE', *, *, #87663, .T. ) ;
#127580=CIRCLE ( 'NONE', #118248, 2.500000000000000888 ) ;
#127582=ORIENTED_EDGE ( 'NONE', *, *, #105983, .F. ) ;
#127588=ADVANCED_FACE ( 'NONE', ( #42978 ), #81002, .T. ) ;
#127593=CARTESIAN_POINT ( 'NONE',  ( -25.39999999999996305, 0.000000000000000000, 0.000000000000000000 ) ) ;
#127643=EDGE_CURVE ( 'NONE', #93367, #77389, #78821, .T. ) ;
#127665=AXIS2_PLACEMENT_3D ( 'NONE', #81296, #37047, #114595 ) ;
#127766=ADVANCED_FACE ( 'NONE', ( #47297 ), #64852, .T. ) ;
#127775=VERTEX_POINT ( 'NONE', #137108 ) ;
#127776=AXIS2_PLACEMENT_3D ( 'NONE', #29821, #18959, #53754 ) ;
#127836=EDGE_CURVE ( 'NONE', #5733, #62841, #130528, .T. ) ;
#127849=EDGE_LOOP ( 'NONE', ( #77619, #115881, #52775, #50546, #53254 ) ) ;
#127877=VECTOR ( 'NONE', #13928, 1000.000000000000000 ) ;
#127880=AXIS2_PLACEMENT_3D ( 'NONE', #8925, #141658, #53195 ) ;
#127882=CARTESIAN_POINT ( 'NONE',  ( 19.88840764549667384, -2.500000000000000888, 0.000000000000000000 ) ) ;
#127886=ORIENTED_EDGE ( 'NONE', *, *, #18601, .F. ) ;
#127938=ORIENTED_EDGE ( 'NONE', *, *, #107315, .T. ) ;
#127947=EDGE_CURVE ( 'NONE', #39432, #9860, #122783, .T. ) ;
#128001=CARTESIAN_POINT ( 'NONE',  ( 15.20840764549667767, 9.139736423841732040E-16, 0.000000000000000000 ) ) ;
#128058=CIRCLE ( 'NONE', #139661, 2.500000000000000888 ) ;
#128095=PRODUCT_DEFINITION ( 'UNKNOWN', '', #104965, #58982 ) ;
#128175=ADVANCED_FACE ( 'NONE', ( #105003 ), #58054, .T. ) ;
#128198=AXIS2_PLACEMENT_3D ( 'NONE', #16147, #37961, #82197 ) ;
#128210=CYLINDRICAL_SURFACE ( 'NONE', #52958, 2.500000000000000000 ) ;
#128212=ORIENTED_EDGE ( 'NONE', *, *, #34657, .T. ) ;
#128260=VERTEX_POINT ( 'NONE', #54242 ) ;
#128262=CIRCLE ( 'NONE', #38028, 2.500000000000000888 ) ;
#128290=EDGE_LOOP ( 'NONE', ( #20522, #63868, #140509, #15787, #2841 ) ) ;
#128334=EDGE_CURVE ( 'NONE', #132789, #15438, #67337, .T. ) ;
#128345=ORIENTED_EDGE ( 'NONE', *, *, #31398, .T. ) ;
#128401=DIRECTION ( 'NONE',  ( 1.000000000000000000, 1.224606353822377258E-16, 0.000000000000000000 ) ) ;
#128434=VECTOR ( 'NONE', #60828, 1000.000000000000000 ) ;
#128454=ORIENTED_EDGE ( 'NONE', *, *, #109950, .T. ) ;
#128487=ORIENTED_EDGE ( 'NONE', *, *, #48886, .T. ) ;
#128491=CONICAL_SURFACE ( 'NONE', #68294, 2.500000000000000888, 0.9599310885968822538 ) ;
#128515=CARTESIAN_POINT ( 'NONE',  ( 19.41999999999999815, -2.055000000000000160, 0.000000000000000000 ) ) ;
#128516=DIRECTION ( 'NONE',  ( 0.000000000000000000, -1.000000000000000000, 0.000000000000000000 ) ) ;
#128529=CIRCLE ( 'NONE', #12796, 2.055000000000001048 ) ;
#128635=ADVANCED_FACE ( 'NONE', ( #130910 ), #79056, .T. ) ;
#128661=CARTESIAN_POINT ( 'NONE',  ( 22.07159235450331991, -3.851859888774471706E-31, 2.500000000000001332 ) ) ;
#128694=EDGE_CURVE ( 'NONE', #17414, #65959, #109841, .T. ) ;
#128695=CARTESIAN_POINT ( 'NONE',  ( 8.188407645496676324, 9.139736423841732040E-16, 0.000000000000000000 ) ) ;
#128710=VECTOR ( 'NONE', #2518, 999.9999999999998863 ) ;
#128728=FACE_OUTER_BOUND ( 'NONE', #35849, .T. ) ;
#128735=ORIENTED_EDGE ( 'NONE', *, *, #91204, .F. ) ;
#128785=CIRCLE ( 'NONE', #61655, 2.055000000000001048 ) ;
#128787=FACE_OUTER_BOUND ( 'NONE', #52901, .T. ) ;
#128813=VERTEX_POINT ( 'NONE', #46788 ) ;
#128831=CARTESIAN_POINT ( 'NONE',  ( 15.83159235450332147, 9.902892378096218942E-16, 0.000000000000000000 ) ) ;
#128841=DIRECTION ( 'NONE',  ( -0.5735764363510507113, 0.8191520442889885789, 1.003171929053520926E-16 ) ) ;
#128873=DIRECTION ( 'NONE',  ( 0.000000000000000000, -1.000000000000000000, 0.000000000000000000 ) ) ;
#128883=CARTESIAN_POINT ( 'NONE',  ( 8.188407645496676324, 9.139736423841732040E-16, 0.000000000000000000 ) ) ;
#128913=EDGE_CURVE ( 'NONE', #110130, #11132, #90505, .T. ) ;
#128919=CARTESIAN_POINT ( 'NONE',  ( 22.53999999999999915, 9.521314400968980422E-16, 0.000000000000000000 ) ) ;
#128927=VERTEX_POINT ( 'NONE', #127882 ) ;
#128966=DIRECTION ( 'NONE',  ( -1.000000000000000000, -1.224606353822377258E-16, -0.000000000000000000 ) ) ;
#128973=ORIENTED_EDGE ( 'NONE', *, *, #119078, .T. ) ;
#129010=VECTOR ( 'NONE', #141281, 1000.000000000000000 ) ;
#129031=FACE_OUTER_BOUND ( 'NONE', #80595, .T. ) ;
#129038=CONICAL_SURFACE ( 'NONE', #13330, 2.500000000000000888, 0.9599310885968822538 ) ;
#129117=FACE_OUTER_BOUND ( 'NONE', #96579, .T. ) ;
#129129=CARTESIAN_POINT ( 'NONE',  ( 5.691592354503320905, -3.851859888774471706E-31, 2.500000000000001332 ) ) ;
#129159=EDGE_LOOP ( 'NONE', ( #102881, #131822, #28525, #44631, #21107 ) ) ;
#129169=CARTESIAN_POINT ( 'NONE',  ( 22.85159235450332105, 2.500000000000001776, 0.000000000000000000 ) ) ;
#129177=ORIENTED_EDGE ( 'NONE', *, *, #116123, .F. ) ;
#129190=ORIENTED_EDGE ( 'NONE', *, *, #127046, .F. ) ;
#129205=AXIS2_PLACEMENT_3D ( 'NONE', #125655, #70590, #2394 ) ;
#129206=AXIS2_PLACEMENT_3D ( 'NONE', #15223, #71089, #60209 ) ;
#129212=ADVANCED_FACE ( 'NONE', ( #12486 ), #89346, .T. ) ;
#129227=ORIENTED_EDGE ( 'NONE', *, *, #125471, .F. ) ;
#129247=CARTESIAN_POINT ( 'NONE',  ( 24.56840764549667355, 2.500000000000003553, 3.061616997868386099E-16 ) ) ;
#129292=FACE_OUTER_BOUND ( 'NONE', #53611, .T. ) ;
#129293=ORIENTED_EDGE ( 'NONE', *, *, #140376, .T. ) ;
#129327=EDGE_CURVE ( 'NONE', #39945, #110130, #95584, .T. ) ;
#129336=VECTOR ( 'NONE', #83511, 1000.000000000000000 ) ;
#129346=AXIS2_PLACEMENT_3D ( 'NONE', #128919, #84709, #39806 ) ;
#129380=VERTEX_POINT ( 'NONE', #1247 ) ;
#129394=ORIENTED_EDGE ( 'NONE', *, *, #5595, .F. ) ;
#129395=AXIS2_PLACEMENT_3D ( 'NONE', #63833, #30480, #86297 ) ;
#129433=CARTESIAN_POINT ( 'NONE',  ( 9.279999999999999361, 2.055000000000001492, 2.516649172247811554E-16 ) ) ;
#129490=CARTESIAN_POINT ( 'NONE',  ( 14.27159235450332098, 9.902892378096218942E-16, 0.000000000000000000 ) ) ;
#129511=FILL_AREA_STYLE_COLOUR ( '', #33112 ) ;
#129577=ADVANCED_FACE ( 'NONE', ( #136067 ), #103419, .T. ) ;
#129585=DIRECTION ( 'NONE',  ( -1.000000000000000000, -1.224606353822377258E-16, -0.000000000000000000 ) ) ;
#129594=DIRECTION ( 'NONE',  ( 0.000000000000000000, 0.000000000000000000, 1.000000000000000000 ) ) ;
#129607=AXIS2_PLACEMENT_3D ( 'NONE', #97442, #99576, #32958 ) ;
#129610=ORIENTED_EDGE ( 'NONE', *, *, #57102, .T. ) ;
#129744=FACE_OUTER_BOUND ( 'NONE', #51735, .T. ) ;
#129746=CIRCLE ( 'NONE', #85764, 2.500000000000000888 ) ;
#129780=ADVANCED_FACE ( 'NONE', ( #109866 ), #142517, .T. ) ;
#129807=CIRCLE ( 'NONE', #127421, 2.500000000000000888 ) ;
#129826=ORIENTED_EDGE ( 'NONE', *, *, #22985, .F. ) ;
#129839=CARTESIAN_POINT ( 'NONE',  ( 11.30840764549667554, 9.139736423841732040E-16, 0.000000000000000000 ) ) ;
#129879=VERTEX_POINT ( 'NONE', #76550 ) ;
#129883=AXIS2_PLACEMENT_3D ( 'NONE', #105568, #31612, #119999 ) ;
#129901=AXIS2_PLACEMENT_3D ( 'NONE', #63881, #17490, #85594 ) ;
#129902=CARTESIAN_POINT ( 'NONE',  ( 15.20840764549667767, 2.500000000000000888, 3.061616997868383141E-16 ) ) ;
#129928=VECTOR ( 'NONE', #98479, 1000.000000000000114 ) ;
#129932=AXIS2_PLACEMENT_3D ( 'NONE', #58323, #3831, #12607 ) ;
#129946=CARTESIAN_POINT ( 'NONE',  ( 9.591592354503321260, 2.500000000000001776, 0.000000000000000000 ) ) ;
#129964=DIRECTION ( 'NONE',  ( 0.000000000000000000, 0.000000000000000000, 1.000000000000000000 ) ) ;
#129965=CARTESIAN_POINT ( 'NONE',  ( 4.288407645496676857, 9.139736423841732040E-16, 0.000000000000000000 ) ) ;
#130002=CARTESIAN_POINT ( 'NONE',  ( 17.39159235450332019, 2.500000000000001776, 0.000000000000000000 ) ) ;
#130008=AXIS2_PLACEMENT_3D ( 'NONE', #55508, #90248, #47521 ) ;
#130026=AXIS2_PLACEMENT_3D ( 'NONE', #137389, #38081, #51097 ) ;
#130082=ORIENTED_EDGE ( 'NONE', *, *, #44003, .F. ) ;
#130095=CARTESIAN_POINT ( 'NONE',  ( 19.88840764549667384, 9.139736423841732040E-16, 0.000000000000000000 ) ) ;
#130168=FACE_OUTER_BOUND ( 'NONE', #13635, .T. ) ;
#130174=AXIS2_PLACEMENT_3D ( 'NONE', #46498, #134918, #35611 ) ;
#130192=VERTEX_POINT ( 'NONE', #127152 ) ;
#130268=AXIS2_PLACEMENT_3D ( 'NONE', #54753, #101082, #110511 ) ;
#130284=PLANE ( 'NONE',  #143384 ) ;
#130291=DIRECTION ( 'NONE',  ( 0.000000000000000000, -1.000000000000000000, 0.000000000000000000 ) ) ;
#130308=CARTESIAN_POINT ( 'NONE',  ( 27.68840764549667455, -2.499999999999996003, 0.000000000000000000 ) ) ;
#130355=CARTESIAN_POINT ( 'NONE',  ( 13.64840764549667540, 3.061616997868380183E-16, -2.500000000000001332 ) ) ;
#130396=DIRECTION ( 'NONE',  ( -1.000000000000000000, -0.000000000000000000, -0.000000000000000000 ) ) ;
#130401=ORIENTED_EDGE ( 'NONE', *, *, #69236, .T. ) ;
#130427=CARTESIAN_POINT ( 'NONE',  ( -25.39999999999996305, 0.000000000000000000, 0.000000000000000000 ) ) ;
#130442=ADVANCED_FACE ( 'NONE', ( #66914 ), #67777, .T. ) ;
#130462=FACE_OUTER_BOUND ( 'NONE', #121005, .T. ) ;
#130486=ORIENTED_EDGE ( 'NONE', *, *, #23338, .T. ) ;
#130497=LINE ( 'NONE', #107283, #111244 ) ;
#130521=EDGE_CURVE ( 'NONE', #28286, #99726, #56069, .T. ) ;
#130528=LINE ( 'NONE', #7268, #74160 ) ;
#130543=CARTESIAN_POINT ( 'NONE',  ( -25.39999999999996305, 0.000000000000000000, 2.500000000000000000 ) ) ;
#130544=CARTESIAN_POINT ( 'NONE',  ( 18.95159235450331892, 9.902892378096218942E-16, 0.000000000000000000 ) ) ;
#130559=VERTEX_POINT ( 'NONE', #13214 ) ;
#130560=CARTESIAN_POINT ( 'NONE',  ( 6.471592354503322042, 2.500000000000001776, 0.000000000000000000 ) ) ;
#130575=CARTESIAN_POINT ( 'NONE',  ( 13.49159235450332162, -3.851859888774471706E-31, 2.500000000000001332 ) ) ;
#130633=VECTOR ( 'NONE', #3509, 1000.000000000000114 ) ;
#130634=CARTESIAN_POINT ( 'NONE',  ( 22.22840764549667725, 3.061616997868380183E-16, -2.500000000000001332 ) ) ;
#130663=ORIENTED_EDGE ( 'NONE', *, *, #14888, .F. ) ;
#130670=CARTESIAN_POINT ( 'NONE',  ( 18.95159235450331892, 9.902892378096218942E-16, 0.000000000000000000 ) ) ;
#130690=ORIENTED_EDGE ( 'NONE', *, *, #107411, .T. ) ;
#130697=EDGE_CURVE ( 'NONE', #137066, #124568, #116365, .T. ) ;
#130698=AXIS2_PLACEMENT_3D ( 'NONE', #99830, #496, #44790 ) ;
#130701=DIRECTION ( 'NONE',  ( 0.000000000000000000, 1.000000000000000000, 0.000000000000000000 ) ) ;
#130703=FACE_OUTER_BOUND ( 'NONE', #70236, .T. ) ;
#130715=CARTESIAN_POINT ( 'NONE',  ( 27.68840764549667455, 9.139736423841732040E-16, 0.000000000000000000 ) ) ;
#130745=FACE_OUTER_BOUND ( 'NONE', #113611, .T. ) ;
#130756=EDGE_CURVE ( 'NONE', #31572, #70129, #20352, .T. ) ;
#130812=CARTESIAN_POINT ( 'NONE',  ( 9.279999999999999361, 2.055000000000001492, 0.000000000000000000 ) ) ;
#130815=ORIENTED_EDGE ( 'NONE', *, *, #76140, .T. ) ;
#130821=AXIS2_PLACEMENT_3D ( 'NONE', #102128, #5625, #28128 ) ;
#130833=EDGE_CURVE ( 'NONE', #78861, #112275, #140462, .T. ) ;
#130849=ORIENTED_EDGE ( 'NONE', *, *, #27402, .F. ) ;
#130909=DIRECTION ( 'NONE',  ( -1.000000000000000000, -1.224606353822377258E-16, -0.000000000000000000 ) ) ;
#130910=FACE_OUTER_BOUND ( 'NONE', #74426, .T. ) ;
#130911=VERTEX_POINT ( 'NONE', #33677 ) ;
#130932=EDGE_LOOP ( 'NONE', ( #113640, #81938, #140013, #70368, #278, #124504 ) ) ;
#130947=CARTESIAN_POINT ( 'NONE',  ( 19.41999999999999815, 9.521314400968980422E-16, 0.000000000000000000 ) ) ;
#131005=ORIENTED_EDGE ( 'NONE', *, *, #57746, .F. ) ;
#131015=CIRCLE ( 'NONE', #93947, 4.582731094065999322 ) ;
#131063=VECTOR ( 'NONE', #75326, 1000.000000000000000 ) ;
#131084=DIRECTION ( 'NONE',  ( -1.000000000000000000, -0.000000000000000000, -0.000000000000000000 ) ) ;
#131096=CARTESIAN_POINT ( 'NONE',  ( 23.63159235450331863, 3.061616997868375253E-16, -2.500000000000001332 ) ) ;
#131104=CIRCLE ( 'NONE', #68614, 2.500000000000000888 ) ;
#131122=CARTESIAN_POINT ( 'NONE',  ( 0.5741843527964840543, 0.5999999999999987566, -4.263785792382349449 ) ) ;
#131172=DIRECTION ( 'NONE',  ( 0.000000000000000000, -1.000000000000000000, 0.000000000000000000 ) ) ;
#131198=ORIENTED_EDGE ( 'NONE', *, *, #3851, .F. ) ;
#131203=DIRECTION ( 'NONE',  ( 0.000000000000000000, -1.000000000000000000, 0.000000000000000000 ) ) ;
#131206=DIRECTION ( 'NONE',  ( -1.000000000000000000, -1.224606353822377258E-16, -0.000000000000000000 ) ) ;
#131221=ORIENTED_EDGE ( 'NONE', *, *, #37149, .T. ) ;
#131261=DIRECTION ( 'NONE',  ( -1.000000000000000000, -1.224606353822377258E-16, -0.000000000000000000 ) ) ;
#131265=DIRECTION ( 'NONE',  ( -1.000000000000000000, -1.224606353822377258E-16, -0.000000000000000000 ) ) ;
#131273=VERTEX_POINT ( 'NONE', #77016 ) ;
#131294=CIRCLE ( 'NONE', #82660, 2.500000000000000888 ) ;
#131312=ORIENTED_EDGE ( 'NONE', *, *, #77429, .F. ) ;
#131436=DIRECTION ( 'NONE',  ( 0.000000000000000000, -1.000000000000000000, 0.000000000000000000 ) ) ;
#131437=CYLINDRICAL_SURFACE ( 'NONE', #73245, 2.500000000000000000 ) ;
#131448=AXIS2_PLACEMENT_3D ( 'NONE', #127463, #48477, #103551 ) ;
#131459=DIRECTION ( 'NONE',  ( -1.000000000000000000, -1.224606353822377258E-16, -0.000000000000000000 ) ) ;
#131468=DIRECTION ( 'NONE',  ( 0.000000000000000000, 1.000000000000000000, 0.000000000000000000 ) ) ;
#131512=CARTESIAN_POINT ( 'NONE',  ( 23.78840764549667597, 9.139736423841732040E-16, 0.000000000000000000 ) ) ;
#131514=ORIENTED_EDGE ( 'NONE', *, *, #91107, .T. ) ;
#131565=CARTESIAN_POINT ( 'NONE',  ( 9.748407645496676821, 3.061616997868380183E-16, -2.500000000000001332 ) ) ;
#131610=AXIS2_PLACEMENT_3D ( 'NONE', #63666, #40482, #18676 ) ;
#131617=CONICAL_SURFACE ( 'NONE', #108379, 2.500000000000000888, 0.9599310885968822538 ) ;
#131677=EDGE_CURVE ( 'NONE', #135110, #35704, #5182, .T. ) ;
#131694=CARTESIAN_POINT ( 'NONE',  ( 7.720000000000001528, -2.055000000000000160, 0.000000000000000000 ) ) ;
#131742=DIRECTION ( 'NONE',  ( -0.5735764363510503783, -0.8191520442889886899, 0.000000000000000000 ) ) ;
#131822=ORIENTED_EDGE ( 'NONE', *, *, #6039, .T. ) ;
#131833=DIRECTION ( 'NONE',  ( -1.000000000000000000, -0.000000000000000000, -0.000000000000000000 ) ) ;
#131840=CONICAL_SURFACE ( 'NONE', #87849, 2.500000000000000888, 0.9599310885968822538 ) ;
#131867=CARTESIAN_POINT ( 'NONE',  ( 14.42840764549667476, 9.139736423841732040E-16, 0.000000000000000000 ) ) ;
#131884=EDGE_CURVE ( 'NONE', #72729, #142002, #37616, .T. ) ;
#131908=AXIS2_PLACEMENT_3D ( 'NONE', #72194, #93887, #17055 ) ;
#131918=ORIENTED_EDGE ( 'NONE', *, *, #101427, .T. ) ;
#131931=ORIENTED_EDGE ( 'NONE', *, *, #9985, .F. ) ;
#131963=DIRECTION ( 'NONE',  ( 0.000000000000000000, -1.000000000000000000, 0.000000000000000000 ) ) ;
#131979=ORIENTED_EDGE ( 'NONE', *, *, #56680, .F. ) ;
#132019=AXIS2_PLACEMENT_3D ( 'NONE', #7973, #96400, #98568 ) ;
#132058=LINE ( 'NONE', #110968, #61987 ) ;
#132067=VECTOR ( 'NONE', #77842, 1000.000000000000000 ) ;
#132070=CARTESIAN_POINT ( 'NONE',  ( 4.288407645496676857, 9.139736423841732040E-16, 0.000000000000000000 ) ) ;
#132076=EDGE_CURVE ( 'NONE', #39432, #48488, #90188, .T. ) ;
#132102=ORIENTED_EDGE ( 'NONE', *, *, #38428, .F. ) ;
#132122=CIRCLE ( 'NONE', #27893, 2.055000000000001048 ) ;
#132146=DIRECTION ( 'NONE',  ( 0.000000000000000000, -1.000000000000000000, 0.000000000000000000 ) ) ;
#132152=ORIENTED_EDGE ( 'NONE', *, *, #78802, .T. ) ;
#132174=CARTESIAN_POINT ( 'NONE',  ( 2.999999999999999556, 2.500000000000000000, 0.000000000000000000 ) ) ;
#132209=CIRCLE ( 'NONE', #85918, 2.500000000000000888 ) ;
#132211=ADVANCED_FACE ( 'NONE', ( #92315 ), #115473, .T. ) ;
#132235=CIRCLE ( 'NONE', #28001, 2.500000000000000888 ) ;
#132253=CARTESIAN_POINT ( 'NONE',  ( 25.34840764549667469, 9.139736423841732040E-16, 0.000000000000000000 ) ) ;
#132275=CARTESIAN_POINT ( 'NONE',  ( 27.99999999999999645, -2.055000000000000160, 0.000000000000000000 ) ) ;
#132277=EDGE_CURVE ( 'NONE', #52856, #80457, #60827, .T. ) ;
#132290=CARTESIAN_POINT ( 'NONE',  ( 16.61159235450331906, 9.902892378096218942E-16, 0.000000000000000000 ) ) ;
#132305=CARTESIAN_POINT ( 'NONE',  ( -25.39999999999996305, 0.000000000000000000, 0.000000000000000000 ) ) ;
#132330=AXIS2_PLACEMENT_3D ( 'NONE', #116417, #17784, #39589 ) ;
#132356=EDGE_LOOP ( 'NONE', ( #108321, #121329, #104465, #21877, #115758 ) ) ;
#132357=DIRECTION ( 'NONE',  ( 0.000000000000000000, -1.000000000000000000, 0.000000000000000000 ) ) ;
#132367=AXIS2_PLACEMENT_3D ( 'NONE', #13271, #124915, #57543 ) ;
#132373=ORIENTED_EDGE ( 'NONE', *, *, #90718, .T. ) ;
#132419=DIRECTION ( 'NONE',  ( -1.000000000000000000, -1.224606353822377258E-16, -0.000000000000000000 ) ) ;
#132455=DIRECTION ( 'NONE',  ( 0.000000000000000000, -1.000000000000000000, 0.000000000000000000 ) ) ;
#132501=CONICAL_SURFACE ( 'NONE', #86104, 2.500000000000000888, 0.9599310885968822538 ) ;
#132522=ORIENTED_EDGE ( 'NONE', *, *, #123395, .T. ) ;
#132528=VERTEX_POINT ( 'NONE', #10306 ) ;
#132558=DIRECTION ( 'NONE',  ( -0.5735764363510507113, 0.8191520442889885789, 1.003171929053520926E-16 ) ) ;
#132560=DIRECTION ( 'NONE',  ( 0.000000000000000000, -1.000000000000000000, 0.000000000000000000 ) ) ;
#132620=DIRECTION ( 'NONE',  ( 0.000000000000000000, -1.000000000000000000, 0.000000000000000000 ) ) ;
#132647=EDGE_LOOP ( 'NONE', ( #96075, #58073, #141472, #41564, #6555, #27272 ) ) ;
#132670=ADVANCED_FACE ( 'NONE', ( #58888 ), #3686, .T. ) ;
#132681=AXIS2_PLACEMENT_3D ( 'NONE', #7030, #18637, #105651 ) ;
#132734=CARTESIAN_POINT ( 'NONE',  ( 1.199999999999999956, -0.5999999999999993117, -4.543283425070392845 ) ) ;
#132737=ORIENTED_EDGE ( 'NONE', *, *, #59381, .F. ) ;
#132767=EDGE_CURVE ( 'NONE', #69819, #100020, #52225, .T. ) ;
#132789=VERTEX_POINT ( 'NONE', #140650 ) ;
#132830=DIRECTION ( 'NONE',  ( 0.000000000000000000, 1.000000000000000000, 0.000000000000000000 ) ) ;
#132844=CARTESIAN_POINT ( 'NONE',  ( 11.15159235450332176, -3.851859888774471706E-31, 2.500000000000001332 ) ) ;
#132857=( GEOMETRIC_REPRESENTATION_CONTEXT ( 3 ) GLOBAL_UNCERTAINTY_ASSIGNED_CONTEXT ( ( #28896 ) ) GLOBAL_UNIT_ASSIGNED_CONTEXT ( ( #13627, #42916, #76987 ) ) REPRESENTATION_CONTEXT ( 'NONE', 'WORKASPACE' ) );
#132964=LINE ( 'NONE', #100312, #132067 ) ;
#132967=EDGE_CURVE ( 'NONE', #57169, #40200, #122465, .T. ) ;
#132976=DIRECTION ( 'NONE',  ( -1.000000000000000000, -1.224606353822377258E-16, -0.000000000000000000 ) ) ;
#133013=CARTESIAN_POINT ( 'NONE',  ( 7.720000000000001528, 2.055000000000001492, 2.516649172247811554E-16 ) ) ;
#133065=CIRCLE ( 'NONE', #123738, 2.500000000000000888 ) ;
#133082=ORIENTED_EDGE ( 'NONE', *, *, #92777, .F. ) ;
#133107=EDGE_CURVE ( 'NONE', #34133, #60854, #2084, .T. ) ;
#133114=VERTEX_POINT ( 'NONE', #47814 ) ;
#133142=DIRECTION ( 'NONE',  ( 0.000000000000000000, -1.000000000000000000, 0.000000000000000000 ) ) ;
#133164=AXIS2_PLACEMENT_3D ( 'NONE', #95052, #109331, #32499 ) ;
#133166=CARTESIAN_POINT ( 'NONE',  ( 22.07159235450331991, 3.061616997868380183E-16, -2.500000000000001332 ) ) ;
#133181=EDGE_CURVE ( 'NONE', #50175, #9966, #49937, .T. ) ;
#133192=AXIS2_PLACEMENT_3D ( 'NONE', #83968, #86800, #96903 ) ;
#133232=DIRECTION ( 'NONE',  ( -1.000000000000000000, -1.224606353822377258E-16, -0.000000000000000000 ) ) ;
#133318=EDGE_CURVE ( 'NONE', #108418, #133114, #131015, .T. ) ;
#133331=CARTESIAN_POINT ( 'NONE',  ( 20.51159235450331764, 9.902892378096218942E-16, 0.000000000000000000 ) ) ;
#133353=ORIENTED_EDGE ( 'NONE', *, *, #137906, .F. ) ;
#133398=DIRECTION ( 'NONE',  ( -1.000000000000000000, -0.000000000000000000, -0.000000000000000000 ) ) ;
#133412=DIRECTION ( 'NONE',  ( -1.000000000000000000, -1.224606353822377258E-16, -0.000000000000000000 ) ) ;
#133418=CYLINDRICAL_SURFACE ( 'NONE', #51163, 2.500000000000000000 ) ;
#133533=DIRECTION ( 'NONE',  ( -1.000000000000000000, -1.224606353822377258E-16, -0.000000000000000000 ) ) ;
#133535=CARTESIAN_POINT ( 'NONE',  ( 24.56840764549667355, 0.000000000000000000, 2.500000000000001332 ) ) ;
#133541=ORIENTED_EDGE ( 'NONE', *, *, #94394, .F. ) ;
#133557=AXIS2_PLACEMENT_3D ( 'NONE', #82301, #17707, #72887 ) ;
#133591=CARTESIAN_POINT ( 'NONE',  ( -25.39999999999996305, 0.000000000000000000, 2.500000000000000000 ) ) ;
#133593=AXIS2_PLACEMENT_3D ( 'NONE', #18782, #60932, #95637 ) ;
#133602=DIRECTION ( 'NONE',  ( -1.000000000000000000, -1.224606353822377258E-16, -0.000000000000000000 ) ) ;
#133636=CARTESIAN_POINT ( 'NONE',  ( 26.43999999999999773, 2.055000000000001492, 0.000000000000000000 ) ) ;
#133720=ORIENTED_EDGE ( 'NONE', *, *, #106030, .F. ) ;
#133730=DIRECTION ( 'NONE',  ( -0.5735764363510503783, -0.8191520442889886899, 0.000000000000000000 ) ) ;
#133743=LINE ( 'NONE', #134460, #111306 ) ;
#133745=DIRECTION ( 'NONE',  ( 0.000000000000000000, -1.000000000000000000, 0.000000000000000000 ) ) ;
#133775=VECTOR ( 'NONE', #1180, 1000.000000000000000 ) ;
#133824=ADVANCED_FACE ( 'NONE', ( #42117 ), #98604, .T. ) ;
#133861=CARTESIAN_POINT ( 'NONE',  ( 8.188407645496676324, -3.851859888774471706E-31, 2.500000000000001332 ) ) ;
#133922=CARTESIAN_POINT ( 'NONE',  ( 23.32000000000000028, 9.521314400968980422E-16, 0.000000000000000000 ) ) ;
#133941=CARTESIAN_POINT ( 'NONE',  ( -25.39999999999996305, 0.000000000000000000, 0.000000000000000000 ) ) ;
#133972=CARTESIAN_POINT ( 'NONE',  ( 24.09999999999999787, 9.521314400968980422E-16, 0.000000000000000000 ) ) ;
#133994=ORIENTED_EDGE ( 'NONE', *, *, #64442, .T. ) ;
#134040=DIRECTION ( 'NONE',  ( -1.000000000000000000, -1.224606353822377258E-16, -0.000000000000000000 ) ) ;
#134076=ORIENTED_EDGE ( 'NONE', *, *, #133107, .T. ) ;
#134097=EDGE_LOOP ( 'NONE', ( #116356, #39140, #28739, #128735, #22468, #120965 ) ) ;
#134148=AXIS2_PLACEMENT_3D ( 'NONE', #24064, #90013, #13151 ) ;
#134172=ORIENTED_EDGE ( 'NONE', *, *, #38227, .F. ) ;
#134176=DIRECTION ( 'NONE',  ( -0.5735764363510507113, 0.8191520442889885789, 1.003171929053520926E-16 ) ) ;
#134189=ADVANCED_FACE ( 'NONE', ( #105029 ), #72456, .T. ) ;
#134190=DIRECTION ( 'NONE',  ( 0.5735764363510453823, -0.8191520442889923537, 1.003171929053525486E-16 ) ) ;
#134241=AXIS2_PLACEMENT_3D ( 'NONE', #12998, #24603, #102188 ) ;
#134287=DIRECTION ( 'NONE',  ( 0.000000000000000000, -1.000000000000000000, 0.000000000000000000 ) ) ;
#134312=ORIENTED_EDGE ( 'NONE', *, *, #56337, .F. ) ;
#134321=CARTESIAN_POINT ( 'NONE',  ( -25.39999999999996305, 3.061616997868383141E-16, -2.500000000000000000 ) ) ;
#134330=DIRECTION ( 'NONE',  ( 0.5735764363510451602, 0.8191520442889924647, 0.000000000000000000 ) ) ;
#134401=CIRCLE ( 'NONE', #2406, 2.055000000000001048 ) ;
#134414=VECTOR ( 'NONE', #94811, 1000.000000000000000 ) ;
#134460=CARTESIAN_POINT ( 'NONE',  ( 22.07159235450331991, -2.500000000000000000, 3.061616997868384127E-16 ) ) ;
#134464=LINE ( 'NONE', #135197, #76273 ) ;
#134501=AXIS2_PLACEMENT_3D ( 'NONE', #42422, #75747, #54715 ) ;
#134507=ORIENTED_EDGE ( 'NONE', *, *, #64947, .F. ) ;
#134545=CARTESIAN_POINT ( 'NONE',  ( 7.251592354503322291, 2.500000000000001776, 0.000000000000000000 ) ) ;
#134583=AXIS2_PLACEMENT_3D ( 'NONE', #104498, #137148, #137872 ) ;
#134608=CIRCLE ( 'NONE', #129932, 2.500000000000000888 ) ;
#134623=EDGE_CURVE ( 'NONE', #21154, #3387, #52443, .T. ) ;
#134714=ADVANCED_FACE ( 'NONE', ( #129292 ), #59517, .T. ) ;
#134768=DIRECTION ( 'NONE',  ( -1.000000000000000000, -1.224606353822377258E-16, -0.000000000000000000 ) ) ;
#134792=ORIENTED_EDGE ( 'NONE', *, *, #41483, .T. ) ;
#134828=CARTESIAN_POINT ( 'NONE',  ( 8.031592354503320763, 9.902892378096218942E-16, 0.000000000000000000 ) ) ;
#134860=CONICAL_SURFACE ( 'NONE', #19124, 2.055000000000001048, 0.9599310885968758145 ) ;
#134885=CIRCLE ( 'NONE', #33066, 2.500000000000000888 ) ;
#134897=ORIENTED_EDGE ( 'NONE', *, *, #76555, .T. ) ;
#134900=LINE ( 'NONE', #34860, #139473 ) ;
#134911=VECTOR ( 'NONE', #139979, 1000.000000000000114 ) ;
#134918=DIRECTION ( 'NONE',  ( -1.000000000000000000, -1.224606353822377258E-16, -0.000000000000000000 ) ) ;
#134955=CIRCLE ( 'NONE', #70090, 2.055000000000001048 ) ;
#134956=ORIENTED_EDGE ( 'NONE', *, *, #53889, .F. ) ;
#134976=CARTESIAN_POINT ( 'NONE',  ( 20.97999999999999687, 2.055000000000001492, 0.000000000000000000 ) ) ;
#135004=DIRECTION ( 'NONE',  ( -1.000000000000000000, -1.224606353822377258E-16, -0.000000000000000000 ) ) ;
#135030=CARTESIAN_POINT ( 'NONE',  ( 17.39159235450332019, 9.902892378096218942E-16, 0.000000000000000000 ) ) ;
#135048=PLANE ( 'NONE',  #53717 ) ;
#135086=DIRECTION ( 'NONE',  ( 0.000000000000000000, 1.000000000000000000, 0.000000000000000000 ) ) ;
#135097=CARTESIAN_POINT ( 'NONE',  ( -25.39999999999996305, 3.061616997868383141E-16, -2.500000000000000000 ) ) ;
#135110=VERTEX_POINT ( 'NONE', #19665 ) ;
#135135=ADVANCED_FACE ( 'NONE', ( #50174 ), #89596, .T. ) ;
#135156=DIRECTION ( 'NONE',  ( -1.000000000000000000, -1.224606353822377258E-16, -0.000000000000000000 ) ) ;
#135172=CIRCLE ( 'NONE', #121358, 2.500000000000000888 ) ;
#135183=EDGE_CURVE ( 'NONE', #100764, #110693, #105250, .T. ) ;
#135196=DIRECTION ( 'NONE',  ( 0.000000000000000000, 0.000000000000000000, 1.000000000000000000 ) ) ;
#135197=CARTESIAN_POINT ( 'NONE',  ( 24.09999999999999787, 2.055000000000001492, 2.516649172247811554E-16 ) ) ;
#135235=DIRECTION ( 'NONE',  ( 0.000000000000000000, -1.000000000000000000, 0.000000000000000000 ) ) ;
#135236=LINE ( 'NONE', #99712, #128710 ) ;
#135237=DIRECTION ( 'NONE',  ( 1.000000000000000000, 1.224606353822377258E-16, 0.000000000000000000 ) ) ;
#135291=AXIS2_PLACEMENT_3D ( 'NONE', #41159, #129585, #52051 ) ;
#135296=VERTEX_POINT ( 'NONE', #122345 ) ;
#135347=CARTESIAN_POINT ( 'NONE',  ( 16.30000000000000071, 2.055000000000001492, 2.516649172247811554E-16 ) ) ;
#135385=EDGE_CURVE ( 'NONE', #97144, #111999, #34150, .T. ) ;
#135398=LINE ( 'NONE', #91851, #30327 ) ;
#135433=DIRECTION ( 'NONE',  ( -1.000000000000000000, -1.224606353822377258E-16, -0.000000000000000000 ) ) ;
#135438=DIRECTION ( 'NONE',  ( -1.000000000000000000, -0.000000000000000000, -0.000000000000000000 ) ) ;
#135449=DIRECTION ( 'NONE',  ( 0.000000000000000000, -1.000000000000000000, 0.000000000000000000 ) ) ;
#135454=DIRECTION ( 'NONE',  ( 0.000000000000000000, -1.000000000000000000, 0.000000000000000000 ) ) ;
#135462=ORIENTED_EDGE ( 'NONE', *, *, #127643, .T. ) ;
#135480=EDGE_LOOP ( 'NONE', ( #13431, #73770, #101669, #119318, #98356 ) ) ;
#135487=ORIENTED_EDGE ( 'NONE', *, *, #64393, .T. ) ;
#135510=EDGE_CURVE ( 'NONE', #36671, #4396, #99003, .T. ) ;
#135543=ADVANCED_FACE ( 'NONE', ( #128787 ), #89703, .T. ) ;
#135574=VERTEX_POINT ( 'NONE', #9859 ) ;
#135647=CARTESIAN_POINT ( 'NONE',  ( 22.85159235450332105, 9.902892378096218942E-16, 0.000000000000000000 ) ) ;
#135650=DIRECTION ( 'NONE',  ( 1.000000000000000000, 1.224606353822377258E-16, 0.000000000000000000 ) ) ;
#135653=CIRCLE ( 'NONE', #26875, 2.500000000000000888 ) ;
#135663=LINE ( 'NONE', #26187, #122771 ) ;
#135679=CARTESIAN_POINT ( 'NONE',  ( 12.08840764549667668, 9.139736423841732040E-16, 0.000000000000000000 ) ) ;
#135688=PLANE ( 'NONE',  #79716 ) ;
#135700=VECTOR ( 'NONE', #10535, 1000.000000000000000 ) ;
#135713=DIRECTION ( 'NONE',  ( -1.000000000000000000, -1.224606353822377258E-16, -0.000000000000000000 ) ) ;
#135730=AXIS2_PLACEMENT_3D ( 'NONE', #38102, #5425, #49705 ) ;
#135732=ADVANCED_FACE ( 'NONE', ( #23598 ), #11993, .T. ) ;
#135738=AXIS2_PLACEMENT_3D ( 'NONE', #70890, #38244, #73714 ) ;
#135786=CYLINDRICAL_SURFACE ( 'NONE', #75925, 2.500000000000000000 ) ;
#135798=ORIENTED_EDGE ( 'NONE', *, *, #74247, .T. ) ;
#135834=CARTESIAN_POINT ( 'NONE',  ( 22.07159235450331991, -2.500000000000000444, 3.061616997868384620E-16 ) ) ;
#135839=CARTESIAN_POINT ( 'NONE',  ( 16.61159235450331906, -7.703719777548943412E-31, 2.500000000000001332 ) ) ;
#135858=AXIS2_PLACEMENT_3D ( 'NONE', #102265, #58069, #58802 ) ;
#135864=FACE_OUTER_BOUND ( 'NONE', #57149, .T. ) ;
#135921=CARTESIAN_POINT ( 'NONE',  ( 17.54840764549667398, 9.139736423841732040E-16, 0.000000000000000000 ) ) ;
#135956=ORIENTED_EDGE ( 'NONE', *, *, #24166, .T. ) ;
#135962=ADVANCED_FACE ( 'NONE', ( #40221 ), #17651, .T. ) ;
#135966=DIRECTION ( 'NONE',  ( 0.000000000000000000, -1.000000000000000000, 0.000000000000000000 ) ) ;
#136003=VERTEX_POINT ( 'NONE', #8919 ) ;
#136056=CARTESIAN_POINT ( 'NONE',  ( 12.08840764549667668, 2.500000000000003553, 3.061616997868386099E-16 ) ) ;
#136067=FACE_OUTER_BOUND ( 'NONE', #139784, .T. ) ;
#136068=ORIENTED_EDGE ( 'NONE', *, *, #23128, .T. ) ;
#136080=DIRECTION ( 'NONE',  ( -1.000000000000000000, -0.000000000000000000, -0.000000000000000000 ) ) ;
#136097=DIRECTION ( 'NONE',  ( -1.000000000000000000, -1.224606353822377258E-16, -0.000000000000000000 ) ) ;
#136143=DIRECTION ( 'NONE',  ( -1.000000000000000000, -1.224606353822377258E-16, -0.000000000000000000 ) ) ;
#136152=VECTOR ( 'NONE', #62353, 1000.000000000000000 ) ;
#136167=CARTESIAN_POINT ( 'NONE',  ( 9.748407645496676821, 9.139736423841732040E-16, 0.000000000000000000 ) ) ;
#136250=CYLINDRICAL_SURFACE ( 'NONE', #5359, 2.500000000000000000 ) ;
#136284=EDGE_CURVE ( 'NONE', #12574, #70009, #131104, .T. ) ;
#136312=EDGE_CURVE ( 'NONE', #118985, #69799, #13096, .T. ) ;
#136315=ORIENTED_EDGE ( 'NONE', *, *, #22191, .F. ) ;
#136338=AXIS2_PLACEMENT_3D ( 'NONE', #24349, #22882, #91064 ) ;
#136366=DIRECTION ( 'NONE',  ( -0.5735764363510507113, 0.8191520442889885789, 1.003171929053520926E-16 ) ) ;
#136372=VERTEX_POINT ( 'NONE', #138630 ) ;
#136381=ORIENTED_EDGE ( 'NONE', *, *, #4822, .F. ) ;
#136444=EDGE_CURVE ( 'NONE', #138815, #57169, #103442, .T. ) ;
#136449=VECTOR ( 'NONE', #58647, 1000.000000000000114 ) ;
#136459=DIRECTION ( 'NONE',  ( 0.000000000000000000, 0.000000000000000000, -1.000000000000000000 ) ) ;
#136539=AXIS2_PLACEMENT_3D ( 'NONE', #80584, #1537, #89995 ) ;
#136601=EDGE_LOOP ( 'NONE', ( #58662, #52276, #134792, #89730 ) ) ;
#136613=DIRECTION ( 'NONE',  ( 0.000000000000000000, 1.687538997430237626E-14, 1.000000000000000000 ) ) ;
#136629=ADVANCED_FACE ( 'NONE', ( #15898 ), #40960, .T. ) ;
#136644=VECTOR ( 'NONE', #102857, 1000.000000000000114 ) ;
#136655=EDGE_CURVE ( 'NONE', #52944, #92199, #54843, .T. ) ;
#136669=DIRECTION ( 'NONE',  ( -1.000000000000000000, -1.224606353822377258E-16, -0.000000000000000000 ) ) ;
#136695=CARTESIAN_POINT ( 'NONE',  ( 24.09999999999999787, -2.055000000000000160, 0.000000000000000000 ) ) ;
#136701=CARTESIAN_POINT ( 'NONE',  ( 24.41159235450331977, 9.902892378096218942E-16, 0.000000000000000000 ) ) ;
#136711=VECTOR ( 'NONE', #58857, 1000.000000000000000 ) ;
#136730=DIRECTION ( 'NONE',  ( 0.000000000000000000, 0.000000000000000000, 1.000000000000000000 ) ) ;
#136757=ORIENTED_EDGE ( 'NONE', *, *, #106663, .F. ) ;
#136764=CARTESIAN_POINT ( 'NONE',  ( 10.06000000000000050, 2.055000000000001492, 2.516649172247811554E-16 ) ) ;
#136780=ADVANCED_FACE ( 'NONE', ( #83355 ), #84943, .T. ) ;
#136830=AXIS2_PLACEMENT_3D ( 'NONE', #29787, #52962, #61745 ) ;
#136856=CARTESIAN_POINT ( 'NONE',  ( 4.911592354503321545, 9.902892378096218942E-16, 0.000000000000000000 ) ) ;
#136880=EDGE_CURVE ( 'NONE', #23695, #130192, #63756, .T. ) ;
#137050=LINE ( 'NONE', #92819, #76919 ) ;
#137058=EDGE_CURVE ( 'NONE', #91883, #21154, #123852, .T. ) ;
#137066=VERTEX_POINT ( 'NONE', #112250 ) ;
#137080=DIRECTION ( 'NONE',  ( 0.000000000000000000, -1.000000000000000000, 0.000000000000000000 ) ) ;
#137097=VECTOR ( 'NONE', #38265, 1000.000000000000000 ) ;
#137101=CARTESIAN_POINT ( 'NONE',  ( 8.188407645496676324, -2.499999999999998224, 0.000000000000000000 ) ) ;
#137108=CARTESIAN_POINT ( 'NONE',  ( 25.97159235450331849, -2.500000000000000444, 3.061616997868384620E-16 ) ) ;
#137112=LINE ( 'NONE', #28357, #43761 ) ;
#137148=DIRECTION ( 'NONE',  ( -1.000000000000000000, -1.224606353822377258E-16, -0.000000000000000000 ) ) ;
#137165=ORIENTED_EDGE ( 'NONE', *, *, #16379, .F. ) ;
#137201=AXIS2_PLACEMENT_3D ( 'NONE', #16185, #60477, #103223 ) ;
#137207=VERTEX_POINT ( 'NONE', #98163 ) ;
#137241=ORIENTED_EDGE ( 'NONE', *, *, #92064, .F. ) ;
#137267=FACE_OUTER_BOUND ( 'NONE', #2170, .T. ) ;
#137281=AXIS2_PLACEMENT_3D ( 'NONE', #64235, #63554, #64963 ) ;
#137284=ADVANCED_FACE ( 'NONE', ( #141673 ), #54942, .T. ) ;
#137342=AXIS2_PLACEMENT_3D ( 'NONE', #130095, #30791, #75715 ) ;
#137389=CARTESIAN_POINT ( 'NONE',  ( 12.86840764549667604, 9.139736423841732040E-16, 0.000000000000000000 ) ) ;
#137401=DIRECTION ( 'NONE',  ( -1.000000000000000000, -0.000000000000000000, -0.000000000000000000 ) ) ;
#137448=ORIENTED_EDGE ( 'NONE', *, *, #124330, .T. ) ;
#137464=ORIENTED_EDGE ( 'NONE', *, *, #139070, .T. ) ;
#137493=CARTESIAN_POINT ( 'NONE',  ( 5.848407645496676466, 2.500000000000002220, 3.061616997868384620E-16 ) ) ;
#137562=FACE_OUTER_BOUND ( 'NONE', #141403, .T. ) ;
#137567=VECTOR ( 'NONE', #50962, 1000.000000000000000 ) ;
#137632=EDGE_CURVE ( 'NONE', #40894, #24671, #132058, .T. ) ;
#137639=DIRECTION ( 'NONE',  ( -1.000000000000000000, -1.224606353822377258E-16, -0.000000000000000000 ) ) ;
#137649=DIRECTION ( 'NONE',  ( 0.5735764363510453823, -0.8191520442889923537, 1.003171929053525486E-16 ) ) ;
#137689=CIRCLE ( 'NONE', #21964, 2.500000000000000888 ) ;
#137699=DIRECTION ( 'NONE',  ( 1.000000000000000000, 1.224606353822377258E-16, 0.000000000000000000 ) ) ;
#137722=CARTESIAN_POINT ( 'NONE',  ( 18.17159235450331778, 3.061616997868380183E-16, -2.500000000000001332 ) ) ;
#137764=DIRECTION ( 'NONE',  ( 0.000000000000000000, -1.000000000000000000, 0.000000000000000000 ) ) ;
#137836=DIRECTION ( 'NONE',  ( 0.000000000000000000, -1.000000000000000000, 0.000000000000000000 ) ) ;
#137845=DIRECTION ( 'NONE',  ( 0.000000000000000000, -1.000000000000000000, 0.000000000000000000 ) ) ;
#137872=DIRECTION ( 'NONE',  ( 0.000000000000000000, -1.000000000000000000, 0.000000000000000000 ) ) ;
#137894=DIRECTION ( 'NONE',  ( -1.000000000000000000, -0.000000000000000000, -0.000000000000000000 ) ) ;
#137897=EDGE_CURVE ( 'NONE', #90786, #27619, #81253, .T. ) ;
#137906=EDGE_CURVE ( 'NONE', #32667, #105469, #45944, .T. ) ;
#137913=CYLINDRICAL_SURFACE ( 'NONE', #85723, 2.500000000000000000 ) ;
#137915=VERTEX_POINT ( 'NONE', #119527 ) ;
#137936=ORIENTED_EDGE ( 'NONE', *, *, #20026, .T. ) ;
#137992=ADVANCED_FACE ( 'NONE', ( #130462 ), #7923, .T. ) ;
#137996=DIRECTION ( 'NONE',  ( -1.000000000000000000, -0.000000000000000000, -0.000000000000000000 ) ) ;
#137998=ORIENTED_EDGE ( 'NONE', *, *, #18616, .T. ) ;
#138029=EDGE_CURVE ( 'NONE', #44190, #142002, #8606, .T. ) ;
#138067=LINE ( 'NONE', #37332, #139752 ) ;
#138069=VERTEX_POINT ( 'NONE', #78219 ) ;
#138107=FACE_OUTER_BOUND ( 'NONE', #40229, .T. ) ;
#138142=DIRECTION ( 'NONE',  ( 0.5735764363510451602, 0.8191520442889924647, 0.000000000000000000 ) ) ;
#138175=ORIENTED_EDGE ( 'NONE', *, *, #91564, .F. ) ;
#138215=DIRECTION ( 'NONE',  ( -1.000000000000000000, -1.224606353822377258E-16, -0.000000000000000000 ) ) ;
#138225=LINE ( 'NONE', #84573, #41933 ) ;
#138230=EDGE_CURVE ( 'NONE', #108448, #44918, #41249, .T. ) ;
#138236=CARTESIAN_POINT ( 'NONE',  ( 27.53159235450332076, 9.902892378096218942E-16, 0.000000000000000000 ) ) ;
#138266=DIRECTION ( 'NONE',  ( 0.000000000000000000, -1.000000000000000000, 0.000000000000000000 ) ) ;
#138290=DIRECTION ( 'NONE',  ( -1.000000000000000000, -1.224606353822377258E-16, -0.000000000000000000 ) ) ;
#138330=VERTEX_POINT ( 'NONE', #24530 ) ;
#138333=AXIS2_PLACEMENT_3D ( 'NONE', #34707, #57911, #78944 ) ;
#138352=CARTESIAN_POINT ( 'NONE',  ( 25.19159235450331735, -2.500000000000000000, 3.061616997868384127E-16 ) ) ;
#138392=ORIENTED_EDGE ( 'NONE', *, *, #133181, .F. ) ;
#138408=DIRECTION ( 'NONE',  ( 0.000000000000000000, 0.000000000000000000, 1.000000000000000000 ) ) ;
#138409=DIRECTION ( 'NONE',  ( 0.5735764363510451602, 0.8191520442889924647, 0.000000000000000000 ) ) ;
#138411=EDGE_CURVE ( 'NONE', #77035, #109693, #140902, .T. ) ;
#138456=LINE ( 'NONE', #94919, #47227 ) ;
#138560=EDGE_LOOP ( 'NONE', ( #68872, #137448, #17895, #90333, #37280 ) ) ;
#138599=CIRCLE ( 'NONE', #66981, 2.055000000000001048 ) ;
#138601=DIRECTION ( 'NONE',  ( -1.000000000000000000, -0.000000000000000000, -0.000000000000000000 ) ) ;
#138612=CARTESIAN_POINT ( 'NONE',  ( 7.251592354503322291, 2.500000000000001332, 0.000000000000000000 ) ) ;
#138630=CARTESIAN_POINT ( 'NONE',  ( 18.32840764549667512, 3.061616997868380183E-16, -2.500000000000001332 ) ) ;
#138675=ORIENTED_EDGE ( 'NONE', *, *, #66744, .F. ) ;
#138691=AXIS2_PLACEMENT_3D ( 'NONE', #2103, #69583, #113766 ) ;
#138701=CONICAL_SURFACE ( 'NONE', #134148, 2.500000000000000888, 0.9599310885968822538 ) ;
#138717=DIRECTION ( 'NONE',  ( 0.000000000000000000, -1.000000000000000000, 0.000000000000000000 ) ) ;
#138775=CARTESIAN_POINT ( 'NONE',  ( -25.39999999999996305, 0.000000000000000000, 0.000000000000000000 ) ) ;
#138815=VERTEX_POINT ( 'NONE', #50999 ) ;
#138859=VECTOR ( 'NONE', #137649, 999.9999999999998863 ) ;
#138935=DIRECTION ( 'NONE',  ( -1.000000000000000000, -0.000000000000000000, -0.000000000000000000 ) ) ;
#138957=EDGE_CURVE ( 'NONE', #94195, #90453, #25305, .T. ) ;
#138960=DIRECTION ( 'NONE',  ( 0.5735764363510451602, 0.8191520442889924647, 0.000000000000000000 ) ) ;
#138966=ORIENTED_EDGE ( 'NONE', *, *, #83978, .T. ) ;
#139008=CARTESIAN_POINT ( 'NONE',  ( 27.53159235450332076, 9.902892378096218942E-16, 0.000000000000000000 ) ) ;
#139061=ORIENTED_EDGE ( 'NONE', *, *, #87391, .F. ) ;
#139070=EDGE_CURVE ( 'NONE', #38741, #12574, #48394, .T. ) ;
#139128=DIRECTION ( 'NONE',  ( -1.000000000000000000, -0.000000000000000000, -0.000000000000000000 ) ) ;
#139165=CIRCLE ( 'NONE', #97527, 2.055000000000001048 ) ;
#139177=VERTEX_POINT ( 'NONE', #92885 ) ;
#139180=EDGE_CURVE ( 'NONE', #31468, #54110, #50780, .T. ) ;
#139203=AXIS2_PLACEMENT_3D ( 'NONE', #125542, #74005, #120313 ) ;
#139214=CYLINDRICAL_SURFACE ( 'NONE', #14918, 2.500000000000000000 ) ;
#139224=ORIENTED_EDGE ( 'NONE', *, *, #138029, .F. ) ;
#139237=EDGE_LOOP ( 'NONE', ( #70556, #141600 ) ) ;
#139253=CARTESIAN_POINT ( 'NONE',  ( 10.52840764549667618, 9.139736423841732040E-16, 0.000000000000000000 ) ) ;
#139304=EDGE_LOOP ( 'NONE', ( #53972, #86550, #3117, #1866, #70407, #98654 ) ) ;
#139309=FACE_OUTER_BOUND ( 'NONE', #38302, .T. ) ;
#139319=APPLICATION_CONTEXT ( 'automotive_design' ) ;
#139327=LINE ( 'NONE', #141436, #74516 ) ;
#139346=DIRECTION ( 'NONE',  ( 0.000000000000000000, -1.000000000000000000, 0.000000000000000000 ) ) ;
#139377=DIRECTION ( 'NONE',  ( 1.000000000000000000, 1.224606353822377258E-16, 0.000000000000000000 ) ) ;
#139383=DIRECTION ( 'NONE',  ( -1.000000000000000000, -1.224606353822377258E-16, -0.000000000000000000 ) ) ;
#139406=AXIS2_PLACEMENT_3D ( 'NONE', #50774, #64499, #95692 ) ;
#139438=CIRCLE ( 'NONE', #83869, 2.500000000000000888 ) ;
#139446=CARTESIAN_POINT ( 'NONE',  ( 13.49159235450332162, 3.061616997868380183E-16, -2.500000000000001332 ) ) ;
#139470=CARTESIAN_POINT ( 'NONE',  ( -25.39999999999996305, 0.000000000000000000, 0.000000000000000000 ) ) ;
#139473=VECTOR ( 'NONE', #23220, 1000.000000000000000 ) ;
#139477=VECTOR ( 'NONE', #51868, 999.9999999999998863 ) ;
#139481=EDGE_LOOP ( 'NONE', ( #5148, #17514, #124464, #49477, #53546 ) ) ;
#139492=CARTESIAN_POINT ( 'NONE',  ( -25.39999999999996305, 0.000000000000000000, 0.000000000000000000 ) ) ;
#139517=ORIENTED_EDGE ( 'NONE', *, *, #123057, .T. ) ;
#139539=AXIS2_PLACEMENT_3D ( 'NONE', #35228, #80159, #23603 ) ;
#139554=FACE_OUTER_BOUND ( 'NONE', #105745, .T. ) ;
#139574=DIRECTION ( 'NONE',  ( -1.000000000000000000, -0.000000000000000000, -0.000000000000000000 ) ) ;
#139575=CARTESIAN_POINT ( 'NONE',  ( -25.39999999999996305, 0.000000000000000000, 2.500000000000000000 ) ) ;
#139607=DIRECTION ( 'NONE',  ( -0.5735764363510507113, 0.8191520442889885789, 1.003171929053520926E-16 ) ) ;
#139611=ORIENTED_EDGE ( 'NONE', *, *, #47991, .F. ) ;
#139657=ORIENTED_EDGE ( 'NONE', *, *, #104694, .T. ) ;
#139661=AXIS2_PLACEMENT_3D ( 'NONE', #138236, #17847, #62839 ) ;
#139731=VECTOR ( 'NONE', #138142, 1000.000000000000000 ) ;
#139733=ORIENTED_EDGE ( 'NONE', *, *, #130756, .F. ) ;
#139747=ORIENTED_EDGE ( 'NONE', *, *, #124875, .T. ) ;
#139752=VECTOR ( 'NONE', #81572, 1000.000000000000000 ) ;
#139762=EDGE_CURVE ( 'NONE', #4396, #137207, #78623, .T. ) ;
#139781=FACE_OUTER_BOUND ( 'NONE', #93341, .T. ) ;
#139784=EDGE_LOOP ( 'NONE', ( #10837, #95841, #76466, #10246, #62454, #59632 ) ) ;
#139785=DIRECTION ( 'NONE',  ( 0.000000000000000000, -1.000000000000000000, 0.000000000000000000 ) ) ;
#139796=ORIENTED_EDGE ( 'NONE', *, *, #55093, .T. ) ;
#139813=DIRECTION ( 'NONE',  ( 0.5735764363510451602, 0.8191520442889924647, 0.000000000000000000 ) ) ;
#139820=CARTESIAN_POINT ( 'NONE',  ( 5.380000000000000782, 9.521314400968980422E-16, 0.000000000000000000 ) ) ;
#139914=DIRECTION ( 'NONE',  ( 0.000000000000000000, -1.000000000000000000, 0.000000000000000000 ) ) ;
#139947=CARTESIAN_POINT ( 'NONE',  ( 22.53999999999999915, -2.055000000000000160, 2.789133085058098087E-16 ) ) ;
#139953=VERTEX_POINT ( 'NONE', #41032 ) ;
#139966=VERTEX_POINT ( 'NONE', #62094 ) ;
#139979=DIRECTION ( 'NONE',  ( -0.5735764363510503783, -0.8191520442889886899, 0.000000000000000000 ) ) ;
#140002=DIRECTION ( 'NONE',  ( -1.000000000000000000, -1.224606353822377258E-16, -0.000000000000000000 ) ) ;
#140013=ORIENTED_EDGE ( 'NONE', *, *, #38428, .T. ) ;
#140043=EDGE_LOOP ( 'NONE', ( #92092, #108286, #23877, #94491, #88381 ) ) ;
#140093=CARTESIAN_POINT ( 'NONE',  ( 26.12840764549667583, 3.061616997868380183E-16, -2.500000000000001332 ) ) ;
#140106=ORIENTED_EDGE ( 'NONE', *, *, #104091, .F. ) ;
#140136=LINE ( 'NONE', #17597, #638 ) ;
#140141=CARTESIAN_POINT ( 'NONE',  ( 14.27159235450332098, 9.902892378096218942E-16, 0.000000000000000000 ) ) ;
#140163=ORIENTED_EDGE ( 'NONE', *, *, #20901, .F. ) ;
#140172=DIRECTION ( 'NONE',  ( -1.000000000000000000, -1.224606353822377258E-16, -0.000000000000000000 ) ) ;
#140228=EDGE_CURVE ( 'NONE', #69799, #1792, #76460, .T. ) ;
#140257=CARTESIAN_POINT ( 'NONE',  ( 4.600000000000001421, -2.055000000000000160, 2.789133085058098087E-16 ) ) ;
#140261=DIRECTION ( 'NONE',  ( -1.000000000000000000, -1.224606353822377258E-16, -0.000000000000000000 ) ) ;
#140313=CARTESIAN_POINT ( 'NONE',  ( 20.97999999999999687, -2.055000000000000160, 2.789133085058098087E-16 ) ) ;
#140372=EDGE_LOOP ( 'NONE', ( #65359, #105518, #46177, #124027, #48081 ) ) ;
#140376=EDGE_CURVE ( 'NONE', #124257, #135110, #23222, .T. ) ;
#140452=ORIENTED_EDGE ( 'NONE', *, *, #18633, .T. ) ;
#140462=LINE ( 'NONE', #6334, #104873 ) ;
#140502=AXIS2_PLACEMENT_3D ( 'NONE', #75306, #76744, #97752 ) ;
#140509=ORIENTED_EDGE ( 'NONE', *, *, #91494, .T. ) ;
#140519=LINE ( 'NONE', #41210, #39629 ) ;
#140544=EDGE_CURVE ( 'NONE', #786, #41180, #141314, .T. ) ;
#140549=CARTESIAN_POINT ( 'NONE',  ( 22.22840764549667725, 9.139736423841732040E-16, 0.000000000000000000 ) ) ;
#140618=DIRECTION ( 'NONE',  ( -1.000000000000000000, -0.000000000000000000, -0.000000000000000000 ) ) ;
#140623=CARTESIAN_POINT ( 'NONE',  ( 8.811592354503320124, -2.500000000000000444, 3.061616997868384620E-16 ) ) ;
#140650=CARTESIAN_POINT ( 'NONE',  ( 9.279999999999999361, -2.055000000000000160, 2.789133085058098087E-16 ) ) ;
#140698=CARTESIAN_POINT ( 'NONE',  ( 22.53999999999999915, 2.055000000000001492, 2.516649172247811554E-16 ) ) ;
#140709=VERTEX_POINT ( 'NONE', #29611 ) ;
#140769=EDGE_CURVE ( 'NONE', #109323, #84890, #83497, .T. ) ;
#140800=CARTESIAN_POINT ( 'NONE',  ( 7.251592354503322291, 9.902892378096218942E-16, 0.000000000000000000 ) ) ;
#140810=DIRECTION ( 'NONE',  ( -1.000000000000000000, -0.000000000000000000, -0.000000000000000000 ) ) ;
#140869=EDGE_CURVE ( 'NONE', #87975, #41180, #140519, .T. ) ;
#140880=DIRECTION ( 'NONE',  ( 0.000000000000000000, -1.000000000000000000, 0.000000000000000000 ) ) ;
#140902=CIRCLE ( 'NONE', #13603, 2.055000000000001048 ) ;
#140951=CARTESIAN_POINT ( 'NONE',  ( 8.500000000000000000, 9.521314400968980422E-16, 0.000000000000000000 ) ) ;
#140976=LINE ( 'NONE', #64880, #139477 ) ;
#140998=AXIS2_PLACEMENT_3D ( 'NONE', #61033, #72620, #137845 ) ;
#141007=ORIENTED_EDGE ( 'NONE', *, *, #62147, .F. ) ;
#141014=DIRECTION ( 'NONE',  ( -1.000000000000000000, -0.000000000000000000, -0.000000000000000000 ) ) ;
#141080=CARTESIAN_POINT ( 'NONE',  ( 6.471592354503322042, 9.902892378096218942E-16, 0.000000000000000000 ) ) ;
#141090=VECTOR ( 'NONE', #16935, 999.9999999999998863 ) ;
#141126=DIRECTION ( 'NONE',  ( -1.000000000000000000, -1.224606353822377258E-16, -0.000000000000000000 ) ) ;
#141152=EDGE_CURVE ( 'NONE', #42879, #110325, #92552, .T. ) ;
#141191=CIRCLE ( 'NONE', #46360, 2.500000000000000888 ) ;
#141227=DIRECTION ( 'NONE',  ( -1.000000000000000000, -1.224606353822377258E-16, -0.000000000000000000 ) ) ;
#141232=CONICAL_SURFACE ( 'NONE', #39439, 2.500000000000000888, 0.9599310885968822538 ) ;
#141255=CARTESIAN_POINT ( 'NONE',  ( 6.160000000000001030, -2.055000000000000160, 2.789133085058098087E-16 ) ) ;
#141280=ORIENTED_EDGE ( 'NONE', *, *, #51503, .F. ) ;
#141281=DIRECTION ( 'NONE',  ( -1.000000000000000000, -0.000000000000000000, -0.000000000000000000 ) ) ;
#141289=DIRECTION ( 'NONE',  ( 0.000000000000000000, -1.000000000000000000, 0.000000000000000000 ) ) ;
#141293=CARTESIAN_POINT ( 'NONE',  ( 15.83159235450332147, 2.500000000000001776, 0.000000000000000000 ) ) ;
#141295=CARTESIAN_POINT ( 'NONE',  ( 17.54840764549667398, 0.000000000000000000, 2.500000000000001332 ) ) ;
#141314=CIRCLE ( 'NONE', #44167, 2.500000000000000888 ) ;
#141375=DIRECTION ( 'NONE',  ( -1.000000000000000000, -1.224606353822377258E-16, -0.000000000000000000 ) ) ;
#141403=EDGE_LOOP ( 'NONE', ( #33186, #83056, #12043, #48257, #96188, #123381 ) ) ;
#141408=CIRCLE ( 'NONE', #81206, 2.500000000000000888 ) ;
#141433=CARTESIAN_POINT ( 'NONE',  ( 0.5724039806122919183, -0.5999999999999993117, -4.262472862582124655 ) ) ;
#141436=CARTESIAN_POINT ( 'NONE',  ( -25.39999999999996305, 0.000000000000000000, 2.500000000000000000 ) ) ;
#141447=DIRECTION ( 'NONE',  ( -1.000000000000000000, -1.224606353822377258E-16, -0.000000000000000000 ) ) ;
#141464=EDGE_CURVE ( 'NONE', #21453, #127775, #2625, .T. ) ;
#141472=ORIENTED_EDGE ( 'NONE', *, *, #130521, .T. ) ;
#141480=ADVANCED_FACE ( 'NONE', ( #122897 ), #118436, .T. ) ;
#141482=DIRECTION ( 'NONE',  ( -1.000000000000000000, -1.224606353822377258E-16, -0.000000000000000000 ) ) ;
#141491=LINE ( 'NONE', #129169, #21263 ) ;
#141514=DIRECTION ( 'NONE',  ( -0.5735764363510507113, 0.8191520442889885789, 1.003171929053520926E-16 ) ) ;
#141523=CARTESIAN_POINT ( 'NONE',  ( 21.29159235450332233, 9.902892378096218942E-16, 0.000000000000000000 ) ) ;
#141530=DIRECTION ( 'NONE',  ( -1.000000000000000000, -1.224606353822377258E-16, -0.000000000000000000 ) ) ;
#141598=CARTESIAN_POINT ( 'NONE',  ( 13.18000000000000149, 2.055000000000001492, 0.000000000000000000 ) ) ;
#141600=ORIENTED_EDGE ( 'NONE', *, *, #112289, .F. ) ;
#141607=CARTESIAN_POINT ( 'NONE',  ( -25.39999999999996305, 0.000000000000000000, 2.500000000000000000 ) ) ;
#141658=DIRECTION ( 'NONE',  ( 0.000000000000000000, 0.000000000000000000, 1.000000000000000000 ) ) ;
#141673=FACE_OUTER_BOUND ( 'NONE', #125608, .T. ) ;
#141686=VERTEX_POINT ( 'NONE', #9662 ) ;
#141735=ORIENTED_EDGE ( 'NONE', *, *, #39157, .F. ) ;
#141781=DIRECTION ( 'NONE',  ( 0.000000000000000000, 1.000000000000000000, 0.000000000000000000 ) ) ;
#141836=AXIS2_PLACEMENT_3D ( 'NONE', #69176, #137996, #49585 ) ;
#141846=CIRCLE ( 'NONE', #113993, 2.500000000000000888 ) ;
#141860=CARTESIAN_POINT ( 'NONE',  ( 0.02904021785397910282, -0.6000000000000001998, 3.399959840769902097 ) ) ;
#141879=CARTESIAN_POINT ( 'NONE',  ( 5.848407645496676466, -3.851859888774471706E-31, 2.500000000000001332 ) ) ;
#141964=ORIENTED_EDGE ( 'NONE', *, *, #81664, .T. ) ;
#142002=VERTEX_POINT ( 'NONE', #106658 ) ;
#142033=EDGE_CURVE ( 'NONE', #64109, #99607, #101988, .T. ) ;
#142073=CARTESIAN_POINT ( 'NONE',  ( 26.75159235450331963, 9.902892378096218942E-16, 0.000000000000000000 ) ) ;
#142086=VECTOR ( 'NONE', #60465, 1000.000000000000000 ) ;
#142087=ORIENTED_EDGE ( 'NONE', *, *, #128694, .T. ) ;
#142095=CARTESIAN_POINT ( 'NONE',  ( 17.07999999999999829, 9.521314400968980422E-16, 0.000000000000000000 ) ) ;
#142106=DIRECTION ( 'NONE',  ( 0.000000000000000000, 1.000000000000000000, 0.000000000000000000 ) ) ;
#142149=ORIENTED_EDGE ( 'NONE', *, *, #133181, .T. ) ;
#142171=DIRECTION ( 'NONE',  ( -1.000000000000000000, -0.000000000000000000, -0.000000000000000000 ) ) ;
#142190=DIRECTION ( 'NONE',  ( 0.000000000000000000, -1.000000000000000000, 0.000000000000000000 ) ) ;
#142208=ORIENTED_EDGE ( 'NONE', *, *, #62036, .F. ) ;
#142256=ORIENTED_EDGE ( 'NONE', *, *, #98802, .F. ) ;
#142287=CYLINDRICAL_SURFACE ( 'NONE', #32047, 2.500000000000000000 ) ;
#142352=CARTESIAN_POINT ( 'NONE',  ( 24.41159235450331977, 2.500000000000001332, 0.000000000000000000 ) ) ;
#142375=ORIENTED_EDGE ( 'NONE', *, *, #19027, .T. ) ;
#142386=CARTESIAN_POINT ( 'NONE',  ( 22.85159235450332105, -2.500000000000000444, 3.061616997868384620E-16 ) ) ;
#142398=AXIS2_PLACEMENT_3D ( 'NONE', #48180, #4597, #118222 ) ;
#142439=ORIENTED_EDGE ( 'NONE', *, *, #27402, .T. ) ;
#142502=DIRECTION ( 'NONE',  ( -1.000000000000000000, -1.224606353822377258E-16, -0.000000000000000000 ) ) ;
#142517=CYLINDRICAL_SURFACE ( 'NONE', #90835, 2.500000000000000000 ) ;
#142548=FACE_OUTER_BOUND ( 'NONE', #4538, .T. ) ;
#142591=ADVANCED_FACE ( 'NONE', ( #67486 ), #13050, .T. ) ;
#142623=CARTESIAN_POINT ( 'NONE',  ( 16.61159235450331906, 2.500000000000001776, 0.000000000000000000 ) ) ;
#142640=ORIENTED_EDGE ( 'NONE', *, *, #113946, .T. ) ;
#142707=EDGE_LOOP ( 'NONE', ( #14393, #33350, #124804, #80440, #2750, #124134 ) ) ;
#142718=CARTESIAN_POINT ( 'NONE',  ( 20.66840764549667497, 3.061616997868385113E-16, -2.500000000000001332 ) ) ;
#142721=AXIS2_PLACEMENT_3D ( 'NONE', #94787, #71652, #126707 ) ;
#142728=VECTOR ( 'NONE', #61765, 1000.000000000000114 ) ;
#142759=PRODUCT ( 'slotted pan head screw_iso_ISO 1580 - M5 x 25 - 25S', 'slotted pan head screw_iso_ISO 1580 - M5 x 25 - 25S', '', ( #60576 ) ) ;
#142781=AXIS2_PLACEMENT_3D ( 'NONE', #70382, #113827, #80513 ) ;
#142790=CARTESIAN_POINT ( 'NONE',  ( 20.51159235450331764, -3.851859888774471706E-31, 2.500000000000001332 ) ) ;
#142800=DIRECTION ( 'NONE',  ( -1.000000000000000000, -1.224606353822377258E-16, -0.000000000000000000 ) ) ;
#142801=ADVANCED_FACE ( 'NONE', ( #94181 ), #74379, .T. ) ;
#142827=EDGE_CURVE ( 'NONE', #57169, #27842, #119488, .T. ) ;
#142851=VECTOR ( 'NONE', #89934, 999.9999999999998863 ) ;
#142859=CARTESIAN_POINT ( 'NONE',  ( -4.921261423547484970E-16, -0.5999999999999994227, -3.228048788193037755 ) ) ;
#142881=ORIENTED_EDGE ( 'NONE', *, *, #99509, .F. ) ;
#142892=CONICAL_SURFACE ( 'NONE', #57237, 2.055000000000001048, 0.9599310885968758145 ) ;
#142895=EDGE_CURVE ( 'NONE', #9148, #29128, #65893, .T. ) ;
#142937=ORIENTED_EDGE ( 'NONE', *, *, #16118, .F. ) ;
#142986=ADVANCED_FACE ( 'NONE', ( #1284 ), #35065, .T. ) ;
#143027=CARTESIAN_POINT ( 'NONE',  ( -25.39999999999996305, 3.061616997868383141E-16, -2.500000000000000000 ) ) ;
#143051=DIRECTION ( 'NONE',  ( -1.000000000000000000, -1.224606353822377258E-16, -0.000000000000000000 ) ) ;
#143074=CIRCLE ( 'NONE', #87506, 2.500000000000000888 ) ;
#143077=ORIENTED_EDGE ( 'NONE', *, *, #106005, .T. ) ;
#143107=DIRECTION ( 'NONE',  ( -1.000000000000000000, -1.224606353822377258E-16, -0.000000000000000000 ) ) ;
#143113=CARTESIAN_POINT ( 'NONE',  ( 18.17159235450331778, 9.902892378096218942E-16, 0.000000000000000000 ) ) ;
#143153=DIRECTION ( 'NONE',  ( -1.000000000000000000, -0.000000000000000000, -0.000000000000000000 ) ) ;
#143160=CARTESIAN_POINT ( 'NONE',  ( 26.90840764549667696, 9.139736423841732040E-16, 0.000000000000000000 ) ) ;
#143169=DIRECTION ( 'NONE',  ( -1.000000000000000000, -0.000000000000000000, -0.000000000000000000 ) ) ;
#143237=DIRECTION ( 'NONE',  ( 0.000000000000000000, -1.000000000000000000, 0.000000000000000000 ) ) ;
#143241=VERTEX_POINT ( 'NONE', #39676 ) ;
#143244=DIRECTION ( 'NONE',  ( 0.000000000000000000, 0.000000000000000000, 1.000000000000000000 ) ) ;
#143251=VERTEX_POINT ( 'NONE', #66416 ) ;
#143259=EDGE_LOOP ( 'NONE', ( #13818, #97872, #125173, #86747, #120406 ) ) ;
#143276=CIRCLE ( 'NONE', #18232, 2.500000000000000888 ) ;
#143300=EDGE_CURVE ( 'NONE', #54903, #5088, #116158, .T. ) ;
#143335=EDGE_CURVE ( 'NONE', #117466, #70361, #25815, .T. ) ;
#143336=CARTESIAN_POINT ( 'NONE',  ( 25.34840764549667469, 9.139736423841732040E-16, 0.000000000000000000 ) ) ;
#143343=ORIENTED_EDGE ( 'NONE', *, *, #74441, .T. ) ;
#143359=ADVANCED_FACE ( 'NONE', ( #142548 ), #123121, .T. ) ;
#143360=CARTESIAN_POINT ( 'NONE',  ( -25.39999999999996305, 0.000000000000000000, 2.500000000000000000 ) ) ;
#143373=AXIS2_PLACEMENT_3D ( 'NONE', #21007, #142800, #65272 ) ;
#143378=EDGE_LOOP ( 'NONE', ( #66580, #47890, #73961, #81170, #139611, #73923 ) ) ;
#143384=AXIS2_PLACEMENT_3D ( 'NONE', #117915, #96177, #28819 ) ;
#143387=CARTESIAN_POINT ( 'NONE',  ( 0.000000000000000000, 0.5999999999999987566, 4.749999999999999112 ) ) ;
#143417=ORIENTED_EDGE ( 'NONE', *, *, #43332, .T. ) ;
#143429=VERTEX_POINT ( 'NONE', #117031 ) ;
#143433=ORIENTED_EDGE ( 'NONE', *, *, #104312, .F. ) ;
#143450=EDGE_LOOP ( 'NONE', ( #6251, #118322, #127938, #53342, #68624 ) ) ;
#143462=EDGE_CURVE ( 'NONE', #5504, #57540, #51494, .T. ) ;
#143463=CARTESIAN_POINT ( 'NONE',  ( 22.53999999999999915, 9.521314400968980422E-16, 0.000000000000000000 ) ) ;
#143534=CARTESIAN_POINT ( 'NONE',  ( 10.83999999999999986, 2.055000000000001492, 2.516649172247811554E-16 ) ) ;
#143550=ORIENTED_EDGE ( 'NONE', *, *, #43374, .T. ) ;
ENDSEC;
END-ISO-10303-21;
